ISO-10303-21;
HEADER;
FILE_DESCRIPTION (('STEP AP214'),
    '1' );
FILE_NAME ('Stepper Motor.step',
    '2026-10-09T16:01:55',
    ( '' ),
    ( '' ),
    'SwSTEP 2.0',
    'SolidWorks 2024',
    '' );
FILE_SCHEMA (( 'AUTOMOTIVE_DESIGN' ));
ENDSEC;

DATA;
#4=ORIENTED_EDGE ( 'NONE', *, *, #679, .F. ) ;
#5=CIRCLE ( 'NONE', #64414, 24.99999999998794920 ) ;
#12=VERTEX_POINT ( 'NONE', #25817 ) ;
#23=AXIS2_PLACEMENT_3D ( 'NONE', #22038, #43598, #28713 ) ;
#26=EDGE_CURVE ( 'NONE', #33489, #6963, #35337, .T. ) ;
#28=VERTEX_POINT ( 'NONE', #47018 ) ;
#29=ORIENTED_EDGE ( 'NONE', *, *, #35649, .T. ) ;
#30=PLANE ( 'NONE',  #1467 ) ;
#32=ADVANCED_FACE ( 'NONE', ( #68598 ), #51631, .F. ) ;
#33=CARTESIAN_POINT ( 'NONE',  ( 32.89999999999999858, -21.00000000000001421, -13.86939075806900945 ) ) ;
#66=DIRECTION ( 'NONE',  ( -1.000000000000000000, 0.000000000000000000, 0.000000000000000000 ) ) ;
#72=ORIENTED_EDGE ( 'NONE', *, *, #39303, .F. ) ;
#82=EDGE_LOOP ( 'NONE', ( #52627, #35376, #11266, #26532 ) ) ;
#105=ORIENTED_EDGE ( 'NONE', *, *, #55339, .T. ) ;
#106=ORIENTED_EDGE ( 'NONE', *, *, #31966, .F. ) ;
#107=VECTOR ( 'NONE', #53809, 1000.000000000000000 ) ;
#108=ADVANCED_FACE ( 'NONE', ( #69649 ), #9907, .T. ) ;
#110=CARTESIAN_POINT ( 'NONE',  ( 14.89999999999999680, 13.66939075806899240, -20.79999999999999361 ) ) ;
#124=EDGE_CURVE ( 'NONE', #2059, #46953, #44248, .T. ) ;
#126=LINE ( 'NONE', #53521, #21596 ) ;
#134=DIRECTION ( 'NONE',  ( 0.000000000000000000, 0.000000000000000000, 1.000000000000000000 ) ) ;
#137=ORIENTED_EDGE ( 'NONE', *, *, #53122, .T. ) ;
#145=DIRECTION ( 'NONE',  ( 1.000000000000000000, 0.000000000000000000, 0.000000000000000000 ) ) ;
#148=EDGE_CURVE ( 'NONE', #32098, #68514, #65034, .T. ) ;
#152=CARTESIAN_POINT ( 'NONE',  ( 47.00000000000000000, 0.000000000000000000, 0.000000000000000000 ) ) ;
#158=CARTESIAN_POINT ( 'NONE',  ( 31.89999999999999858, -0.2000000000089119934, -8.913009219568841313E-12 ) ) ;
#159=ORIENTED_EDGE ( 'NONE', *, *, #8792, .F. ) ;
#188=ORIENTED_EDGE ( 'NONE', *, *, #41288, .T. ) ;
#203=EDGE_CURVE ( 'NONE', #26279, #24611, #49905, .T. ) ;
#205=ORIENTED_EDGE ( 'NONE', *, *, #6943, .T. ) ;
#213=CARTESIAN_POINT ( 'NONE',  ( 32.89999999999999858, 20.60000000000000142, 13.86939075806900057 ) ) ;
#216=DIRECTION ( 'NONE',  ( 0.000000000000000000, -0.7071067811865474617, -0.7071067811865474617 ) ) ;
#226=LINE ( 'NONE', #22825, #12692 ) ;
#243=FACE_OUTER_BOUND ( 'NONE', #8510, .T. ) ;
#245=VERTEX_POINT ( 'NONE', #54763 ) ;
#248=ORIENTED_EDGE ( 'NONE', *, *, #20850, .F. ) ;
#250=ADVANCED_FACE ( 'NONE', ( #56401 ), #28821, .T. ) ;
#253=ORIENTED_EDGE ( 'NONE', *, *, #15197, .T. ) ;
#259=DIRECTION ( 'NONE',  ( -0.000000000000000000, -0.7071067811865474617, 0.7071067811865474617 ) ) ;
#270=FACE_OUTER_BOUND ( 'NONE', #3892, .T. ) ;
#277=ADVANCED_FACE ( 'NONE', ( #51453 ), #24234, .T. ) ;
#282=EDGE_CURVE ( 'NONE', #46458, #1557, #680, .T. ) ;
#290=DIRECTION ( 'NONE',  ( 1.000000000000000000, -0.000000000000000000, 0.000000000000000000 ) ) ;
#296=DIRECTION ( 'NONE',  ( 1.000000000000000000, -0.000000000000000000, 0.000000000000000000 ) ) ;
#321=VECTOR ( 'NONE', #3166, 1000.000000000000000 ) ;
#329=CYLINDRICAL_SURFACE ( 'NONE', #52589, 2.458500000000000796 ) ;
#335=PLANE ( 'NONE',  #53647 ) ;
#361=VERTEX_POINT ( 'NONE', #69466 ) ;
#362=AXIS2_PLACEMENT_3D ( 'NONE', #29002, #49877, #27973 ) ;
#365=CARTESIAN_POINT ( 'NONE',  ( 39.00000000000000000, -21.00000000000000000, -16.96999999999999886 ) ) ;
#367=CARTESIAN_POINT ( 'NONE',  ( 39.00000000000000000, 4.286263797015736595E-16, -3.500000000000000000 ) ) ;
#371=EDGE_CURVE ( 'NONE', #42134, #10117, #15730, .T. ) ;
#372=LINE ( 'NONE', #65080, #9063 ) ;
#377=CARTESIAN_POINT ( 'NONE',  ( 25.90000000000000213, 13.66939075806899240, 20.79999999999999361 ) ) ;
#385=EDGE_CURVE ( 'NONE', #21656, #53653, #49808, .T. ) ;
#395=DIRECTION ( 'NONE',  ( 0.5001543609659999667, 1.060466075314215496E-16, 0.8659362650950080953 ) ) ;
#400=CARTESIAN_POINT ( 'NONE',  ( 0.000000000000000000, -17.79289321881345032, 20.50000000000000000 ) ) ;
#409=AXIS2_PLACEMENT_3D ( 'NONE', #62583, #37393, #19457 ) ;
#417=CARTESIAN_POINT ( 'NONE',  ( 18.89999999999999858, -21.00000000000001421, -13.86939075806900945 ) ) ;
#420=EDGE_CURVE ( 'NONE', #60080, #69579, #58869, .T. ) ;
#421=PLANE ( 'NONE',  #68238 ) ;
#426=ORIENTED_EDGE ( 'NONE', *, *, #27573, .F. ) ;
#427=VERTEX_POINT ( 'NONE', #21020 ) ;
#450=ORIENTED_EDGE ( 'NONE', *, *, #43002, .T. ) ;
#456=DIRECTION ( 'NONE',  ( 0.000000000000000000, 0.000000000000000000, -1.000000000000000000 ) ) ;
#459=CARTESIAN_POINT ( 'NONE',  ( 39.00000000000000000, -0.2000000000000000111, 0.000000000000000000 ) ) ;
#467=DIRECTION ( 'NONE',  ( 0.000000000000000000, 0.000000000000000000, -1.000000000000000000 ) ) ;
#475=DIRECTION ( 'NONE',  ( 0.000000000000000000, -0.8188976377952758012, -0.5739395950910839428 ) ) ;
#490=EDGE_CURVE ( 'NONE', #33868, #48285, #12497, .T. ) ;
#495=EDGE_CURVE ( 'NONE', #42963, #28954, #53915, .T. ) ;
#502=VECTOR ( 'NONE', #16926, 1000.000000000000000 ) ;
#522=AXIS2_PLACEMENT_3D ( 'NONE', #27556, #699, #37140 ) ;
#528=ORIENTED_EDGE ( 'NONE', *, *, #49827, .F. ) ;
#533=ORIENTED_EDGE ( 'NONE', *, *, #46307, .T. ) ;
#536=UNCERTAINTY_MEASURE_WITH_UNIT (LENGTH_MEASURE( 1.000000000000000082E-05 ), #15361, 'distance_accuracy_value', 'NONE');
#541=EDGE_CURVE ( 'NONE', #27734, #10730, #30589, .T. ) ;
#549=ORIENTED_EDGE ( 'NONE', *, *, #26936, .F. ) ;
#551=AXIS2_PLACEMENT_3D ( 'NONE', #51333, #46036, #67608 ) ;
#553=CARTESIAN_POINT ( 'NONE',  ( 36.90000000000000568, 20.60000000000000142, -13.86939075806900057 ) ) ;
#558=DIRECTION ( 'NONE',  ( -1.000000000000000000, 0.000000000000000000, 0.000000000000000000 ) ) ;
#559=COLOUR_RGB ( '', 0.08235294, 0.09019608, 0.10196078) ;
#560=CARTESIAN_POINT ( 'NONE',  ( 39.00000000000000000, -21.00000000000000000, -14.57806571531352091 ) ) ;
#562=CIRCLE ( 'NONE', #40052, 2.458500000000000796 ) ;
#564=DIRECTION ( 'NONE',  ( 1.000000000000000000, -0.000000000000000000, 0.000000000000000000 ) ) ;
#575=FACE_OUTER_BOUND ( 'NONE', #39075, .T. ) ;
#591=PLANE ( 'NONE',  #55308 ) ;
#602=ORIENTED_EDGE ( 'NONE', *, *, #62615, .F. ) ;
#609=AXIS2_PLACEMENT_3D ( 'NONE', #20518, #59049, #32541 ) ;
#612=DIRECTION ( 'NONE',  ( 1.000000000000000000, -0.000000000000000000, 0.000000000000000000 ) ) ;
#621=CARTESIAN_POINT ( 'NONE',  ( 40.90000000000000568, 21.00000000000000355, -13.98999642601812354 ) ) ;
#622=CARTESIAN_POINT ( 'NONE',  ( 14.89999999999999680, 20.60000000000000142, -13.86939075806900057 ) ) ;
#640=ORIENTED_EDGE ( 'NONE', *, *, #69472, .F. ) ;
#644=PLANE ( 'NONE',  #32533 ) ;
#654=VECTOR ( 'NONE', #47837, 1000.000000000000000 ) ;
#660=AXIS2_PLACEMENT_3D ( 'NONE', #3330, #61305, #29143 ) ;
#673=PLANE ( 'NONE',  #54224 ) ;
#679=EDGE_CURVE ( 'NONE', #53653, #2028, #29441, .T. ) ;
#680=LINE ( 'NONE', #46143, #37362 ) ;
#682=EDGE_CURVE ( 'NONE', #36598, #40990, #13532, .T. ) ;
#699=DIRECTION ( 'NONE',  ( 0.000000000000000000, -1.000000000000000000, 0.000000000000000000 ) ) ;
#711=VECTOR ( 'NONE', #11442, 1000.000000000000000 ) ;
#713=VECTOR ( 'NONE', #29747, 1000.000000000000000 ) ;
#714=AXIS2_PLACEMENT_3D ( 'NONE', #11350, #11017, #4670 ) ;
#719=AXIS2_PLACEMENT_3D ( 'NONE', #53529, #25960, #46803 ) ;
#724=ORIENTED_EDGE ( 'NONE', *, *, #43067, .T. ) ;
#729=CARTESIAN_POINT ( 'NONE',  ( 41.09999999999999432, 13.66939075806899950, 20.80000000000000426 ) ) ;
#734=DIRECTION ( 'NONE',  ( 0.000000000000000000, 0.000000000000000000, -1.000000000000000000 ) ) ;
#738=FACE_OUTER_BOUND ( 'NONE', #41918, .T. ) ;
#743=DIRECTION ( 'NONE',  ( 0.000000000000000000, 0.000000000000000000, -1.000000000000000000 ) ) ;
#755=VECTOR ( 'NONE', #5820, 1000.000000000000000 ) ;
#771=ORIENTED_EDGE ( 'NONE', *, *, #36456, .T. ) ;
#772=ADVANCED_FACE ( 'NONE', ( #63030, #46754 ), #4686, .T. ) ;
#777=CARTESIAN_POINT ( 'NONE',  ( 33.89999999999999858, -0.000000000000000000, 20.80000000000000426 ) ) ;
#780=AXIS2_PLACEMENT_3D ( 'NONE', #16871, #22182, #10518 ) ;
#784=CARTESIAN_POINT ( 'NONE',  ( 46.39999999999999858, 21.00000000000000000, -0.2500000000000000000 ) ) ;
#787=ORIENTED_EDGE ( 'NONE', *, *, #45856, .F. ) ;
#789=ORIENTED_EDGE ( 'NONE', *, *, #32438, .F. ) ;
#797=DIRECTION ( 'NONE',  ( 0.000000000000000000, 0.000000000000000000, -1.000000000000000000 ) ) ;
#804=CARTESIAN_POINT ( 'NONE',  ( 39.90000000000000568, -21.00000000000000000, 14.57806571531351914 ) ) ;
#806=DIRECTION ( 'NONE',  ( 0.000000000000000000, 0.000000000000000000, -1.000000000000000000 ) ) ;
#809=EDGE_LOOP ( 'NONE', ( #4041, #12322, #25517, #67082 ) ) ;
#813=CARTESIAN_POINT ( 'NONE',  ( 32.89999999999999858, 0.000000000000000000, 0.000000000000000000 ) ) ;
#814=ORIENTED_EDGE ( 'NONE', *, *, #16232, .F. ) ;
#820=FACE_OUTER_BOUND ( 'NONE', #25377, .T. ) ;
#843=ORIENTED_EDGE ( 'NONE', *, *, #23067, .F. ) ;
#846=DIRECTION ( 'NONE',  ( 0.000000000000000000, 1.000000000000000000, 0.000000000000000000 ) ) ;
#849=ADVANCED_FACE ( 'NONE', ( #36875 ), #67886, .F. ) ;
#856=VERTEX_POINT ( 'NONE', #64779 ) ;
#866=FACE_OUTER_BOUND ( 'NONE', #3479, .T. ) ;
#868=VERTEX_POINT ( 'NONE', #37910 ) ;
#878=ORIENTED_EDGE ( 'NONE', *, *, #43600, .T. ) ;
#940=PLANE ( 'NONE',  #55617 ) ;
#944=CARTESIAN_POINT ( 'NONE',  ( 28.90000000000000213, -0.1999999999911430404, -8.864436962241481021E-12 ) ) ;
#956=ORIENTED_EDGE ( 'NONE', *, *, #21730, .F. ) ;
#969=ORIENTED_EDGE ( 'NONE', *, *, #8252, .F. ) ;
#977=DIRECTION ( 'NONE',  ( 0.000000000000000000, 0.000000000000000000, 1.000000000000000000 ) ) ;
#1021=LINE ( 'NONE', #7329, #52709 ) ;
#1026=AXIS2_PLACEMENT_3D ( 'NONE', #14029, #61406, #51523 ) ;
#1036=ADVANCED_FACE ( 'NONE', ( #67193 ), #22806, .F. ) ;
#1061=AXIS2_PLACEMENT_3D ( 'NONE', #24470, #41423, #61936 ) ;
#1074=DIRECTION ( 'NONE',  ( 1.000000000000000000, -0.000000000000000000, 0.000000000000000000 ) ) ;
#1077=CARTESIAN_POINT ( 'NONE',  ( 48.83288643746762148, -0.7500000000000002220, 3.758927509733821726 ) ) ;
#1079=CARTESIAN_POINT ( 'NONE',  ( 41.09999999999999432, -14.06939075806900163, 20.80000000000000426 ) ) ;
#1080=AXIS2_PLACEMENT_3D ( 'NONE', #28442, #50013, #34091 ) ;
#1084=DIRECTION ( 'NONE',  ( 0.000000000000000000, 0.000000000000000000, -1.000000000000000000 ) ) ;
#1107=EDGE_LOOP ( 'NONE', ( #6092, #33644, #51229, #28813 ) ) ;
#1129=CARTESIAN_POINT ( 'NONE',  ( 0.000000000000000000, 17.79289321881347163, -20.50000000000002487 ) ) ;
#1131=CARTESIAN_POINT ( 'NONE',  ( 41.09999999999999432, 13.66939075806899950, 20.80000000000000426 ) ) ;
#1136=CARTESIAN_POINT ( 'NONE',  ( 27.90000000000000213, -21.00000000000001421, -13.86939075806900945 ) ) ;
#1137=DIRECTION ( 'NONE',  ( -1.000000000000000000, 0.000000000000000000, 0.000000000000000000 ) ) ;
#1145=ORIENTED_EDGE ( 'NONE', *, *, #54162, .T. ) ;
#1173=VECTOR ( 'NONE', #30051, 1000.000000000000000 ) ;
#1188=VECTOR ( 'NONE', #4712, 1000.000000000000000 ) ;
#1189=DIRECTION ( 'NONE',  ( 1.000000000000000000, -0.000000000000000000, 0.000000000000000000 ) ) ;
#1192=ORIENTED_EDGE ( 'NONE', *, *, #19802, .F. ) ;
#1209=AXIS2_PLACEMENT_3D ( 'NONE', #21962, #6056, #53118 ) ;
#1225=LINE ( 'NONE', #48975, #63309 ) ;
#1228=ORIENTED_EDGE ( 'NONE', *, *, #64048, .T. ) ;
#1236=DIRECTION ( 'NONE',  ( 0.000000000000000000, 0.000000000000000000, -1.000000000000000000 ) ) ;
#1240=EDGE_LOOP ( 'NONE', ( #28286, #25016, #26977, #63500 ) ) ;
#1243=CARTESIAN_POINT ( 'NONE',  ( 10.00000000000000000, 18.00000000000000355, 21.00000000000000000 ) ) ;
#1258=CARTESIAN_POINT ( 'NONE',  ( 47.00000000000000000, -0.7500000000000000000, 3.418698582794335028 ) ) ;
#1263=ORIENTED_EDGE ( 'NONE', *, *, #54330, .F. ) ;
#1292=DIRECTION ( 'NONE',  ( 0.000000000000000000, 0.000000000000000000, -1.000000000000000000 ) ) ;
#1295=AXIS2_PLACEMENT_3D ( 'NONE', #68288, #9243, #30806 ) ;
#1296=ORIENTED_EDGE ( 'NONE', *, *, #4827, .F. ) ;
#1302=VERTEX_POINT ( 'NONE', #27959 ) ;
#1307=VERTEX_POINT ( 'NONE', #10946 ) ;
#1320=DIRECTION ( 'NONE',  ( 1.000000000000000000, -0.000000000000000000, 0.000000000000000000 ) ) ;
#1331=CARTESIAN_POINT ( 'NONE',  ( 39.90000000000000568, 14.08845687959340154, -20.99999999999999645 ) ) ;
#1352=CIRCLE ( 'NONE', #39742, 25.39999999999999858 ) ;
#1359=CARTESIAN_POINT ( 'NONE',  ( 25.90000000000000213, 20.60000000000000142, 1.939442395502021001E-15 ) ) ;
#1361=CARTESIAN_POINT ( 'NONE',  ( 49.00000000000000000, -0.1999999999911430404, -8.864436962241481021E-12 ) ) ;
#1364=LINE ( 'NONE', #33536, #69805 ) ;
#1367=ADVANCED_FACE ( 'NONE', ( #38517 ), #10253, .T. ) ;
#1368=FACE_OUTER_BOUND ( 'NONE', #6690, .T. ) ;
#1369=VERTEX_POINT ( 'NONE', #53398 ) ;
#1370=EDGE_CURVE ( 'NONE', #16386, #66031, #4950, .T. ) ;
#1381=CARTESIAN_POINT ( 'NONE',  ( 7.900000000000000355, -18.00000000000000355, 21.00000000000000000 ) ) ;
#1396=ORIENTED_EDGE ( 'NONE', *, *, #50921, .T. ) ;
#1407=FACE_OUTER_BOUND ( 'NONE', #53741, .T. ) ;
#1420=ORIENTED_EDGE ( 'NONE', *, *, #47528, .F. ) ;
#1430=PLANE ( 'NONE',  #63020 ) ;
#1434=CARTESIAN_POINT ( 'NONE',  ( 10.90000000000000036, -21.00000000000001421, -13.86939075806900945 ) ) ;
#1461=ORIENTED_EDGE ( 'NONE', *, *, #25428, .F. ) ;
#1467=AXIS2_PLACEMENT_3D ( 'NONE', #20534, #63686, #37508 ) ;
#1477=VECTOR ( 'NONE', #52633, 1000.000000000000000 ) ;
#1482=( LENGTH_UNIT ( ) NAMED_UNIT ( * ) SI_UNIT ( .MILLI., .METRE. ) );
#1485=ORIENTED_EDGE ( 'NONE', *, *, #31305, .T. ) ;
#1489=CARTESIAN_POINT ( 'NONE',  ( 16.89999999999999858, -21.00000000000000000, 13.86939075806900057 ) ) ;
#1501=CARTESIAN_POINT ( 'NONE',  ( 39.90000000000000568, 20.60000000000000142, 13.86939075806899702 ) ) ;
#1526=ORIENTED_EDGE ( 'NONE', *, *, #42730, .F. ) ;
#1532=DIRECTION ( 'NONE',  ( 0.000000000000000000, -1.000000000000000000, 0.000000000000000000 ) ) ;
#1533=EDGE_LOOP ( 'NONE', ( #21122, #40347, #45235, #65247 ) ) ;
#1546=CARTESIAN_POINT ( 'NONE',  ( 49.49873889023718476, 0.7500000000000000000, 4.436432704656454895 ) ) ;
#1557=VERTEX_POINT ( 'NONE', #19704 ) ;
#1567=LINE ( 'NONE', #65589, #38121 ) ;
#1569=ORIENTED_EDGE ( 'NONE', *, *, #60453, .F. ) ;
#1574=VERTEX_POINT ( 'NONE', #62486 ) ;
#1580=EDGE_CURVE ( 'NONE', #38637, #12098, #57900, .T. ) ;
#1593=FACE_OUTER_BOUND ( 'NONE', #63694, .T. ) ;
#1595=DIRECTION ( 'NONE',  ( -1.000000000000000000, 0.000000000000000000, 0.000000000000000000 ) ) ;
#1596=CARTESIAN_POINT ( 'NONE',  ( 8.900000000000005684, -14.06939075806900163, -20.80000000000000426 ) ) ;
#1612=ORIENTED_EDGE ( 'NONE', *, *, #7995, .T. ) ;
#1620=EDGE_CURVE ( 'NONE', #61917, #27668, #9116, .T. ) ;
#1624=CARTESIAN_POINT ( 'NONE',  ( 32.89999999999999858, 20.60000000000000142, -13.86939075806900057 ) ) ;
#1625=ORIENTED_EDGE ( 'NONE', *, *, #63006, .T. ) ;
#1653=DIRECTION ( 'NONE',  ( 0.000000000000000000, 0.000000000000000000, 1.000000000000000000 ) ) ;
#1654=DIRECTION ( 'NONE',  ( 0.000000000000000000, 0.000000000000000000, 1.000000000000000000 ) ) ;
#1657=EDGE_CURVE ( 'NONE', #57888, #27734, #62142, .T. ) ;
#1678=PLANE ( 'NONE',  #59210 ) ;
#1694=VECTOR ( 'NONE', #14522, 1000.000000000000114 ) ;
#1697=DIRECTION ( 'NONE',  ( 1.000000000000000000, 0.000000000000000000, 0.000000000000000000 ) ) ;
#1705=DIRECTION ( 'NONE',  ( -1.000000000000000000, -0.000000000000000000, -0.000000000000000000 ) ) ;
#1707=VERTEX_POINT ( 'NONE', #15127 ) ;
#1709=ADVANCED_FACE ( 'NONE', ( #36689 ), #15817, .F. ) ;
#1710=ORIENTED_EDGE ( 'NONE', *, *, #124, .F. ) ;
#1713=PLANE ( 'NONE',  #57515 ) ;
#1720=DIRECTION ( 'NONE',  ( -1.000000000000000000, 0.000000000000000000, 0.000000000000000000 ) ) ;
#1728=DIRECTION ( 'NONE',  ( 1.000000000000000000, -0.000000000000000000, 0.000000000000000000 ) ) ;
#1735=DIRECTION ( 'NONE',  ( -1.000000000000000000, 0.000000000000000000, 0.000000000000000000 ) ) ;
#1739=EDGE_LOOP ( 'NONE', ( #36567, #1625, #38351, #20773 ) ) ;
#1741=VECTOR ( 'NONE', #56009, 1000.000000000000000 ) ;
#1746=PRESENTATION_STYLE_ASSIGNMENT (( #18704 ) ) ;
#1747=ORIENTED_EDGE ( 'NONE', *, *, #16600, .F. ) ;
#1752=CIRCLE ( 'NONE', #14234, 24.99999999998784972 ) ;
#1755=CARTESIAN_POINT ( 'NONE',  ( 33.89999999999999858, 0.000000000000000000, 2.801416793502919355E-15 ) ) ;
#1780=EDGE_LOOP ( 'NONE', ( #11033, #31500, #64794, #15896 ) ) ;
#1800=DIRECTION ( 'NONE',  ( 0.000000000000000000, 0.000000000000000000, -1.000000000000000000 ) ) ;
#1801=DIRECTION ( 'NONE',  ( 0.000000000000000000, -1.000000000000000000, 0.000000000000000000 ) ) ;
#1828=ORIENTED_EDGE ( 'NONE', *, *, #60940, .F. ) ;
#1839=DIRECTION ( 'NONE',  ( -1.000000000000000000, 0.000000000000000000, 0.000000000000000000 ) ) ;
#1841=CARTESIAN_POINT ( 'NONE',  ( 39.00000000000000000, 0.000000000000000000, 0.000000000000000000 ) ) ;
#1852=DIRECTION ( 'NONE',  ( 1.000000000000000000, -0.000000000000000000, 0.000000000000000000 ) ) ;
#1882=ORIENTED_EDGE ( 'NONE', *, *, #8487, .T. ) ;
#1888=CARTESIAN_POINT ( 'NONE',  ( 7.900000000000000355, -18.00000000000000355, 21.00000000000000000 ) ) ;
#1898=ORIENTED_EDGE ( 'NONE', *, *, #64918, .F. ) ;
#1904=FACE_OUTER_BOUND ( 'NONE', #24343, .T. ) ;
#1908=PRODUCT_DEFINITION_FORMATION_WITH_SPECIFIED_SOURCE ( 'ANY', '', #62794, .NOT_KNOWN. ) ;
#1910=VERTEX_POINT ( 'NONE', #50068 ) ;
#1912=CARTESIAN_POINT ( 'NONE',  ( 30.90000000000000213, -14.06939075806900874, 20.80000000000001137 ) ) ;
#1914=AXIS2_PLACEMENT_3D ( 'NONE', #5914, #612, #6257 ) ;
#1917=ORIENTED_EDGE ( 'NONE', *, *, #3301, .F. ) ;
#1919=VECTOR ( 'NONE', #20110, 1000.000000000000000 ) ;
#1925=VECTOR ( 'NONE', #33922, 1000.000000000000000 ) ;
#1934=EDGE_CURVE ( 'NONE', #57421, #59763, #7269, .T. ) ;
#1936=CARTESIAN_POINT ( 'NONE',  ( 37.90000000000000568, 0.000000000000000000, 0.000000000000000000 ) ) ;
#1940=VECTOR ( 'NONE', #64322, 1000.000000000000114 ) ;
#1988=CARTESIAN_POINT ( 'NONE',  ( 16.89999999999999858, -14.06939075806902117, -20.80000000000000426 ) ) ;
#1990=ORIENTED_EDGE ( 'NONE', *, *, #49365, .F. ) ;
#2005=EDGE_LOOP ( 'NONE', ( #28923, #44760, #13918, #33372 ) ) ;
#2012=EDGE_CURVE ( 'NONE', #55425, #68679, #66748, .T. ) ;
#2017=ADVANCED_FACE ( 'NONE', ( #30601 ), #13631, .F. ) ;
#2018=DIRECTION ( 'NONE',  ( -1.000000000000000000, 0.000000000000000000, 0.000000000000000000 ) ) ;
#2021=CARTESIAN_POINT ( 'NONE',  ( 13.90000000000000213, 20.60000000000000142, 13.86939075806899702 ) ) ;
#2022=CARTESIAN_POINT ( 'NONE',  ( 33.89999999999999858, 0.000000000000000000, 2.458500000000000796 ) ) ;
#2025=EDGE_CURVE ( 'NONE', #10730, #59143, #35908, .T. ) ;
#2028=VERTEX_POINT ( 'NONE', #46853 ) ;
#2035=PLANE ( 'NONE',  #64269 ) ;
#2036=DIRECTION ( 'NONE',  ( 0.000000000000000000, 0.000000000000000000, -1.000000000000000000 ) ) ;
#2038=ORIENTED_EDGE ( 'NONE', *, *, #28352, .T. ) ;
#2052=ADVANCED_FACE ( 'NONE', ( #14687 ), #51466, .F. ) ;
#2054=LINE ( 'NONE', #20067, #3220 ) ;
#2057=SURFACE_STYLE_FILL_AREA ( #7000 ) ;
#2059=VERTEX_POINT ( 'NONE', #36250 ) ;
#2068=DIRECTION ( 'NONE',  ( 0.000000000000000000, 0.000000000000000000, 1.000000000000000000 ) ) ;
#2070=CARTESIAN_POINT ( 'NONE',  ( 19.90000000000000213, 20.60000000000000142, -13.86939075806900057 ) ) ;
#2084=EDGE_CURVE ( 'NONE', #36374, #24688, #14347, .T. ) ;
#2089=ADVANCED_FACE ( 'NONE', ( #61721 ), #13282, .F. ) ;
#2104=CARTESIAN_POINT ( 'NONE',  ( 48.66606140682858239, -0.7499999999999964473, 3.588709161325267516 ) ) ;
#2106=EDGE_CURVE ( 'NONE', #66978, #54625, #43214, .T. ) ;
#2110=FACE_OUTER_BOUND ( 'NONE', #47645, .T. ) ;
#2173=CARTESIAN_POINT ( 'NONE',  ( 25.57999999999999829, 0.000000000000000000, 0.000000000000000000 ) ) ;
#2185=CARTESIAN_POINT ( 'NONE',  ( 40.90000000000000568, -16.96999999999999886, 21.00000000000000000 ) ) ;
#2192=DIRECTION ( 'NONE',  ( 1.000000000000000000, 0.000000000000000000, 0.000000000000000000 ) ) ;
#2200=EDGE_CURVE ( 'NONE', #37027, #7815, #6437, .T. ) ;
#2207=ORIENTED_EDGE ( 'NONE', *, *, #13982, .F. ) ;
#2222=DIRECTION ( 'NONE',  ( 0.000000000000000000, 0.000000000000000000, 1.000000000000000000 ) ) ;
#2233=CARTESIAN_POINT ( 'NONE',  ( 49.00000000000000000, -0.1999999999911795112, 8.826273045769999343E-12 ) ) ;
#2235=DIRECTION ( 'NONE',  ( -1.000000000000000000, 0.000000000000000000, 0.000000000000000000 ) ) ;
#2245=DIRECTION ( 'NONE',  ( 0.000000000000000000, 0.000000000000000000, -1.000000000000000000 ) ) ;
#2250=AXIS2_PLACEMENT_3D ( 'NONE', #26432, #6601, #27824 ) ;
#2254=ADVANCED_FACE ( 'NONE', ( #7457 ), #66166, .T. ) ;
#2255=ORIENTED_EDGE ( 'NONE', *, *, #31102, .F. ) ;
#2257=VERTEX_POINT ( 'NONE', #23382 ) ;
#2267=ORIENTED_EDGE ( 'NONE', *, *, #16073, .F. ) ;
#2296=AXIS2_PLACEMENT_3D ( 'NONE', #68979, #62266, #46706 ) ;
#2298=DIRECTION ( 'NONE',  ( 0.000000000000000000, 0.000000000000000000, 1.000000000000000000 ) ) ;
#2303=AXIS2_PLACEMENT_3D ( 'NONE', #67615, #35779, #39417 ) ;
#2322=FACE_OUTER_BOUND ( 'NONE', #4311, .T. ) ;
#2323=ORIENTED_EDGE ( 'NONE', *, *, #16232, .T. ) ;
#2332=CYLINDRICAL_SURFACE ( 'NONE', #39309, 24.99999999998794920 ) ;
#2351=AXIS2_PLACEMENT_3D ( 'NONE', #60475, #56222, #34638 ) ;
#2359=CARTESIAN_POINT ( 'NONE',  ( 49.00000000000000000, -14.06939075806900163, -20.80000000000000426 ) ) ;
#2366=EDGE_CURVE ( 'NONE', #29539, #17564, #31902, .T. ) ;
#2378=VECTOR ( 'NONE', #58559, 1000.000000000000000 ) ;
#2384=LINE ( 'NONE', #67449, #66601 ) ;
#2393=CARTESIAN_POINT ( 'NONE',  ( 41.09999999999999432, 20.60000000000000142, -13.86939075806900057 ) ) ;
#2394=VECTOR ( 'NONE', #45651, 1000.000000000000000 ) ;
#2399=ORIENTED_EDGE ( 'NONE', *, *, #11737, .T. ) ;
#2408=EDGE_LOOP ( 'NONE', ( #21125, #20626, #64503, #8577 ) ) ;
#2411=CARTESIAN_POINT ( 'NONE',  ( 22.90000000000000213, 13.66939075806899240, -20.79999999999999361 ) ) ;
#2427=EDGE_CURVE ( 'NONE', #33149, #36598, #20174, .T. ) ;
#2437=ORIENTED_EDGE ( 'NONE', *, *, #36456, .F. ) ;
#2445=DIRECTION ( 'NONE',  ( 0.000000000000000000, 0.000000000000000000, -1.000000000000000000 ) ) ;
#2449=CYLINDRICAL_SURFACE ( 'NONE', #37417, 24.99999999998784972 ) ;
#2453=CLOSED_SHELL ( 'NONE', ( #68580, #27616, #53861, #6340, #58274, #29581 ) ) ;
#2458=DIRECTION ( 'NONE',  ( 0.000000000000000000, 0.000000000000000000, -1.000000000000000000 ) ) ;
#2469=DIRECTION ( 'NONE',  ( 0.000000000000000000, 0.000000000000000000, -1.000000000000000000 ) ) ;
#2472=EDGE_CURVE ( 'NONE', #13751, #1910, #57301, .T. ) ;
#2485=DIRECTION ( 'NONE',  ( -1.000000000000000000, 0.000000000000000000, 0.000000000000000000 ) ) ;
#2514=CIRCLE ( 'NONE', #56728, 2.458500000000000796 ) ;
#2519=DIRECTION ( 'NONE',  ( 0.000000000000000000, 0.000000000000000000, 1.000000000000000000 ) ) ;
#2520=DIRECTION ( 'NONE',  ( 0.000000000000000000, 0.000000000000000000, 1.000000000000000000 ) ) ;
#2521=ORIENTED_EDGE ( 'NONE', *, *, #58516, .F. ) ;
#2524=FILL_AREA_STYLE_COLOUR ( '', #18186 ) ;
#2530=AXIS2_PLACEMENT_3D ( 'NONE', #65291, #55030, #38406 ) ;
#2533=EDGE_CURVE ( 'NONE', #38911, #55382, #27234, .T. ) ;
#2546=CARTESIAN_POINT ( 'NONE',  ( 49.00000000000000000, -14.06939075806900163, -20.80000000000000426 ) ) ;
#2550=CARTESIAN_POINT ( 'NONE',  ( 37.90000000000000568, 20.60000000000000142, 3.232403992503367940E-15 ) ) ;
#2554=DIRECTION ( 'NONE',  ( 0.000000000000000000, -0.7071067811865474617, 0.7071067811865474617 ) ) ;
#2563=VECTOR ( 'NONE', #20046, 1000.000000000000000 ) ;
#2586=CIRCLE ( 'NONE', #24031, 24.99999999998784972 ) ;
#2591=LINE ( 'NONE', #45717, #14129 ) ;
#2601=LINE ( 'NONE', #35463, #12450 ) ;
#2613=DIRECTION ( 'NONE',  ( 0.000000000000000000, 0.000000000000000000, -1.000000000000000000 ) ) ;
#2615=LINE ( 'NONE', #28437, #30086 ) ;
#2620=LINE ( 'NONE', #66626, #26087 ) ;
#2624=VERTEX_POINT ( 'NONE', #10607 ) ;
#2629=ORIENTED_EDGE ( 'NONE', *, *, #67340, .T. ) ;
#2633=CARTESIAN_POINT ( 'NONE',  ( 37.90000000000000568, -14.06939075806902117, -20.80000000000000426 ) ) ;
#2636=ORIENTED_EDGE ( 'NONE', *, *, #43110, .T. ) ;
#2641=FACE_OUTER_BOUND ( 'NONE', #5074, .T. ) ;
#2650=EDGE_CURVE ( 'NONE', #32206, #61792, #13379, .T. ) ;
#2652=LINE ( 'NONE', #62046, #24926 ) ;
#2659=DIRECTION ( 'NONE',  ( 0.000000000000000000, -1.000000000000000000, 0.000000000000000000 ) ) ;
#2664=VECTOR ( 'NONE', #57739, 1000.000000000000000 ) ;
#2666=VECTOR ( 'NONE', #10902, 1000.000000000000000 ) ;
#2667=LINE ( 'NONE', #45444, #2978 ) ;
#2668=ORIENTED_EDGE ( 'NONE', *, *, #56721, .T. ) ;
#2681=CARTESIAN_POINT ( 'NONE',  ( 39.00000000000000000, 6.123233995736766282E-16, -5.000000000000000000 ) ) ;
#2685=DIRECTION ( 'NONE',  ( -1.000000000000000000, 0.000000000000000000, 0.000000000000000000 ) ) ;
#2700=LINE ( 'NONE', #24281, #61516 ) ;
#2704=DIRECTION ( 'NONE',  ( 0.000000000000000000, 0.000000000000000000, -1.000000000000000000 ) ) ;
#2706=LINE ( 'NONE', #29578, #12717 ) ;
#2718=( NAMED_UNIT ( * ) SI_UNIT ( $, .STERADIAN. ) SOLID_ANGLE_UNIT ( ) );
#2721=DIRECTION ( 'NONE',  ( -1.000000000000000000, 0.000000000000000000, 0.000000000000000000 ) ) ;
#2725=ORIENTED_EDGE ( 'NONE', *, *, #42409, .F. ) ;
#2764=VERTEX_POINT ( 'NONE', #22945 ) ;
#2768=EDGE_CURVE ( 'NONE', #44787, #2257, #46665, .T. ) ;
#2783=CARTESIAN_POINT ( 'NONE',  ( 31.89999999999999858, -0.1999999999911430404, -8.864436962241481021E-12 ) ) ;
#2789=FACE_OUTER_BOUND ( 'NONE', #50617, .T. ) ;
#2801=EDGE_CURVE ( 'NONE', #44331, #44196, #39883, .T. ) ;
#2809=LINE ( 'NONE', #17688, #49351 ) ;
#2818=ORIENTED_EDGE ( 'NONE', *, *, #42486, .F. ) ;
#2822=EDGE_CURVE ( 'NONE', #60107, #55424, #18426, .T. ) ;
#2826=MECHANICAL_DESIGN_GEOMETRIC_PRESENTATION_REPRESENTATION('',(#11849),#66006);
#2829=EDGE_LOOP ( 'NONE', ( #50662, #55681 ) ) ;
#2831=CIRCLE ( 'NONE', #42365, 24.99999999998789946 ) ;
#2835=ORIENTED_EDGE ( 'NONE', *, *, #43160, .F. ) ;
#2849=VERTEX_POINT ( 'NONE', #56853 ) ;
#2850=AXIS2_PLACEMENT_3D ( 'NONE', #28738, #29095, #2222 ) ;
#2858=AXIS2_PLACEMENT_3D ( 'NONE', #4019, #31594, #64131 ) ;
#2862=CIRCLE ( 'NONE', #18653, 0.5540281690140901327 ) ;
#2867=ORIENTED_EDGE ( 'NONE', *, *, #57305, .F. ) ;
#2877=PRESENTATION_STYLE_ASSIGNMENT (( #39991 ) ) ;
#2878=ORIENTED_EDGE ( 'NONE', *, *, #63499, .T. ) ;
#2885=DIRECTION ( 'NONE',  ( 0.000000000000000000, 0.000000000000000000, -1.000000000000000000 ) ) ;
#2886=DIRECTION ( 'NONE',  ( -1.000000000000000000, 0.000000000000000000, 0.000000000000000000 ) ) ;
#2896=EDGE_CURVE ( 'NONE', #62756, #29427, #63595, .T. ) ;
#2899=LINE ( 'NONE', #46040, #19373 ) ;
#2901=EDGE_CURVE ( 'NONE', #59143, #62865, #42125, .T. ) ;
#2916=VERTEX_POINT ( 'NONE', #40112 ) ;
#2920=CARTESIAN_POINT ( 'NONE',  ( 13.90000000000000213, -21.00000000000000000, 13.86939075806900057 ) ) ;
#2922=AXIS2_PLACEMENT_3D ( 'NONE', #47814, #26605, #21307 ) ;
#2925=LINE ( 'NONE', #57010, #20793 ) ;
#2943=VERTEX_POINT ( 'NONE', #18917 ) ;
#2954=ORIENTED_EDGE ( 'NONE', *, *, #51097, .F. ) ;
#2966=DIRECTION ( 'NONE',  ( 0.000000000000000000, 0.000000000000000000, -1.000000000000000000 ) ) ;
#2974=ORIENTED_EDGE ( 'NONE', *, *, #15266, .T. ) ;
#2978=VECTOR ( 'NONE', #61353, 1000.000000000000000 ) ;
#3000=ORIENTED_EDGE ( 'NONE', *, *, #40561, .T. ) ;
#3003=DIRECTION ( 'NONE',  ( -1.000000000000000000, 0.000000000000000000, 0.000000000000000000 ) ) ;
#3005=EDGE_LOOP ( 'NONE', ( #6232, #45603 ) ) ;
#3006=DIRECTION ( 'NONE',  ( -1.000000000000000000, 0.000000000000000000, 0.000000000000000000 ) ) ;
#3008=DIRECTION ( 'NONE',  ( -1.000000000000000000, 0.000000000000000000, 0.000000000000000000 ) ) ;
#3014=CIRCLE ( 'NONE', #42536, 24.99999999998784972 ) ;
#3023=ORIENTED_EDGE ( 'NONE', *, *, #12455, .T. ) ;
#3039=CARTESIAN_POINT ( 'NONE',  ( 25.57999999999999829, 0.000000000000000000, 0.000000000000000000 ) ) ;
#3059=CARTESIAN_POINT ( 'NONE',  ( 49.00000000000000000, 20.60000000000000142, -13.86939075806900057 ) ) ;
#3068=CYLINDRICAL_SURFACE ( 'NONE', #45050, 3.500000000000000000 ) ;
#3069=CONICAL_SURFACE ( 'NONE', #56165, 2.458500000000000796, 1.047019301333029784 ) ;
#3078=CARTESIAN_POINT ( 'NONE',  ( 39.90000000000000568, 21.00000000000000000, -16.96999999999999886 ) ) ;
#3079=AXIS2_PLACEMENT_3D ( 'NONE', #18190, #558, #61676 ) ;
#3081=DIRECTION ( 'NONE',  ( -1.000000000000000000, 0.000000000000000000, 0.000000000000000000 ) ) ;
#3098=DIRECTION ( 'NONE',  ( 0.000000000000000000, 0.000000000000000000, -1.000000000000000000 ) ) ;
#3104=ORIENTED_EDGE ( 'NONE', *, *, #124, .T. ) ;
#3110=ORIENTED_EDGE ( 'NONE', *, *, #59580, .F. ) ;
#3113=ORIENTED_EDGE ( 'NONE', *, *, #40487, .F. ) ;
#3118=AXIS2_PLACEMENT_3D ( 'NONE', #69373, #63730, #26588 ) ;
#3140=PLANE ( 'NONE',  #24314 ) ;
#3148=EDGE_LOOP ( 'NONE', ( #533, #30779 ) ) ;
#3151=PLANE ( 'NONE',  #24566 ) ;
#3155=DIRECTION ( 'NONE',  ( -1.000000000000000000, 0.000000000000000000, 0.000000000000000000 ) ) ;
#3158=CYLINDRICAL_SURFACE ( 'NONE', #30849, 0.5000000000000000000 ) ;
#3160=LINE ( 'NONE', #24720, #68186 ) ;
#3166=DIRECTION ( 'NONE',  ( -0.000000000000000000, -1.000000000000000000, 0.000000000000000000 ) ) ;
#3167=ORIENTED_EDGE ( 'NONE', *, *, #5781, .T. ) ;
#3185=EDGE_CURVE ( 'NONE', #51099, #18545, #16283, .T. ) ;
#3193=CARTESIAN_POINT ( 'NONE',  ( 14.89999999999999680, -14.06939075806900163, -20.80000000000000426 ) ) ;
#3195=CARTESIAN_POINT ( 'NONE',  ( 49.00000000000000000, -14.06939075806900163, -20.80000000000000426 ) ) ;
#3204=EDGE_CURVE ( 'NONE', #7460, #20883, #34325, .T. ) ;
#3215=EDGE_LOOP ( 'NONE', ( #12569, #14902, #54564, #45194 ) ) ;
#3218=EDGE_CURVE ( 'NONE', #41932, #56820, #22413, .T. ) ;
#3220=VECTOR ( 'NONE', #47636, 1000.000000000000000 ) ;
#3221=CYLINDRICAL_SURFACE ( 'NONE', #21422, 5.000000000000000000 ) ;
#3248=LINE ( 'NONE', #26219, #24336 ) ;
#3260=EDGE_LOOP ( 'NONE', ( #42424, #45796, #10768, #67926 ) ) ;
#3261=AXIS2_PLACEMENT_3D ( 'NONE', #52173, #62773, #31329 ) ;
#3280=ORIENTED_EDGE ( 'NONE', *, *, #54319, .T. ) ;
#3301=EDGE_CURVE ( 'NONE', #4233, #28489, #11436, .T. ) ;
#3309=ORIENTED_EDGE ( 'NONE', *, *, #2427, .T. ) ;
#3320=VECTOR ( 'NONE', #17628, 1000.000000000000000 ) ;
#3330=CARTESIAN_POINT ( 'NONE',  ( 41.09999999999999432, -0.2000000000000000111, 0.000000000000000000 ) ) ;
#3333=ORIENTED_EDGE ( 'NONE', *, *, #44868, .T. ) ;
#3335=CIRCLE ( 'NONE', #36085, 2.458500000000000796 ) ;
#3372=ORIENTED_EDGE ( 'NONE', *, *, #44899, .T. ) ;
#3385=CARTESIAN_POINT ( 'NONE',  ( 27.00000000000000000, 0.000000000000000000, 0.000000000000000000 ) ) ;
#3386=EDGE_CURVE ( 'NONE', #42535, #43129, #14504, .T. ) ;
#3387=ORIENTED_EDGE ( 'NONE', *, *, #56039, .T. ) ;
#3390=DIRECTION ( 'NONE',  ( -1.000000000000000000, 0.000000000000000000, 0.000000000000000000 ) ) ;
#3396=UNCERTAINTY_MEASURE_WITH_UNIT (LENGTH_MEASURE( 1.000000000000000082E-05 ), #31112, 'distance_accuracy_value', 'NONE');
#3406=ADVANCED_FACE ( 'NONE', ( #50923 ), #41365, .F. ) ;
#3415=EDGE_LOOP ( 'NONE', ( #53166, #25420, #5626, #20052 ) ) ;
#3431=CARTESIAN_POINT ( 'NONE',  ( 39.00000000000000000, 14.08845687959340331, 21.00000000000000000 ) ) ;
#3446=FILL_AREA_STYLE_COLOUR ( '', #8265 ) ;
#3458=ADVANCED_FACE ( 'NONE', ( #35707 ), #61889, .F. ) ;
#3463=EDGE_LOOP ( 'NONE', ( #60874, #36949, #10789, #64791 ) ) ;
#3465=CARTESIAN_POINT ( 'NONE',  ( 41.09999999999999432, -14.06939075806900163, 20.80000000000000426 ) ) ;
#3479=EDGE_LOOP ( 'NONE', ( #24456, #63406, #9131, #37658 ) ) ;
#3481=ORIENTED_EDGE ( 'NONE', *, *, #4609, .T. ) ;
#3485=CYLINDRICAL_SURFACE ( 'NONE', #29912, 2.458500000000000796 ) ;
#3492=CARTESIAN_POINT ( 'NONE',  ( 39.00000000000000000, -16.96999999999999886, -21.00000000000000000 ) ) ;
#3499=DIRECTION ( 'NONE',  ( 0.000000000000000000, 0.000000000000000000, -1.000000000000000000 ) ) ;
#3518=EDGE_CURVE ( 'NONE', #24611, #26279, #6193, .T. ) ;
#3521=VECTOR ( 'NONE', #55241, 1000.000000000000000 ) ;
#3522=LINE ( 'NONE', #9525, #57261 ) ;
#3539=AXIS2_PLACEMENT_3D ( 'NONE', #3985, #58442, #30499 ) ;
#3547=DIRECTION ( 'NONE',  ( 0.000000000000000000, 1.000000000000000000, 0.000000000000000000 ) ) ;
#3549=CARTESIAN_POINT ( 'NONE',  ( 39.90000000000000568, 16.96999999999999886, 21.00000000000000000 ) ) ;
#3551=VERTEX_POINT ( 'NONE', #58354 ) ;
#3564=DIRECTION ( 'NONE',  ( 0.000000000000000000, 0.000000000000000000, 1.000000000000000000 ) ) ;
#3574=AXIS2_PLACEMENT_3D ( 'NONE', #56195, #7741, #2445 ) ;
#3582=CLOSED_SHELL ( 'NONE', ( #40542, #64342, #11733, #10084, #58799, #54196, #14833, #66593, #59238, #46770 ) ) ;
#3585=FACE_OUTER_BOUND ( 'NONE', #30082, .T. ) ;
#3598=CARTESIAN_POINT ( 'NONE',  ( 29.89999999999999858, -0.000000000000000000, -20.80000000000000071 ) ) ;
#3606=LINE ( 'NONE', #14555, #28987 ) ;
#3613=DIRECTION ( 'NONE',  ( -1.000000000000000000, 0.000000000000000000, 0.000000000000000000 ) ) ;
#3614=EDGE_CURVE ( 'NONE', #43972, #62304, #23133, .T. ) ;
#3626=VERTEX_POINT ( 'NONE', #50144 ) ;
#3630=VECTOR ( 'NONE', #21031, 1000.000000000000000 ) ;
#3639=CARTESIAN_POINT ( 'NONE',  ( 41.09999999999999432, 21.00000000000000000, 13.98999642601811999 ) ) ;
#3648=ORIENTED_EDGE ( 'NONE', *, *, #68475, .F. ) ;
#3666=ORIENTED_EDGE ( 'NONE', *, *, #36786, .F. ) ;
#3668=CIRCLE ( 'NONE', #58986, 5.000000000000000000 ) ;
#3682=CARTESIAN_POINT ( 'NONE',  ( 11.90000000000000036, -0.2000000000089119934, 8.909539772616881237E-12 ) ) ;
#3683=ORIENTED_EDGE ( 'NONE', *, *, #63341, .T. ) ;
#3684=CARTESIAN_POINT ( 'NONE',  ( 35.89999999999999858, 3.010794155703768650E-16, -2.458500000000000796 ) ) ;
#3694=DIRECTION ( 'NONE',  ( 1.000000000000000000, -0.000000000000000000, -0.000000000000000000 ) ) ;
#3698=EDGE_CURVE ( 'NONE', #1302, #63520, #69438, .T. ) ;
#3703=ADVANCED_FACE ( 'NONE', ( #22254 ), #335, .F. ) ;
#3707=ORIENTED_EDGE ( 'NONE', *, *, #10214, .F. ) ;
#3716=VECTOR ( 'NONE', #40186, 1000.000000000000000 ) ;
#3717=ORIENTED_EDGE ( 'NONE', *, *, #64847, .T. ) ;
#3731=FACE_OUTER_BOUND ( 'NONE', #5062, .T. ) ;
#3738=MECHANICAL_DESIGN_GEOMETRIC_PRESENTATION_REPRESENTATION('',(#22908),#57942);
#3740=ADVANCED_FACE ( 'NONE', ( #1368 ), #39193, .T. ) ;
#3745=CARTESIAN_POINT ( 'NONE',  ( 41.09999999999999432, 13.66939075806899950, 20.80000000000000426 ) ) ;
#3747=DIRECTION ( 'NONE',  ( 0.000000000000000000, 0.000000000000000000, -1.000000000000000000 ) ) ;
#3748=DIRECTION ( 'NONE',  ( 1.000000000000000000, -0.000000000000000000, 0.000000000000000000 ) ) ;
#3756=FACE_OUTER_BOUND ( 'NONE', #23093, .T. ) ;
#3759=DIRECTION ( 'NONE',  ( 0.000000000000000000, 0.000000000000000000, -1.000000000000000000 ) ) ;
#3765=LINE ( 'NONE', #46191, #28524 ) ;
#3769=EDGE_LOOP ( 'NONE', ( #26954, #2399, #45318, #68730 ) ) ;
#3771=DIRECTION ( 'NONE',  ( 1.000000000000000000, -0.000000000000000000, 0.000000000000000000 ) ) ;
#3772=CARTESIAN_POINT ( 'NONE',  ( 20.90000000000000213, -21.00000000000000000, 13.86939075806900057 ) ) ;
#3774=CIRCLE ( 'NONE', #59104, 24.99999999998784972 ) ;
#3797=LINE ( 'NONE', #9374, #8204 ) ;
#3799=CARTESIAN_POINT ( 'NONE',  ( 9.900000000000000355, -21.00000000000000000, -18.00000000000000355 ) ) ;
#3815=ADVANCED_FACE ( 'NONE', ( #39525 ), #56493, .F. ) ;
#3817=CARTESIAN_POINT ( 'NONE',  ( 39.90000000000000568, 20.60000000000000142, 3.447897592003593022E-15 ) ) ;
#3833=LINE ( 'NONE', #3492, #32777 ) ;
#3839=EDGE_CURVE ( 'NONE', #16920, #43746, #23614, .T. ) ;
#3843=CARTESIAN_POINT ( 'NONE',  ( 39.00000000000000000, 3.010794155703768650E-16, -2.458500000000000796 ) ) ;
#3861=DIRECTION ( 'NONE',  ( 1.000000000000000000, -0.000000000000000000, 0.000000000000000000 ) ) ;
#3873=PLANE ( 'NONE',  #15546 ) ;
#3875=VECTOR ( 'NONE', #27020, 1000.000000000000000 ) ;
#3885=CARTESIAN_POINT ( 'NONE',  ( 41.09999999999999432, -0.2000000000000000111, 0.000000000000000000 ) ) ;
#3886=DIRECTION ( 'NONE',  ( -1.000000000000000000, 0.000000000000000000, 0.000000000000000000 ) ) ;
#3889=EDGE_CURVE ( 'NONE', #10676, #61094, #57544, .T. ) ;
#3892=EDGE_LOOP ( 'NONE', ( #48021, #5906, #66933, #45636 ) ) ;
#3895=DIRECTION ( 'NONE',  ( 0.000000000000000000, 0.000000000000000000, 1.000000000000000000 ) ) ;
#3898=CARTESIAN_POINT ( 'NONE',  ( 49.00000000000000000, -21.00000000000000000, 13.86939075806900057 ) ) ;
#3909=CYLINDRICAL_SURFACE ( 'NONE', #67668, 24.99999999998784972 ) ;
#3915=DIRECTION ( 'NONE',  ( 1.000000000000000000, -0.000000000000000000, 0.000000000000000000 ) ) ;
#3919=EDGE_LOOP ( 'NONE', ( #66401, #34503, #7870, #64097, #35086, #969, #106, #32997 ) ) ;
#3930=DIRECTION ( 'NONE',  ( 1.000000000000000000, -0.000000000000000000, 0.000000000000000000 ) ) ;
#3949=CARTESIAN_POINT ( 'NONE',  ( 25.90000000000000213, 6.784888238205741802E-17, 0.5540281690140901327 ) ) ;
#3950=EDGE_CURVE ( 'NONE', #20196, #54988, #40155, .T. ) ;
#3954=ORIENTED_EDGE ( 'NONE', *, *, #38715, .T. ) ;
#3958=FACE_OUTER_BOUND ( 'NONE', #16004, .T. ) ;
#3963=ORIENTED_EDGE ( 'NONE', *, *, #60940, .T. ) ;
#3972=ORIENTED_EDGE ( 'NONE', *, *, #40481, .T. ) ;
#3985=CARTESIAN_POINT ( 'NONE',  ( 27.00000000000000000, 0.000000000000000000, 0.000000000000000000 ) ) ;
#3993=CARTESIAN_POINT ( 'NONE',  ( 37.90000000000000568, 3.010794155703768650E-16, -2.458500000000000796 ) ) ;
#3994=CARTESIAN_POINT ( 'NONE',  ( 35.89999999999999858, -14.06939075806900874, 20.80000000000001137 ) ) ;
#3996=AXIS2_PLACEMENT_3D ( 'NONE', #34584, #29629, #35993 ) ;
#4009=DIRECTION ( 'NONE',  ( 0.000000000000000000, 1.000000000000000000, -0.000000000000000000 ) ) ;
#4015=DIRECTION ( 'NONE',  ( 0.000000000000000000, 0.000000000000000000, -1.000000000000000000 ) ) ;
#4016=ORIENTED_EDGE ( 'NONE', *, *, #59672, .F. ) ;
#4019=CARTESIAN_POINT ( 'NONE',  ( 10.00000000000000000, 18.00000000000000355, 21.00000000000000000 ) ) ;
#4023=LINE ( 'NONE', #68015, #62107 ) ;
#4025=EDGE_CURVE ( 'NONE', #27370, #12812, #62728, .T. ) ;
#4039=CYLINDRICAL_SURFACE ( 'NONE', #54931, 5.000000000000000000 ) ;
#4040=FACE_OUTER_BOUND ( 'NONE', #28519, .T. ) ;
#4041=ORIENTED_EDGE ( 'NONE', *, *, #64230, .T. ) ;
#4043=AXIS2_PLACEMENT_3D ( 'NONE', #24540, #9322, #41499 ) ;
#4045=AXIS2_PLACEMENT_3D ( 'NONE', #813, #64809, #456 ) ;
#4055=VECTOR ( 'NONE', #37453, 1000.000000000000000 ) ;
#4068=FACE_OUTER_BOUND ( 'NONE', #34195, .T. ) ;
#4080=DIRECTION ( 'NONE',  ( 0.000000000000000000, -1.000000000000000000, 0.000000000000000000 ) ) ;
#4090=AXIS2_PLACEMENT_3D ( 'NONE', #10754, #58153, #48246 ) ;
#4098=VECTOR ( 'NONE', #8426, 1000.000000000000000 ) ;
#4112=UNCERTAINTY_MEASURE_WITH_UNIT (LENGTH_MEASURE( 1.000000000000000082E-05 ), #36386, 'distance_accuracy_value', 'NONE');
#4116=CARTESIAN_POINT ( 'NONE',  ( 39.00000000000000000, -16.96999999999999886, 21.00000000000000000 ) ) ;
#4120=CARTESIAN_POINT ( 'NONE',  ( 49.00000000000000000, -0.1999999999911795112, 8.826273045769999343E-12 ) ) ;
#4124=CARTESIAN_POINT ( 'NONE',  ( 9.899999999999998579, 20.60000000000000142, -13.86939075806900057 ) ) ;
#4126=SURFACE_SIDE_STYLE ('',( #68468 ) ) ;
#4136=VECTOR ( 'NONE', #59430, 1000.000000000000000 ) ;
#4137=CIRCLE ( 'NONE', #13144, 24.99999999998789946 ) ;
#4155=CARTESIAN_POINT ( 'NONE',  ( 49.00000000000000000, -0.2000000000089119934, 8.909539772616881237E-12 ) ) ;
#4163=ORIENTED_EDGE ( 'NONE', *, *, #33390, .T. ) ;
#4168=ADVANCED_FACE ( 'NONE', ( #54345, #65308 ), #33464, .T. ) ;
#4186=VERTEX_POINT ( 'NONE', #32436 ) ;
#4210=VERTEX_POINT ( 'NONE', #6921 ) ;
#4214=EDGE_CURVE ( 'NONE', #30799, #2028, #7266, .T. ) ;
#4224=CARTESIAN_POINT ( 'NONE',  ( 46.39999999999999858, 21.00000000000000000, 1.250000000000000000 ) ) ;
#4231=DIRECTION ( 'NONE',  ( 0.000000000000000000, 1.000000000000000000, 0.000000000000000000 ) ) ;
#4233=VERTEX_POINT ( 'NONE', #50421 ) ;
#4235=ADVANCED_FACE ( 'NONE', ( #18227 ), #23890, .F. ) ;
#4236=MECHANICAL_DESIGN_GEOMETRIC_PRESENTATION_REPRESENTATION('',(#64106),#6496);
#4239=ORIENTED_EDGE ( 'NONE', *, *, #55745, .F. ) ;
#4243=( NAMED_UNIT ( * ) PLANE_ANGLE_UNIT ( ) SI_UNIT ( $, .RADIAN. ) );
#4244=EDGE_CURVE ( 'NONE', #6097, #48107, #2667, .T. ) ;
#4248=CARTESIAN_POINT ( 'NONE',  ( 25.57999999999999829, 0.000000000000000000, 2.458500000000000796 ) ) ;
#4249=CARTESIAN_POINT ( 'NONE',  ( 16.89999999999999858, 13.66939075806899240, -20.79999999999999361 ) ) ;
#4250=VECTOR ( 'NONE', #58114, 1000.000000000000000 ) ;
#4261=LINE ( 'NONE', #3549, #34342 ) ;
#4269=CIRCLE ( 'NONE', #30247, 25.39999999999999858 ) ;
#4282=ADVANCED_FACE ( 'NONE', ( #28831 ), #18942, .F. ) ;
#4311=EDGE_LOOP ( 'NONE', ( #42824, #25465, #46743, #26360 ) ) ;
#4312=CARTESIAN_POINT ( 'NONE',  ( 39.90000000000000568, 21.00000000000000000, -16.96999999999999886 ) ) ;
#4314=LINE ( 'NONE', #40716, #30668 ) ;
#4316=LINE ( 'NONE', #25870, #54996 ) ;
#4332=VERTEX_POINT ( 'NONE', #10007 ) ;
#4347=EDGE_CURVE ( 'NONE', #60085, #27370, #9655, .T. ) ;
#4366=EDGE_LOOP ( 'NONE', ( #188, #52403, #25502, #1882 ) ) ;
#4374=CIRCLE ( 'NONE', #37121, 24.99999999998794920 ) ;
#4398=LINE ( 'NONE', #25611, #27812 ) ;
#4412=FILL_AREA_STYLE ('',( #20306 ) ) ;
#4431=( NAMED_UNIT ( * ) SI_UNIT ( $, .STERADIAN. ) SOLID_ANGLE_UNIT ( ) );
#4443=CARTESIAN_POINT ( 'NONE',  ( 40.90000000000000568, 14.08845687959340331, -21.00000000000000000 ) ) ;
#4446=VERTEX_POINT ( 'NONE', #39290 ) ;
#4449=CARTESIAN_POINT ( 'NONE',  ( 41.09999999999999432, -21.00000000000000000, 13.86939075806900057 ) ) ;
#4463=AXIS2_PLACEMENT_3D ( 'NONE', #32410, #18206, #67356 ) ;
#4465=EDGE_CURVE ( 'NONE', #36902, #64226, #8566, .T. ) ;
#4489=CIRCLE ( 'NONE', #36068, 24.99999999998784972 ) ;
#4507=EDGE_CURVE ( 'NONE', #66814, #39291, #11714, .T. ) ;
#4520=VERTEX_POINT ( 'NONE', #34312 ) ;
#4531=VERTEX_POINT ( 'NONE', #55899 ) ;
#4537=VECTOR ( 'NONE', #13186, 1000.000000000000114 ) ;
#4539=LINE ( 'NONE', #20441, #55689 ) ;
#4541=CARTESIAN_POINT ( 'NONE',  ( 39.90000000000000568, -0.1999999999911430404, -8.864436962241481021E-12 ) ) ;
#4548=EDGE_CURVE ( 'NONE', #47484, #62940, #54879, .T. ) ;
#4569=CARTESIAN_POINT ( 'NONE',  ( 46.39999999999999858, 21.00000000000000000, -1.250000000000000000 ) ) ;
#4590=FACE_BOUND ( 'NONE', #12126, .T. ) ;
#4593=CYLINDRICAL_SURFACE ( 'NONE', #51068, 5.000000000000000000 ) ;
#4605=VECTOR ( 'NONE', #12900, 1000.000000000000000 ) ;
#4609=EDGE_CURVE ( 'NONE', #22670, #4860, #7796, .T. ) ;
#4610=ORIENTED_EDGE ( 'NONE', *, *, #61252, .F. ) ;
#4613=VERTEX_POINT ( 'NONE', #61531 ) ;
#4622=DIRECTION ( 'NONE',  ( 0.000000000000000000, 0.000000000000000000, -1.000000000000000000 ) ) ;
#4623=EDGE_LOOP ( 'NONE', ( #42884, #29273, #44952, #1420 ) ) ;
#4653=FACE_OUTER_BOUND ( 'NONE', #56511, .T. ) ;
#4655=DIRECTION ( 'NONE',  ( 1.000000000000000000, -0.000000000000000000, 0.000000000000000000 ) ) ;
#4661=LINE ( 'NONE', #47432, #27893 ) ;
#4663=DIRECTION ( 'NONE',  ( 0.000000000000000000, 0.000000000000000000, -1.000000000000000000 ) ) ;
#4664=AXIS2_PLACEMENT_3D ( 'NONE', #46465, #14648, #68042 ) ;
#4670=DIRECTION ( 'NONE',  ( 0.000000000000000000, 0.000000000000000000, 1.000000000000000000 ) ) ;
#4682=VERTEX_POINT ( 'NONE', #29367 ) ;
#4686=PLANE ( 'NONE',  #30633 ) ;
#4688=ADVANCED_FACE ( 'NONE', ( #46336 ), #24779, .T. ) ;
#4695=DIRECTION ( 'NONE',  ( 0.000000000000000000, 0.000000000000000000, -1.000000000000000000 ) ) ;
#4698=VERTEX_POINT ( 'NONE', #40338 ) ;
#4700=EDGE_LOOP ( 'NONE', ( #17136, #9793 ) ) ;
#4712=DIRECTION ( 'NONE',  ( -1.000000000000000000, 0.000000000000000000, 0.000000000000000000 ) ) ;
#4713=ORIENTED_EDGE ( 'NONE', *, *, #14794, .T. ) ;
#4717=ORIENTED_EDGE ( 'NONE', *, *, #5310, .F. ) ;
#4723=DIRECTION ( 'NONE',  ( 1.000000000000000000, -0.000000000000000000, 0.000000000000000000 ) ) ;
#4732=EDGE_CURVE ( 'NONE', #36943, #29826, #5328, .T. ) ;
#4733=CARTESIAN_POINT ( 'NONE',  ( 41.09999999999999432, -21.00000000000000000, -13.86939075806900057 ) ) ;
#4737=EDGE_LOOP ( 'NONE', ( #2267, #64202, #58598, #45820 ) ) ;
#4739=ORIENTED_EDGE ( 'NONE', *, *, #44869, .T. ) ;
#4749=CIRCLE ( 'NONE', #33006, 24.99999999998789946 ) ;
#4755=( NAMED_UNIT ( * ) SI_UNIT ( $, .STERADIAN. ) SOLID_ANGLE_UNIT ( ) );
#4756=EDGE_CURVE ( 'NONE', #21542, #41212, #66217, .T. ) ;
#4787=DIRECTION ( 'NONE',  ( 0.000000000000000000, 1.000000000000000000, 0.000000000000000000 ) ) ;
#4796=VECTOR ( 'NONE', #11796, 1000.000000000000000 ) ;
#4800=UNCERTAINTY_MEASURE_WITH_UNIT (LENGTH_MEASURE( 1.000000000000000082E-05 ), #66052, 'distance_accuracy_value', 'NONE');
#4804=FACE_OUTER_BOUND ( 'NONE', #58913, .T. ) ;
#4819=DIRECTION ( 'NONE',  ( 0.000000000000000000, 0.000000000000000000, -1.000000000000000000 ) ) ;
#4827=EDGE_CURVE ( 'NONE', #30457, #25912, #36797, .T. ) ;
#4837=DIRECTION ( 'NONE',  ( -0.000000000000000000, -1.000000000000000000, 0.000000000000000000 ) ) ;
#4845=FACE_BOUND ( 'NONE', #37652, .T. ) ;
#4860=VERTEX_POINT ( 'NONE', #48791 ) ;
#4872=VERTEX_POINT ( 'NONE', #27561 ) ;
#4873=LINE ( 'NONE', #30696, #65130 ) ;
#4878=ORIENTED_EDGE ( 'NONE', *, *, #66902, .F. ) ;
#4887=LINE ( 'NONE', #58632, #36254 ) ;
#4913=MECHANICAL_DESIGN_GEOMETRIC_PRESENTATION_REPRESENTATION('',(#11648),#35370);
#4916=VERTEX_POINT ( 'NONE', #43826 ) ;
#4944=EDGE_CURVE ( 'NONE', #36995, #4210, #2862, .T. ) ;
#4950=LINE ( 'NONE', #26515, #12493 ) ;
#4956=AXIS2_PLACEMENT_3D ( 'NONE', #23195, #23543, #12571 ) ;
#4969=AXIS2_PLACEMENT_3D ( 'NONE', #51304, #34326, #61201 ) ;
#4980=EDGE_CURVE ( 'NONE', #5469, #51099, #11291, .T. ) ;
#4992=STYLED_ITEM ( 'NONE', ( #39934 ), #21524 ) ;
#5003=CIRCLE ( 'NONE', #46726, 3.500000000000000000 ) ;
#5006=CARTESIAN_POINT ( 'NONE',  ( 35.89999999999999858, 20.60000000000000142, 13.86939075806899702 ) ) ;
#5025=ADVANCED_FACE ( 'NONE', ( #57213 ), #30344, .T. ) ;
#5035=CARTESIAN_POINT ( 'NONE',  ( 33.89999999999999858, 20.60000000000000142, -13.86939075806900057 ) ) ;
#5057=STYLED_ITEM ( 'NONE', ( #55543 ), #66857 ) ;
#5062=EDGE_LOOP ( 'NONE', ( #44246, #6596, #41817, #15793 ) ) ;
#5072=EDGE_CURVE ( 'NONE', #11985, #50419, #13012, .T. ) ;
#5074=EDGE_LOOP ( 'NONE', ( #22341, #17229, #48029, #30149 ) ) ;
#5076=ORIENTED_EDGE ( 'NONE', *, *, #31945, .T. ) ;
#5081=CARTESIAN_POINT ( 'NONE',  ( 15.89999999999999680, -21.00000000000001421, -13.86939075806900945 ) ) ;
#5082=ADVANCED_FACE ( 'NONE', ( #8057 ), #62868, .T. ) ;
#5123=LINE ( 'NONE', #38343, #40246 ) ;
#5126=STYLED_ITEM ( 'NONE', ( #67428 ), #43268 ) ;
#5127=DIRECTION ( 'NONE',  ( 1.000000000000000000, -0.000000000000000000, 0.000000000000000000 ) ) ;
#5137=EDGE_CURVE ( 'NONE', #37491, #51717, #58965, .T. ) ;
#5139=VERTEX_POINT ( 'NONE', #52980 ) ;
#5150=EDGE_LOOP ( 'NONE', ( #34977, #10089, #66327, #54719 ) ) ;
#5151=EDGE_CURVE ( 'NONE', #21321, #17475, #31756, .T. ) ;
#5152=CARTESIAN_POINT ( 'NONE',  ( 38.90000000000000568, 0.000000000000000000, 3.232403992503367940E-15 ) ) ;
#5160=EDGE_CURVE ( 'NONE', #12117, #31270, #10175, .T. ) ;
#5172=DIRECTION ( 'NONE',  ( 1.000000000000000000, -0.000000000000000000, 0.000000000000000000 ) ) ;
#5181=CARTESIAN_POINT ( 'NONE',  ( 14.90000000000000036, 0.000000000000000000, 6.464807985006735683E-16 ) ) ;
#5198=AXIS2_PLACEMENT_3D ( 'NONE', #33783, #27797, #16839 ) ;
#5207=DIRECTION ( 'NONE',  ( -1.000000000000000000, 0.000000000000000000, 0.000000000000000000 ) ) ;
#5221=EDGE_CURVE ( 'NONE', #65046, #19943, #37404, .T. ) ;
#5226=CARTESIAN_POINT ( 'NONE',  ( 0.000000000000000000, -17.79289321881345032, -20.50000000000000000 ) ) ;
#5234=CARTESIAN_POINT ( 'NONE',  ( 41.09999999999999432, -14.06939075806900163, 20.80000000000000426 ) ) ;
#5245=AXIS2_PLACEMENT_3D ( 'NONE', #59534, #846, #69797 ) ;
#5248=AXIS2_PLACEMENT_3D ( 'NONE', #61976, #60586, #28401 ) ;
#5264=LINE ( 'NONE', #36735, #2666 ) ;
#5269=DIRECTION ( 'NONE',  ( 0.000000000000000000, 0.000000000000000000, -1.000000000000000000 ) ) ;
#5271=CARTESIAN_POINT ( 'NONE',  ( 26.90000000000000213, 13.66939075806899240, -20.79999999999999361 ) ) ;
#5273=LINE ( 'NONE', #16910, #58405 ) ;
#5274=CARTESIAN_POINT ( 'NONE',  ( 40.90000000000000568, 16.96999999999999886, 21.00000000000000000 ) ) ;
#5280=LINE ( 'NONE', #6302, #1940 ) ;
#5282=DIRECTION ( 'NONE',  ( 0.000000000000000000, 0.000000000000000000, -1.000000000000000000 ) ) ;
#5298=VECTOR ( 'NONE', #44203, 1000.000000000000000 ) ;
#5300=EDGE_CURVE ( 'NONE', #56820, #23370, #45766, .T. ) ;
#5302=COLOUR_RGB ( '', 0.09019608, 0.27058824, 0.51372549) ;
#5303=EDGE_CURVE ( 'NONE', #15679, #13897, #33478, .T. ) ;
#5310=EDGE_CURVE ( 'NONE', #24647, #14509, #49734, .T. ) ;
#5328=LINE ( 'NONE', #41731, #25439 ) ;
#5334=CIRCLE ( 'NONE', #16463, 24.99999999998784972 ) ;
#5345=CARTESIAN_POINT ( 'NONE',  ( 14.89999999999999680, -21.00000000000000000, 13.86939075806900057 ) ) ;
#5346=EDGE_LOOP ( 'NONE', ( #20860, #29043, #29, #6725 ) ) ;
#5349=FACE_OUTER_BOUND ( 'NONE', #11418, .T. ) ;
#5353=ORIENTED_EDGE ( 'NONE', *, *, #40160, .T. ) ;
#5373=DIRECTION ( 'NONE',  ( -1.000000000000000000, 0.000000000000000000, 0.000000000000000000 ) ) ;
#5375=CARTESIAN_POINT ( 'NONE',  ( 47.00000000000000000, 0.7500000000000000000, 4.943429983321300014 ) ) ;
#5391=CARTESIAN_POINT ( 'NONE',  ( 26.90000000000000213, 0.000000000000000000, 1.939442395502021001E-15 ) ) ;
#5422=CARTESIAN_POINT ( 'NONE',  ( 18.89999999999999858, -14.06939075806900163, -20.80000000000000426 ) ) ;
#5429=DIRECTION ( 'NONE',  ( 0.000000000000000000, 0.000000000000000000, -1.000000000000000000 ) ) ;
#5439=EDGE_CURVE ( 'NONE', #19639, #21838, #43385, .T. ) ;
#5443=ADVANCED_FACE ( 'NONE', ( #51121 ), #19295, .T. ) ;
#5447=DIRECTION ( 'NONE',  ( -1.000000000000000000, 0.000000000000000000, 0.000000000000000000 ) ) ;
#5459=ADVANCED_FACE ( 'NONE', ( #67737 ), #39799, .T. ) ;
#5461=CARTESIAN_POINT ( 'NONE',  ( 10.00000000000000000, 21.00000000000000000, -18.00000000000000355 ) ) ;
#5464=DIRECTION ( 'NONE',  ( 0.000000000000000000, 0.000000000000000000, -1.000000000000000000 ) ) ;
#5466=VERTEX_POINT ( 'NONE', #56773 ) ;
#5469=VERTEX_POINT ( 'NONE', #45112 ) ;
#5471=DIRECTION ( 'NONE',  ( 0.000000000000000000, 1.000000000000000000, -0.000000000000000000 ) ) ;
#5480=EDGE_CURVE ( 'NONE', #35475, #34278, #50766, .T. ) ;
#5488=VERTEX_POINT ( 'NONE', #1988 ) ;
#5490=EDGE_CURVE ( 'NONE', #67015, #21542, #62071, .T. ) ;
#5504=UNCERTAINTY_MEASURE_WITH_UNIT (LENGTH_MEASURE( 1.000000000000000082E-05 ), #41262, 'distance_accuracy_value', 'NONE');
#5515=CARTESIAN_POINT ( 'NONE',  ( 9.900000000000000355, -18.00000000000000355, 21.00000000000000000 ) ) ;
#5527=LINE ( 'NONE', #54659, #12428 ) ;
#5540=DIRECTION ( 'NONE',  ( 0.000000000000000000, 0.000000000000000000, -1.000000000000000000 ) ) ;
#5554=CARTESIAN_POINT ( 'NONE',  ( 24.90000000000000213, 13.66939075806899240, -20.79999999999999361 ) ) ;
#5571=VECTOR ( 'NONE', #30815, 1000.000000000000114 ) ;
#5574=ORIENTED_EDGE ( 'NONE', *, *, #28356, .F. ) ;
#5579=LINE ( 'NONE', #32096, #19763 ) ;
#5583=DIRECTION ( 'NONE',  ( 0.000000000000000000, 0.000000000000000000, 1.000000000000000000 ) ) ;
#5593=CIRCLE ( 'NONE', #45089, 5.250000000000000000 ) ;
#5605=CARTESIAN_POINT ( 'NONE',  ( 46.39999999999999858, 33.00000000000000000, 2.250000000000000444 ) ) ;
#5616=ORIENTED_EDGE ( 'NONE', *, *, #2822, .T. ) ;
#5626=ORIENTED_EDGE ( 'NONE', *, *, #47324, .T. ) ;
#5629=ADVANCED_FACE ( 'NONE', ( #35917 ), #57825, .T. ) ;
#5641=VERTEX_POINT ( 'NONE', #63493 ) ;
#5652=AXIS2_PLACEMENT_3D ( 'NONE', #57551, #15130, #52616 ) ;
#5673=ORIENTED_EDGE ( 'NONE', *, *, #43160, .T. ) ;
#5675=VECTOR ( 'NONE', #17075, 1000.000000000000000 ) ;
#5678=DIRECTION ( 'NONE',  ( -1.000000000000000000, 0.000000000000000000, 0.000000000000000000 ) ) ;
#5683=CARTESIAN_POINT ( 'NONE',  ( 34.89999999999999858, -14.06939075806900874, 20.80000000000001137 ) ) ;
#5691=CARTESIAN_POINT ( 'NONE',  ( 49.00000000000000000, 13.66939075806899950, 20.80000000000000426 ) ) ;
#5694=PLANE ( 'NONE',  #31693 ) ;
#5698=EDGE_CURVE ( 'NONE', #33150, #36374, #10210, .T. ) ;
#5711=CARTESIAN_POINT ( 'NONE',  ( 38.90000000000000568, 0.000000000000000000, 2.458500000000000796 ) ) ;
#5727=DIRECTION ( 'NONE',  ( 0.000000000000000000, 1.000000000000000000, 0.000000000000000000 ) ) ;
#5728=VECTOR ( 'NONE', #2886, 1000.000000000000000 ) ;
#5729=DIRECTION ( 'NONE',  ( 0.000000000000000000, 0.000000000000000000, -1.000000000000000000 ) ) ;
#5744=LINE ( 'NONE', #12063, #13049 ) ;
#5759=ORIENTED_EDGE ( 'NONE', *, *, #12475, .F. ) ;
#5764=ORIENTED_EDGE ( 'NONE', *, *, #47528, .T. ) ;
#5769=PLANE ( 'NONE',  #60499 ) ;
#5781=EDGE_CURVE ( 'NONE', #53834, #16791, #1225, .T. ) ;
#5806=CARTESIAN_POINT ( 'NONE',  ( 39.00000000000000000, 16.96999999999999886, 21.00000000000000000 ) ) ;
#5820=DIRECTION ( 'NONE',  ( -1.000000000000000000, 0.000000000000000000, 0.000000000000000000 ) ) ;
#5836=ORIENTED_EDGE ( 'NONE', *, *, #40723, .F. ) ;
#5842=ORIENTED_EDGE ( 'NONE', *, *, #42893, .F. ) ;
#5847=CARTESIAN_POINT ( 'NONE',  ( 40.90000000000000568, 16.96999999999999886, -21.00000000000000000 ) ) ;
#5853=CLOSED_SHELL ( 'NONE', ( #50046, #21725, #54852, #14534, #66643, #13406, #47801, #14301, #32297, #63488 ) ) ;
#5858=EDGE_CURVE ( 'NONE', #23370, #57901, #2601, .T. ) ;
#5859=PLANE ( 'NONE',  #50106 ) ;
#5865=CARTESIAN_POINT ( 'NONE',  ( 9.900000000000000355, 21.00000000000000000, -18.00000000000000355 ) ) ;
#5873=PLANE ( 'NONE',  #29045 ) ;
#5877=VECTOR ( 'NONE', #1236, 1000.000000000000000 ) ;
#5878=ORIENTED_EDGE ( 'NONE', *, *, #65910, .F. ) ;
#5883=ORIENTED_EDGE ( 'NONE', *, *, #26537, .T. ) ;
#5888=DIRECTION ( 'NONE',  ( 1.000000000000000000, -0.000000000000000000, 0.000000000000000000 ) ) ;
#5896=EDGE_LOOP ( 'NONE', ( #63825, #8103, #12593, #21492 ) ) ;
#5899=ORIENTED_EDGE ( 'NONE', *, *, #27887, .T. ) ;
#5900=VECTOR ( 'NONE', #6238, 1000.000000000000114 ) ;
#5906=ORIENTED_EDGE ( 'NONE', *, *, #10480, .T. ) ;
#5914=CARTESIAN_POINT ( 'NONE',  ( 26.90000000000000213, -0.2000000000089119934, -8.913009219568841313E-12 ) ) ;
#5918=ORIENTED_EDGE ( 'NONE', *, *, #68534, .T. ) ;
#5925=DIRECTION ( 'NONE',  ( 0.000000000000000000, 0.000000000000000000, 1.000000000000000000 ) ) ;
#5926=CARTESIAN_POINT ( 'NONE',  ( 40.90000000000000568, -21.00000000000000355, 14.57806571531352269 ) ) ;
#5930=EDGE_CURVE ( 'NONE', #60486, #67015, #45378, .T. ) ;
#5931=VERTEX_POINT ( 'NONE', #1912 ) ;
#5940=EDGE_LOOP ( 'NONE', ( #37900, #27612, #12846, #8353 ) ) ;
#5948=ADVANCED_FACE ( 'NONE', ( #8599 ), #23477, .T. ) ;
#5959=DIRECTION ( 'NONE',  ( 0.000000000000000000, 1.000000000000000000, 0.000000000000000000 ) ) ;
#5962=AXIS2_PLACEMENT_3D ( 'NONE', #40742, #68678, #24834 ) ;
#5969=CARTESIAN_POINT ( 'NONE',  ( 12.90000000000000213, -14.06939075806900874, 20.80000000000001137 ) ) ;
#5974=AXIS2_PLACEMENT_3D ( 'NONE', #52371, #10621, #37852 ) ;
#5985=ORIENTED_EDGE ( 'NONE', *, *, #10398, .F. ) ;
#5996=EDGE_CURVE ( 'NONE', #35542, #68516, #28274, .T. ) ;
#5998=LINE ( 'NONE', #54786, #37778 ) ;
#6023=DIRECTION ( 'NONE',  ( 0.000000000000000000, 1.000000000000000000, -0.000000000000000000 ) ) ;
#6024=( GEOMETRIC_REPRESENTATION_CONTEXT ( 3 ) GLOBAL_UNCERTAINTY_ASSIGNED_CONTEXT ( ( #42967 ) ) GLOBAL_UNIT_ASSIGNED_CONTEXT ( ( #31784, #53352, #64303 ) ) REPRESENTATION_CONTEXT ( 'NONE', 'WORKASPACE' ) );
#6028=CARTESIAN_POINT ( 'NONE',  ( 28.90000000000000213, -0.2000000000089119934, 8.909539772616881237E-12 ) ) ;
#6033=DIRECTION ( 'NONE',  ( 0.000000000000000000, -0.1500000000000000777, 0.9886859966642594921 ) ) ;
#6035=DIRECTION ( 'NONE',  ( -1.000000000000000000, 0.000000000000000000, 0.000000000000000000 ) ) ;
#6046=CARTESIAN_POINT ( 'NONE',  ( 41.09999999999999432, 13.66939075806899950, -20.80000000000000426 ) ) ;
#6047=EDGE_CURVE ( 'NONE', #4682, #7560, #51750, .T. ) ;
#6049=CARTESIAN_POINT ( 'NONE',  ( 41.09999999999999432, -14.06939075806900163, 20.80000000000000426 ) ) ;
#6056=DIRECTION ( 'NONE',  ( 1.000000000000000000, -0.000000000000000000, 0.000000000000000000 ) ) ;
#6091=VERTEX_POINT ( 'NONE', #54547 ) ;
#6092=ORIENTED_EDGE ( 'NONE', *, *, #58593, .T. ) ;
#6094=EDGE_CURVE ( 'NONE', #42963, #12117, #43230, .T. ) ;
#6097=VERTEX_POINT ( 'NONE', #7031 ) ;
#6108=AXIS2_PLACEMENT_3D ( 'NONE', #21530, #38821, #22574 ) ;
#6111=CARTESIAN_POINT ( 'NONE',  ( 19.90000000000000213, 13.66939075806899240, 20.79999999999999361 ) ) ;
#6112=ORIENTED_EDGE ( 'NONE', *, *, #8257, .T. ) ;
#6115=CARTESIAN_POINT ( 'NONE',  ( 55.00000000000000000, -16.96999999999999886, -21.00000000000000000 ) ) ;
#6122=EDGE_CURVE ( 'NONE', #61720, #66978, #38440, .T. ) ;
#6129=FACE_OUTER_BOUND ( 'NONE', #5940, .T. ) ;
#6136=ORIENTED_EDGE ( 'NONE', *, *, #11666, .T. ) ;
#6148=CARTESIAN_POINT ( 'NONE',  ( 7.900000000000000355, 21.00000000000000000, 18.00000000000000355 ) ) ;
#6162=AXIS2_PLACEMENT_3D ( 'NONE', #63025, #9991, #14581 ) ;
#6187=UNCERTAINTY_MEASURE_WITH_UNIT (LENGTH_MEASURE( 1.000000000000000082E-05 ), #12318, 'distance_accuracy_value', 'NONE');
#6188=DIRECTION ( 'NONE',  ( 0.000000000000000000, 0.000000000000000000, -1.000000000000000000 ) ) ;
#6193=CIRCLE ( 'NONE', #19695, 2.458500000000000796 ) ;
#6195=AXIS2_PLACEMENT_3D ( 'NONE', #32752, #5888, #27452 ) ;
#6202=DIRECTION ( 'NONE',  ( 0.000000000000000000, 0.000000000000000000, -1.000000000000000000 ) ) ;
#6210=PLANE ( 'NONE',  #20617 ) ;
#6218=CARTESIAN_POINT ( 'NONE',  ( 21.90000000000000213, -14.06939075806900874, 20.80000000000001137 ) ) ;
#6224=LINE ( 'NONE', #1596, #67375 ) ;
#6225=DIRECTION ( 'NONE',  ( -1.000000000000000000, 0.000000000000000000, 0.000000000000000000 ) ) ;
#6232=ORIENTED_EDGE ( 'NONE', *, *, #42919, .T. ) ;
#6238=DIRECTION ( 'NONE',  ( 0.000000000000000000, -0.7071067811865474617, -0.7071067811865474617 ) ) ;
#6257=DIRECTION ( 'NONE',  ( 0.000000000000000000, 0.000000000000000000, -1.000000000000000000 ) ) ;
#6258=DIRECTION ( 'NONE',  ( 0.000000000000000000, 0.000000000000000000, -1.000000000000000000 ) ) ;
#6259=VECTOR ( 'NONE', #6934, 1000.000000000000000 ) ;
#6263=ORIENTED_EDGE ( 'NONE', *, *, #28672, .F. ) ;
#6266=LINE ( 'NONE', #10530, #30870 ) ;
#6270=AXIS2_PLACEMENT_3D ( 'NONE', #67354, #8990, #9352 ) ;
#6278=ORIENTED_EDGE ( 'NONE', *, *, #23486, .T. ) ;
#6282=FILL_AREA_STYLE ('',( #39485 ) ) ;
#6287=DIRECTION ( 'NONE',  ( -1.000000000000000000, 0.000000000000000000, 0.000000000000000000 ) ) ;
#6293=FACE_BOUND ( 'NONE', #17429, .T. ) ;
#6297=DIRECTION ( 'NONE',  ( 1.000000000000000000, -0.000000000000000000, 0.000000000000000000 ) ) ;
#6302=CARTESIAN_POINT ( 'NONE',  ( 0.5000000000000000000, 18.00000000000000355, -21.00000000000000000 ) ) ;
#6324=CARTESIAN_POINT ( 'NONE',  ( 41.09999999999999432, -21.00000000000000000, 13.86939075806900057 ) ) ;
#6326=( GEOMETRIC_REPRESENTATION_CONTEXT ( 3 ) GLOBAL_UNCERTAINTY_ASSIGNED_CONTEXT ( ( #4112 ) ) GLOBAL_UNIT_ASSIGNED_CONTEXT ( ( #36386, #14827, #14479 ) ) REPRESENTATION_CONTEXT ( 'NONE', 'WORKASPACE' ) );
#6328=CARTESIAN_POINT ( 'NONE',  ( 16.89999999999999858, 20.60000000000000142, -13.86939075806900057 ) ) ;
#6329=CARTESIAN_POINT ( 'NONE',  ( 49.00000000000000000, -0.2000000000089119934, 8.909539772616881237E-12 ) ) ;
#6335=EDGE_CURVE ( 'NONE', #33050, #61094, #3833, .T. ) ;
#6340=ADVANCED_FACE ( 'NONE', ( #57576 ), #19045, .F. ) ;
#6352=AXIS2_PLACEMENT_3D ( 'NONE', #58523, #41886, #19971 ) ;
#6364=VECTOR ( 'NONE', #18314, 1000.000000000000114 ) ;
#6366=DIRECTION ( 'NONE',  ( -1.000000000000000000, 0.000000000000000000, 0.000000000000000000 ) ) ;
#6378=CARTESIAN_POINT ( 'NONE',  ( 39.00000000000000000, -0.2000000000000000111, 0.000000000000000000 ) ) ;
#6400=FACE_OUTER_BOUND ( 'NONE', #8282, .T. ) ;
#6401=CARTESIAN_POINT ( 'NONE',  ( 28.90000000000000213, -21.00000000000000000, 13.86939075806900057 ) ) ;
#6413=EDGE_CURVE ( 'NONE', #8950, #47029, #26114, .T. ) ;
#6417=CIRCLE ( 'NONE', #1914, 24.99999999998784972 ) ;
#6424=ORIENTED_EDGE ( 'NONE', *, *, #9020, .T. ) ;
#6437=LINE ( 'NONE', #1131, #43189 ) ;
#6440=ORIENTED_EDGE ( 'NONE', *, *, #28472, .T. ) ;
#6442=EDGE_CURVE ( 'NONE', #60266, #6963, #4887, .T. ) ;
#6458=CARTESIAN_POINT ( 'NONE',  ( 48.66598694767480993, -0.7500000000000044409, -3.588632928360947272 ) ) ;
#6464=LINE ( 'NONE', #48552, #69033 ) ;
#6473=EDGE_CURVE ( 'NONE', #27668, #63779, #28324, .T. ) ;
#6474=DIRECTION ( 'NONE',  ( 1.000000000000000000, -0.000000000000000000, 0.000000000000000000 ) ) ;
#6483=DIRECTION ( 'NONE',  ( 1.000000000000000000, 0.000000000000000000, 0.000000000000000000 ) ) ;
#6484=EDGE_CURVE ( 'NONE', #48934, #20922, #63318, .T. ) ;
#6485=DIRECTION ( 'NONE',  ( 0.000000000000000000, 0.000000000000000000, -1.000000000000000000 ) ) ;
#6492=CARTESIAN_POINT ( 'NONE',  ( 46.39999999999999858, 33.00000000000000000, -1.250000000000000000 ) ) ;
#6496=( GEOMETRIC_REPRESENTATION_CONTEXT ( 3 ) GLOBAL_UNCERTAINTY_ASSIGNED_CONTEXT ( ( #15414 ) ) GLOBAL_UNIT_ASSIGNED_CONTEXT ( ( #53713, #59701, #38150 ) ) REPRESENTATION_CONTEXT ( 'NONE', 'WORKASPACE' ) );
#6497=EDGE_CURVE ( 'NONE', #2624, #17564, #43055, .T. ) ;
#6500=DIRECTION ( 'NONE',  ( 0.000000000000000000, 0.000000000000000000, 1.000000000000000000 ) ) ;
#6505=ADVANCED_FACE ( 'NONE', ( #25772 ), #63592, .F. ) ;
#6514=EDGE_CURVE ( 'NONE', #38926, #12, #43397, .T. ) ;
#6522=AXIS2_PLACEMENT_3D ( 'NONE', #43379, #21820, #32776 ) ;
#6526=ORIENTED_EDGE ( 'NONE', *, *, #42402, .T. ) ;
#6543=PLANE ( 'NONE',  #37913 ) ;
#6547=CARTESIAN_POINT ( 'NONE',  ( 49.00000000000000000, -0.1999999999911430404, -8.864436962241481021E-12 ) ) ;
#6559=EDGE_LOOP ( 'NONE', ( #4717, #8847, #22737, #28260 ) ) ;
#6562=VECTOR ( 'NONE', #12669, 1000.000000000000000 ) ;
#6576=VECTOR ( 'NONE', #35148, 1000.000000000000000 ) ;
#6577=EDGE_LOOP ( 'NONE', ( #56751, #53889, #60130, #9657, #28682, #22718, #64286, #31868, #53854, #3333, #31565, #59999 ) ) ;
#6585=CARTESIAN_POINT ( 'NONE',  ( 41.09999999999999432, 13.66939075806899950, -20.80000000000000426 ) ) ;
#6589=CARTESIAN_POINT ( 'NONE',  ( 39.90000000000000568, 13.66939075806899240, -20.79999999999999361 ) ) ;
#6596=ORIENTED_EDGE ( 'NONE', *, *, #51394, .T. ) ;
#6601=DIRECTION ( 'NONE',  ( 1.000000000000000000, -0.000000000000000000, 0.000000000000000000 ) ) ;
#6612=DIRECTION ( 'NONE',  ( 1.000000000000000000, 0.000000000000000000, 0.000000000000000000 ) ) ;
#6613=DIRECTION ( 'NONE',  ( 0.000000000000000000, 0.000000000000000000, 1.000000000000000000 ) ) ;
#6620=CARTESIAN_POINT ( 'NONE',  ( 39.90000000000000568, -21.00000000000000000, 16.96999999999999886 ) ) ;
#6624=DIRECTION ( 'NONE',  ( 0.000000000000000000, 0.000000000000000000, -1.000000000000000000 ) ) ;
#6653=DIRECTION ( 'NONE',  ( 1.000000000000000000, -0.000000000000000000, 0.000000000000000000 ) ) ;
#6660=VERTEX_POINT ( 'NONE', #5926 ) ;
#6664=DIRECTION ( 'NONE',  ( 0.000000000000000000, 0.000000000000000000, 1.000000000000000000 ) ) ;
#6668=ORIENTED_EDGE ( 'NONE', *, *, #20241, .T. ) ;
#6672=CYLINDRICAL_SURFACE ( 'NONE', #41136, 2.458500000000000796 ) ;
#6683=EDGE_LOOP ( 'NONE', ( #56005, #49913, #69060, #41127 ) ) ;
#6690=EDGE_LOOP ( 'NONE', ( #35826, #66377, #14501, #26171 ) ) ;
#6700=ORIENTED_EDGE ( 'NONE', *, *, #44058, .F. ) ;
#6705=CARTESIAN_POINT ( 'NONE',  ( 48.50000000000000000, -0.7500000000000000000, 3.418698582794335028 ) ) ;
#6707=CARTESIAN_POINT ( 'NONE',  ( 41.09999999999999432, 20.60000000000000142, 13.86939075806900057 ) ) ;
#6721=ADVANCED_FACE ( 'NONE', ( #13652 ), #30623, .F. ) ;
#6725=ORIENTED_EDGE ( 'NONE', *, *, #26979, .F. ) ;
#6734=VECTOR ( 'NONE', #21116, 1000.000000000000000 ) ;
#6747=DIRECTION ( 'NONE',  ( 1.000000000000000000, -0.000000000000000000, 0.000000000000000000 ) ) ;
#6749=ORIENTED_EDGE ( 'NONE', *, *, #13085, .T. ) ;
#6773=DIRECTION ( 'NONE',  ( 1.000000000000000000, -0.000000000000000000, 0.000000000000000000 ) ) ;
#6779=CARTESIAN_POINT ( 'NONE',  ( 48.50000000000000000, -0.7500000000000000000, -3.418698582794335028 ) ) ;
#6785=EDGE_LOOP ( 'NONE', ( #40661, #26020, #58476, #17000 ) ) ;
#6787=CIRCLE ( 'NONE', #13560, 0.5000000000000000000 ) ;
#6791=CARTESIAN_POINT ( 'NONE',  ( 46.39999999999999858, 33.00000000000000000, 2.250000000000000444 ) ) ;
#6792=ADVANCED_FACE ( 'NONE', ( #35929 ), #18965, .F. ) ;
#6796=ORIENTED_EDGE ( 'NONE', *, *, #20653, .F. ) ;
#6799=DIRECTION ( 'NONE',  ( 1.000000000000000000, -0.000000000000000000, 0.000000000000000000 ) ) ;
#6805=DIRECTION ( 'NONE',  ( 1.000000000000000000, 0.000000000000000000, 0.000000000000000000 ) ) ;
#6808=CARTESIAN_POINT ( 'NONE',  ( 41.09999999999999432, 20.60000000000000142, -13.86939075806900057 ) ) ;
#6827=AXIS2_PLACEMENT_3D ( 'NONE', #40703, #25508, #52742 ) ;
#6832=FACE_OUTER_BOUND ( 'NONE', #47492, .T. ) ;
#6835=AXIS2_PLACEMENT_3D ( 'NONE', #57699, #57350, #8904 ) ;
#6837=PLANE ( 'NONE',  #12676 ) ;
#6841=EDGE_CURVE ( 'NONE', #32973, #53390, #58886, .T. ) ;
#6852=ADVANCED_FACE ( 'NONE', ( #68808 ), #41581, .T. ) ;
#6863=ORIENTED_EDGE ( 'NONE', *, *, #3698, .T. ) ;
#6872=EDGE_CURVE ( 'NONE', #44485, #11292, #26369, .T. ) ;
#6877=CYLINDRICAL_SURFACE ( 'NONE', #1080, 5.250000000000000000 ) ;
#6879=ORIENTED_EDGE ( 'NONE', *, *, #52090, .T. ) ;
#6883=AXIS2_PLACEMENT_3D ( 'NONE', #29054, #50625, #50970 ) ;
#6895=CARTESIAN_POINT ( 'NONE',  ( 49.00000000000000000, 20.60000000000000142, -13.86939075806900057 ) ) ;
#6900=VERTEX_POINT ( 'NONE', #21065 ) ;
#6917=CYLINDRICAL_SURFACE ( 'NONE', #16495, 2.458500000000000796 ) ;
#6921=CARTESIAN_POINT ( 'NONE',  ( 25.90000000000000213, 0.000000000000000000, -0.5540281690140901327 ) ) ;
#6933=FACE_OUTER_BOUND ( 'NONE', #20918, .T. ) ;
#6934=DIRECTION ( 'NONE',  ( 0.000000000000000000, 0.000000000000000000, 1.000000000000000000 ) ) ;
#6939=CLOSED_SHELL ( 'NONE', ( #28752, #14437, #2017, #66865, #35373, #14211, #25258, #19018, #7757, #65169, #59861, #47669 ) ) ;
#6941=ORIENTED_EDGE ( 'NONE', *, *, #68215, .T. ) ;
#6943=EDGE_CURVE ( 'NONE', #34215, #15393, #8015, .T. ) ;
#6954=DIRECTION ( 'NONE',  ( 0.000000000000000000, 0.000000000000000000, -1.000000000000000000 ) ) ;
#6959=FACE_OUTER_BOUND ( 'NONE', #54193, .T. ) ;
#6961=DIRECTION ( 'NONE',  ( -1.000000000000000000, 0.000000000000000000, 0.000000000000000000 ) ) ;
#6963=VERTEX_POINT ( 'NONE', #54997 ) ;
#6965=DIRECTION ( 'NONE',  ( 0.000000000000000000, 0.000000000000000000, 1.000000000000000000 ) ) ;
#6967=DIRECTION ( 'NONE',  ( -1.000000000000000000, 0.000000000000000000, 0.000000000000000000 ) ) ;
#6969=ORIENTED_EDGE ( 'NONE', *, *, #14227, .T. ) ;
#6987=AXIS2_PLACEMENT_3D ( 'NONE', #13268, #12902, #35524 ) ;
#7000=FILL_AREA_STYLE ('',( #45171 ) ) ;
#7016=DIRECTION ( 'NONE',  ( 0.000000000000000000, 0.000000000000000000, -1.000000000000000000 ) ) ;
#7023=EDGE_CURVE ( 'NONE', #27652, #40990, #22461, .T. ) ;
#7031=CARTESIAN_POINT ( 'NONE',  ( 24.90000000000000213, 20.60000000000000142, -13.86939075806900057 ) ) ;
#7044=( NAMED_UNIT ( * ) SI_UNIT ( $, .STERADIAN. ) SOLID_ANGLE_UNIT ( ) );
#7082=VERTEX_POINT ( 'NONE', #54643 ) ;
#7083=VECTOR ( 'NONE', #16261, 1000.000000000000000 ) ;
#7108=DIRECTION ( 'NONE',  ( 1.000000000000000000, -0.000000000000000000, 0.000000000000000000 ) ) ;
#7113=EDGE_CURVE ( 'NONE', #57421, #20590, #56644, .T. ) ;
#7120=DIRECTION ( 'NONE',  ( 1.000000000000000000, -0.000000000000000000, 0.000000000000000000 ) ) ;
#7127=( NAMED_UNIT ( * ) PLANE_ANGLE_UNIT ( ) SI_UNIT ( $, .RADIAN. ) );
#7136=ORIENTED_EDGE ( 'NONE', *, *, #38484, .T. ) ;
#7146=FACE_OUTER_BOUND ( 'NONE', #25978, .T. ) ;
#7152=VERTEX_POINT ( 'NONE', #18888 ) ;
#7153=STYLED_ITEM ( 'NONE', ( #37775 ), #43035 ) ;
#7158=ORIENTED_EDGE ( 'NONE', *, *, #58638, .F. ) ;
#7166=FACE_OUTER_BOUND ( 'NONE', #19143, .T. ) ;
#7167=DIRECTION ( 'NONE',  ( 0.000000000000000000, 0.000000000000000000, -1.000000000000000000 ) ) ;
#7179=ORIENTED_EDGE ( 'NONE', *, *, #61740, .F. ) ;
#7199=ADVANCED_FACE ( 'NONE', ( #39734 ), #56359, .T. ) ;
#7201=ORIENTED_EDGE ( 'NONE', *, *, #8252, .T. ) ;
#7207=FACE_OUTER_BOUND ( 'NONE', #31511, .T. ) ;
#7214=ORIENTED_EDGE ( 'NONE', *, *, #20688, .T. ) ;
#7215=VECTOR ( 'NONE', #797, 1000.000000000000000 ) ;
#7223=CARTESIAN_POINT ( 'NONE',  ( 49.49874101024862227, 0.7500000000000000000, -4.436434848928188401 ) ) ;
#7233=LINE ( 'NONE', #47100, #31703 ) ;
#7237=AXIS2_PLACEMENT_3D ( 'NONE', #21316, #64799, #27657 ) ;
#7239=CARTESIAN_POINT ( 'NONE',  ( 49.00000000000000000, -0.2000000000089119934, -8.913009219568841313E-12 ) ) ;
#7253=VERTEX_POINT ( 'NONE', #42193 ) ;
#7256=DIRECTION ( 'NONE',  ( 0.000000000000000000, 0.000000000000000000, 1.000000000000000000 ) ) ;
#7259=ORIENTED_EDGE ( 'NONE', *, *, #63855, .F. ) ;
#7266=LINE ( 'NONE', #56413, #11987 ) ;
#7269=LINE ( 'NONE', #28157, #57733 ) ;
#7273=CARTESIAN_POINT ( 'NONE',  ( 27.90000000000000213, 13.66939075806899240, -20.79999999999999361 ) ) ;
#7274=EDGE_CURVE ( 'NONE', #42593, #37725, #35175, .T. ) ;
#7282=ORIENTED_EDGE ( 'NONE', *, *, #63437, .T. ) ;
#7296=CARTESIAN_POINT ( 'NONE',  ( 41.09999999999999432, -0.2000000000000000111, 0.000000000000000000 ) ) ;
#7300=MECHANICAL_DESIGN_GEOMETRIC_PRESENTATION_REPRESENTATION('',(#35526),#52511);
#7316=EDGE_CURVE ( 'NONE', #44206, #16386, #41502, .T. ) ;
#7322=ORIENTED_EDGE ( 'NONE', *, *, #56224, .F. ) ;
#7329=CARTESIAN_POINT ( 'NONE',  ( 39.00000000000000000, -14.48845687959340012, -21.00000000000000000 ) ) ;
#7338=EDGE_LOOP ( 'NONE', ( #7978, #33174, #7785, #29976 ) ) ;
#7344=VECTOR ( 'NONE', #51563, 1000.000000000000000 ) ;
#7358=DIRECTION ( 'NONE',  ( -1.000000000000000000, 0.000000000000000000, 0.000000000000000000 ) ) ;
#7361=LINE ( 'NONE', #2070, #54933 ) ;
#7362=DIRECTION ( 'NONE',  ( -1.000000000000000000, 0.000000000000000000, 0.000000000000000000 ) ) ;
#7370=ADVANCED_FACE ( 'NONE', ( #41039 ), #3221, .T. ) ;
#7381=LINE ( 'NONE', #14093, #20023 ) ;
#7389=CARTESIAN_POINT ( 'NONE',  ( 25.57999999999999829, 0.000000000000000000, 5.250000000000000000 ) ) ;
#7394=ORIENTED_EDGE ( 'NONE', *, *, #49660, .F. ) ;
#7395=DIRECTION ( 'NONE',  ( -1.000000000000000000, 0.000000000000000000, 0.000000000000000000 ) ) ;
#7400=DIRECTION ( 'NONE',  ( 1.000000000000000000, -0.000000000000000000, 0.000000000000000000 ) ) ;
#7432=ORIENTED_EDGE ( 'NONE', *, *, #51264, .F. ) ;
#7443=ORIENTED_EDGE ( 'NONE', *, *, #4756, .T. ) ;
#7448=DIRECTION ( 'NONE',  ( 1.000000000000000000, -0.000000000000000000, 0.000000000000000000 ) ) ;
#7451=VECTOR ( 'NONE', #27419, 1000.000000000000000 ) ;
#7457=FACE_OUTER_BOUND ( 'NONE', #34564, .T. ) ;
#7460=VERTEX_POINT ( 'NONE', #18778 ) ;
#7470=CARTESIAN_POINT ( 'NONE',  ( 7.899999999999999467, 14.08845687959340331, -21.00000000000000000 ) ) ;
#7472=VERTEX_POINT ( 'NONE', #29729 ) ;
#7478=AXIS2_PLACEMENT_3D ( 'NONE', #40012, #62288, #8540 ) ;
#7483=CARTESIAN_POINT ( 'NONE',  ( 39.00000000000000000, 0.000000000000000000, 3.500000000000000000 ) ) ;
#7491=FACE_OUTER_BOUND ( 'NONE', #57979, .T. ) ;
#7496=VECTOR ( 'NONE', #60819, 1000.000000000000114 ) ;
#7516=EDGE_CURVE ( 'NONE', #50665, #59763, #58686, .T. ) ;
#7519=ORIENTED_EDGE ( 'NONE', *, *, #22070, .F. ) ;
#7523=ORIENTED_EDGE ( 'NONE', *, *, #53100, .F. ) ;
#7528=ORIENTED_EDGE ( 'NONE', *, *, #18541, .F. ) ;
#7532=DIRECTION ( 'NONE',  ( 0.000000000000000000, 0.000000000000000000, -1.000000000000000000 ) ) ;
#7533=CARTESIAN_POINT ( 'NONE',  ( 55.00000000000000000, 6.429395695523604153E-16, -5.250000000000000000 ) ) ;
#7544=EDGE_LOOP ( 'NONE', ( #25228, #10074, #37006, #41603 ) ) ;
#7548=VECTOR ( 'NONE', #62384, 1000.000000000000000 ) ;
#7551=ORIENTED_EDGE ( 'NONE', *, *, #66819, .F. ) ;
#7555=EDGE_CURVE ( 'NONE', #28, #48934, #10276, .T. ) ;
#7558=VECTOR ( 'NONE', #20032, 1000.000000000000000 ) ;
#7560=VERTEX_POINT ( 'NONE', #36086 ) ;
#7564=VERTEX_POINT ( 'NONE', #32186 ) ;
#7569=CARTESIAN_POINT ( 'NONE',  ( 49.00000000000000000, -0.1999999999911430404, -8.864436962241481021E-12 ) ) ;
#7605=DIRECTION ( 'NONE',  ( 0.000000000000000000, 0.000000000000000000, 1.000000000000000000 ) ) ;
#7612=FILL_AREA_STYLE_COLOUR ( '', #47852 ) ;
#7614=DIRECTION ( 'NONE',  ( -1.000000000000000000, 0.000000000000000000, 0.000000000000000000 ) ) ;
#7618=EDGE_CURVE ( 'NONE', #57546, #64704, #14882, .T. ) ;
#7620=DIRECTION ( 'NONE',  ( 0.000000000000000000, 0.000000000000000000, -1.000000000000000000 ) ) ;
#7625=ORIENTED_EDGE ( 'NONE', *, *, #67010, .F. ) ;
#7628=CARTESIAN_POINT ( 'NONE',  ( 39.90000000000000568, -0.000000000000000000, 20.80000000000000426 ) ) ;
#7634=CYLINDRICAL_SURFACE ( 'NONE', #22214, 24.99999999998784972 ) ;
#7645=CARTESIAN_POINT ( 'NONE',  ( 49.00000000000000000, -14.06939075806900163, -20.80000000000000426 ) ) ;
#7652=CARTESIAN_POINT ( 'NONE',  ( 49.00000000000000000, -0.1999999999911430404, -8.864436962241481021E-12 ) ) ;
#7673=VECTOR ( 'NONE', #32592, 1000.000000000000000 ) ;
#7676=DIRECTION ( 'NONE',  ( 0.000000000000000000, 0.1500000000000006328, -0.9886859966642592701 ) ) ;
#7684=LINE ( 'NONE', #8746, #13876 ) ;
#7697=SURFACE_SIDE_STYLE ('',( #2057 ) ) ;
#7741=DIRECTION ( 'NONE',  ( 1.000000000000000000, -0.000000000000000000, 0.000000000000000000 ) ) ;
#7757=ADVANCED_FACE ( 'NONE', ( #32548 ), #33814, .F. ) ;
#7758=SURFACE_STYLE_USAGE ( .BOTH. , #56211 ) ;
#7765=ORIENTED_EDGE ( 'NONE', *, *, #30884, .F. ) ;
#7768=ORIENTED_EDGE ( 'NONE', *, *, #7516, .T. ) ;
#7769=CARTESIAN_POINT ( 'NONE',  ( 8.900000000000005684, -0.2000000000000000111, 0.000000000000000000 ) ) ;
#7781=DIRECTION ( 'NONE',  ( 0.000000000000000000, -1.000000000000000000, 0.000000000000000000 ) ) ;
#7785=ORIENTED_EDGE ( 'NONE', *, *, #17247, .T. ) ;
#7788=LINE ( 'NONE', #62236, #20275 ) ;
#7796=LINE ( 'NONE', #25479, #50416 ) ;
#7799=ORIENTED_EDGE ( 'NONE', *, *, #22569, .T. ) ;
#7815=VERTEX_POINT ( 'NONE', #8332 ) ;
#7817=CARTESIAN_POINT ( 'NONE',  ( 39.00000000000000000, 21.00000000000000000, -16.96999999999999886 ) ) ;
#7824=ORIENTED_EDGE ( 'NONE', *, *, #43135, .F. ) ;
#7832=DIRECTION ( 'NONE',  ( -1.000000000000000000, 0.000000000000000000, 0.000000000000000000 ) ) ;
#7835=AXIS2_PLACEMENT_3D ( 'NONE', #8752, #55541, #60488 ) ;
#7852=AXIS2_PLACEMENT_3D ( 'NONE', #7938, #66646, #50035 ) ;
#7870=ORIENTED_EDGE ( 'NONE', *, *, #490, .F. ) ;
#7877=SURFACE_SIDE_STYLE ('',( #61265 ) ) ;
#7886=EDGE_CURVE ( 'NONE', #32538, #30457, #24621, .T. ) ;
#7887=DIRECTION ( 'NONE',  ( -1.000000000000000000, 0.000000000000000000, 0.000000000000000000 ) ) ;
#7901=DIRECTION ( 'NONE',  ( 0.000000000000000000, -1.000000000000000000, 0.000000000000000000 ) ) ;
#7903=EDGE_CURVE ( 'NONE', #29653, #30889, #41214, .T. ) ;
#7906=ORIENTED_EDGE ( 'NONE', *, *, #4347, .F. ) ;
#7909=CARTESIAN_POINT ( 'NONE',  ( 49.00000000000000000, -0.2000000000089119934, -8.913009219568841313E-12 ) ) ;
#7922=LINE ( 'NONE', #50371, #19625 ) ;
#7937=VERTEX_POINT ( 'NONE', #41921 ) ;
#7938=CARTESIAN_POINT ( 'NONE',  ( 30.90000000000000213, 0.000000000000000000, 2.370429594502469981E-15 ) ) ;
#7948=DIRECTION ( 'NONE',  ( 0.000000000000000000, 0.000000000000000000, 1.000000000000000000 ) ) ;
#7952=DIRECTION ( 'NONE',  ( 0.000000000000000000, 1.000000000000000000, -0.000000000000000000 ) ) ;
#7953=AXIS2_PLACEMENT_3D ( 'NONE', #459, #28693, #12087 ) ;
#7954=ORIENTED_EDGE ( 'NONE', *, *, #6872, .T. ) ;
#7963=EDGE_LOOP ( 'NONE', ( #44618, #14542, #58710, #23753 ) ) ;
#7964=DIRECTION ( 'NONE',  ( -1.000000000000000000, 0.000000000000000000, 0.000000000000000000 ) ) ;
#7965=ORIENTED_EDGE ( 'NONE', *, *, #36786, .T. ) ;
#7967=CARTESIAN_POINT ( 'NONE',  ( 49.00000000000000000, -21.00000000000000000, 13.86939075806900057 ) ) ;
#7968=CARTESIAN_POINT ( 'NONE',  ( 34.89999999999999858, 0.000000000000000000, 0.000000000000000000 ) ) ;
#7978=ORIENTED_EDGE ( 'NONE', *, *, #51634, .F. ) ;
#7984=EDGE_CURVE ( 'NONE', #43890, #46512, #10446, .T. ) ;
#7993=DIRECTION ( 'NONE',  ( 1.000000000000000000, -0.000000000000000000, 0.000000000000000000 ) ) ;
#7995=EDGE_CURVE ( 'NONE', #60486, #20922, #15413, .T. ) ;
#7996=LINE ( 'NONE', #12601, #17946 ) ;
#7998=VECTOR ( 'NONE', #50320, 1000.000000000000000 ) ;
#8007=CARTESIAN_POINT ( 'NONE',  ( 47.00000000000000000, 4.286263797015736595E-16, -3.500000000000000000 ) ) ;
#8015=CIRCLE ( 'NONE', #22731, 24.99999999998784972 ) ;
#8024=CARTESIAN_POINT ( 'NONE',  ( 27.90000000000000213, -0.1999999999911430404, -8.864436962241481021E-12 ) ) ;
#8026=DIRECTION ( 'NONE',  ( 1.000000000000000000, 0.000000000000000000, 0.000000000000000000 ) ) ;
#8030=ORIENTED_EDGE ( 'NONE', *, *, #44863, .F. ) ;
#8034=LINE ( 'NONE', #40575, #14161 ) ;
#8045=EDGE_LOOP ( 'NONE', ( #15241, #41370, #7625, #7179 ) ) ;
#8049=ORIENTED_EDGE ( 'NONE', *, *, #42409, .T. ) ;
#8053=ORIENTED_EDGE ( 'NONE', *, *, #31082, .T. ) ;
#8057=FACE_OUTER_BOUND ( 'NONE', #63666, .T. ) ;
#8078=DIRECTION ( 'NONE',  ( 1.000000000000000000, -0.000000000000000000, 0.000000000000000000 ) ) ;
#8081=AXIS2_PLACEMENT_3D ( 'NONE', #8888, #52035, #31179 ) ;
#8098=VERTEX_POINT ( 'NONE', #17478 ) ;
#8101=DIRECTION ( 'NONE',  ( -1.000000000000000000, 0.000000000000000000, 0.000000000000000000 ) ) ;
#8103=ORIENTED_EDGE ( 'NONE', *, *, #16394, .T. ) ;
#8106=CARTESIAN_POINT ( 'NONE',  ( 40.90000000000000568, -16.96999999999999886, 21.00000000000000000 ) ) ;
#8112=ORIENTED_EDGE ( 'NONE', *, *, #27139, .F. ) ;
#8147=CARTESIAN_POINT ( 'NONE',  ( 0.5000000000000000000, -18.00000000000000355, -21.00000000000000000 ) ) ;
#8154=EDGE_CURVE ( 'NONE', #28954, #56111, #27750, .T. ) ;
#8156=EDGE_CURVE ( 'NONE', #1910, #55424, #39728, .T. ) ;
#8165=FACE_OUTER_BOUND ( 'NONE', #31987, .T. ) ;
#8166=ORIENTED_EDGE ( 'NONE', *, *, #39820, .F. ) ;
#8175=LINE ( 'NONE', #17398, #3521 ) ;
#8186=AXIS2_PLACEMENT_3D ( 'NONE', #10815, #15434, #53618 ) ;
#8188=CARTESIAN_POINT ( 'NONE',  ( 28.90000000000000213, 13.66939075806899240, -20.79999999999999361 ) ) ;
#8196=LINE ( 'NONE', #29766, #13370 ) ;
#8201=CARTESIAN_POINT ( 'NONE',  ( 49.00000000000000000, -0.1999999999911795112, 8.826273045769999343E-12 ) ) ;
#8204=VECTOR ( 'NONE', #24595, 1000.000000000000114 ) ;
#8205=ORIENTED_EDGE ( 'NONE', *, *, #34931, .F. ) ;
#8209=ORIENTED_EDGE ( 'NONE', *, *, #46738, .T. ) ;
#8211=DIRECTION ( 'NONE',  ( -1.000000000000000000, 0.000000000000000000, 0.000000000000000000 ) ) ;
#8221=VERTEX_POINT ( 'NONE', #35836 ) ;
#8229=DIRECTION ( 'NONE',  ( 0.000000000000000000, 1.000000000000000000, 0.000000000000000000 ) ) ;
#8236=EDGE_CURVE ( 'NONE', #5139, #27370, #4023, .T. ) ;
#8244=ORIENTED_EDGE ( 'NONE', *, *, #17591, .T. ) ;
#8252=EDGE_CURVE ( 'NONE', #62948, #51099, #29480, .T. ) ;
#8257=EDGE_CURVE ( 'NONE', #59763, #50665, #49710, .T. ) ;
#8265=COLOUR_RGB ( '', 0.08235294, 0.09019608, 0.10196078) ;
#8266=CIRCLE ( 'NONE', #47800, 24.99999999998784972 ) ;
#8282=EDGE_LOOP ( 'NONE', ( #5574, #39725, #9669, #67524, #13706, #42156, #32015, #55094 ) ) ;
#8288=DIRECTION ( 'NONE',  ( 0.000000000000000000, 0.000000000000000000, -1.000000000000000000 ) ) ;
#8292=LINE ( 'NONE', #51444, #47723 ) ;
#8295=FACE_OUTER_BOUND ( 'NONE', #52612, .T. ) ;
#8301=PLANE ( 'NONE',  #20384 ) ;
#8331=ORIENTED_EDGE ( 'NONE', *, *, #29576, .F. ) ;
#8332=CARTESIAN_POINT ( 'NONE',  ( 36.90000000000000568, 13.66939075806899240, 20.79999999999999361 ) ) ;
#8342=VECTOR ( 'NONE', #20834, 1000.000000000000000 ) ;
#8344=CARTESIAN_POINT ( 'NONE',  ( 17.89999999999999858, -0.1999999999911430404, -8.864436962241481021E-12 ) ) ;
#8347=VECTOR ( 'NONE', #46650, 1000.000000000000114 ) ;
#8350=DIRECTION ( 'NONE',  ( 1.000000000000000000, 0.000000000000000000, 0.000000000000000000 ) ) ;
#8351=DIRECTION ( 'NONE',  ( 0.000000000000000000, 0.000000000000000000, -1.000000000000000000 ) ) ;
#8353=ORIENTED_EDGE ( 'NONE', *, *, #54021, .T. ) ;
#8356=CARTESIAN_POINT ( 'NONE',  ( 41.09999999999999432, -0.2000000000000000111, 0.000000000000000000 ) ) ;
#8371=FACE_OUTER_BOUND ( 'NONE', #40411, .T. ) ;
#8408=AXIS2_PLACEMENT_3D ( 'NONE', #29012, #66832, #29348 ) ;
#8423=ORIENTED_EDGE ( 'NONE', *, *, #30090, .T. ) ;
#8426=DIRECTION ( 'NONE',  ( 0.000000000000000000, 0.000000000000000000, -1.000000000000000000 ) ) ;
#8437=VERTEX_POINT ( 'NONE', #52831 ) ;
#8439=ORIENTED_EDGE ( 'NONE', *, *, #59326, .F. ) ;
#8468=DIRECTION ( 'NONE',  ( 1.000000000000000000, -0.000000000000000000, 0.000000000000000000 ) ) ;
#8480=CARTESIAN_POINT ( 'NONE',  ( 49.00000000000000000, 20.60000000000000142, -13.86939075806900057 ) ) ;
#8483=ORIENTED_EDGE ( 'NONE', *, *, #12475, .T. ) ;
#8487=EDGE_CURVE ( 'NONE', #48502, #245, #29408, .T. ) ;
#8503=ORIENTED_EDGE ( 'NONE', *, *, #47724, .T. ) ;
#8504=CARTESIAN_POINT ( 'NONE',  ( 39.00000000000000000, -21.00000000000000000, -16.96999999999999886 ) ) ;
#8506=VECTOR ( 'NONE', #37790, 1000.000000000000000 ) ;
#8510=EDGE_LOOP ( 'NONE', ( #55154, #35024, #10865, #15061 ) ) ;
#8513=DIRECTION ( 'NONE',  ( 0.000000000000000000, 0.000000000000000000, 1.000000000000000000 ) ) ;
#8517=CARTESIAN_POINT ( 'NONE',  ( 9.900000000000000355, 18.00000000000000355, -21.00000000000000000 ) ) ;
#8524=( LENGTH_UNIT ( ) NAMED_UNIT ( * ) SI_UNIT ( .MILLI., .METRE. ) );
#8525=ORIENTED_EDGE ( 'NONE', *, *, #53658, .F. ) ;
#8533=EDGE_CURVE ( 'NONE', #67686, #22473, #61205, .T. ) ;
#8540=DIRECTION ( 'NONE',  ( 0.000000000000000000, 0.000000000000000000, 1.000000000000000000 ) ) ;
#8547=EDGE_LOOP ( 'NONE', ( #7322, #54692, #12201, #21917 ) ) ;
#8549=DIRECTION ( 'NONE',  ( 0.000000000000000000, -0.7071067811865474617, 0.7071067811865474617 ) ) ;
#8566=CIRCLE ( 'NONE', #61664, 24.99999999998794920 ) ;
#8572=EDGE_CURVE ( 'NONE', #33487, #51627, #47497, .T. ) ;
#8577=ORIENTED_EDGE ( 'NONE', *, *, #43183, .F. ) ;
#8599=FACE_OUTER_BOUND ( 'NONE', #23475, .T. ) ;
#8607=VECTOR ( 'NONE', #22751, 1000.000000000000114 ) ;
#8610=ORIENTED_EDGE ( 'NONE', *, *, #68341, .T. ) ;
#8645=VERTEX_POINT ( 'NONE', #8517 ) ;
#8647=CARTESIAN_POINT ( 'NONE',  ( 41.09999999999999432, 20.60000000000000142, 13.86939075806900057 ) ) ;
#8653=CIRCLE ( 'NONE', #44769, 24.99999999998784972 ) ;
#8665=CARTESIAN_POINT ( 'NONE',  ( 25.57999999999999829, 3.010794155703768650E-16, -2.458500000000000796 ) ) ;
#8692=DIRECTION ( 'NONE',  ( -1.000000000000000000, 0.000000000000000000, 0.000000000000000000 ) ) ;
#8699=VERTEX_POINT ( 'NONE', #14533 ) ;
#8709=CYLINDRICAL_SURFACE ( 'NONE', #11204, 25.39999999999999858 ) ;
#8714=ADVANCED_FACE ( 'NONE', ( #34693, #41050, #9236, #66867, #14181 ), #46011, .T. ) ;
#8720=DIRECTION ( 'NONE',  ( 1.000000000000000000, -0.000000000000000000, 0.000000000000000000 ) ) ;
#8723=CARTESIAN_POINT ( 'NONE',  ( 39.00000000000000000, 14.08845687959340331, 21.00000000000000000 ) ) ;
#8727=CARTESIAN_POINT ( 'NONE',  ( 29.89999999999999858, -14.06939075806900874, 20.80000000000001137 ) ) ;
#8732=CARTESIAN_POINT ( 'NONE',  ( 48.50000000000000000, 0.000000000000000000, 0.000000000000000000 ) ) ;
#8738=DIRECTION ( 'NONE',  ( -1.000000000000000000, 0.000000000000000000, 0.000000000000000000 ) ) ;
#8746=CARTESIAN_POINT ( 'NONE',  ( 10.00000000000000000, -18.00000000000000355, 21.00000000000000000 ) ) ;
#8752=CARTESIAN_POINT ( 'NONE',  ( 8.900000000000005684, -0.1999999999911795112, 8.826273045769999343E-12 ) ) ;
#8755=ORIENTED_EDGE ( 'NONE', *, *, #39297, .T. ) ;
#8757=FACE_OUTER_BOUND ( 'NONE', #45641, .T. ) ;
#8760=CIRCLE ( 'NONE', #35870, 5.000000000000000000 ) ;
#8779=DIRECTION ( 'NONE',  ( 1.000000000000000000, -0.000000000000000000, 0.000000000000000000 ) ) ;
#8784=CARTESIAN_POINT ( 'NONE',  ( 39.00000000000000000, 21.00000000000000000, 13.98999642601811999 ) ) ;
#8785=ORIENTED_EDGE ( 'NONE', *, *, #47251, .F. ) ;
#8789=CARTESIAN_POINT ( 'NONE',  ( 10.00000000000000000, 18.00000000000000355, 21.00000000000000000 ) ) ;
#8792=EDGE_CURVE ( 'NONE', #4531, #32705, #56734, .T. ) ;
#8793=CARTESIAN_POINT ( 'NONE',  ( 41.09999999999999432, 13.66939075806899950, -20.80000000000000426 ) ) ;
#8798=PLANE ( 'NONE',  #9812 ) ;
#8823=CARTESIAN_POINT ( 'NONE',  ( 41.09999999999999432, 13.66939075806899950, 20.80000000000000426 ) ) ;
#8824=VECTOR ( 'NONE', #9747, 1000.000000000000114 ) ;
#8837=DIRECTION ( 'NONE',  ( 0.000000000000000000, 0.000000000000000000, 1.000000000000000000 ) ) ;
#8842=ADVANCED_FACE ( 'NONE', ( #26903 ), #30, .T. ) ;
#8845=DIRECTION ( 'NONE',  ( -1.000000000000000000, 0.000000000000000000, 0.000000000000000000 ) ) ;
#8847=ORIENTED_EDGE ( 'NONE', *, *, #13767, .T. ) ;
#8856=DIRECTION ( 'NONE',  ( 1.000000000000000000, -0.000000000000000000, 0.000000000000000000 ) ) ;
#8872=EDGE_LOOP ( 'NONE', ( #29556, #69671 ) ) ;
#8882=EDGE_CURVE ( 'NONE', #12, #31689, #15243, .T. ) ;
#8888=CARTESIAN_POINT ( 'NONE',  ( 49.00000000000000000, -14.06939075806900163, -20.80000000000000426 ) ) ;
#8891=CARTESIAN_POINT ( 'NONE',  ( 7.900000000000003908, -21.00000000000000000, -18.00000000000000355 ) ) ;
#8904=DIRECTION ( 'NONE',  ( 0.000000000000000000, 0.000000000000000000, -1.000000000000000000 ) ) ;
#8907=CARTESIAN_POINT ( 'NONE',  ( 21.90000000000000213, -0.1999999999911795112, 8.826273045769999343E-12 ) ) ;
#8908=AXIS2_PLACEMENT_3D ( 'NONE', #64437, #53485, #42515 ) ;
#8912=ORIENTED_EDGE ( 'NONE', *, *, #29764, .F. ) ;
#8926=ORIENTED_EDGE ( 'NONE', *, *, #40367, .F. ) ;
#8928=CIRCLE ( 'NONE', #48464, 24.99999999998789946 ) ;
#8932=CARTESIAN_POINT ( 'NONE',  ( 29.89999999999999858, -0.000000000000000000, 20.80000000000000426 ) ) ;
#8934=AXIS2_PLACEMENT_3D ( 'NONE', #29070, #7832, #50981 ) ;
#8940=EDGE_LOOP ( 'NONE', ( #42303, #22298, #38215, #34282 ) ) ;
#8950=VERTEX_POINT ( 'NONE', #32556 ) ;
#8958=LINE ( 'NONE', #52105, #23244 ) ;
#8960=AXIS2_PLACEMENT_3D ( 'NONE', #12219, #39104, #54685 ) ;
#8964=DIRECTION ( 'NONE',  ( 0.000000000000000000, -1.000000000000000000, 0.000000000000000000 ) ) ;
#8965=EDGE_CURVE ( 'NONE', #29539, #8221, #27247, .T. ) ;
#8973=DIRECTION ( 'NONE',  ( 0.000000000000000000, -1.000000000000000000, 0.000000000000000000 ) ) ;
#8980=AXIS2_PLACEMENT_3D ( 'NONE', #63100, #47875, #14658 ) ;
#8990=DIRECTION ( 'NONE',  ( 1.000000000000000000, 0.000000000000000000, 0.000000000000000000 ) ) ;
#8992=ORIENTED_EDGE ( 'NONE', *, *, #22597, .F. ) ;
#8994=CYLINDRICAL_SURFACE ( 'NONE', #49615, 24.99999999998784972 ) ;
#8996=DIRECTION ( 'NONE',  ( 0.000000000000000000, 0.000000000000000000, 1.000000000000000000 ) ) ;
#9013=FACE_OUTER_BOUND ( 'NONE', #56048, .T. ) ;
#9015=LINE ( 'NONE', #47218, #17245 ) ;
#9020=EDGE_CURVE ( 'NONE', #34472, #57523, #44513, .T. ) ;
#9026=EDGE_LOOP ( 'NONE', ( #11233, #50337, #64364, #59153 ) ) ;
#9027=DIRECTION ( 'NONE',  ( 0.000000000000000000, 0.000000000000000000, -1.000000000000000000 ) ) ;
#9031=CYLINDRICAL_SURFACE ( 'NONE', #48358, 2.458500000000000796 ) ;
#9036=EDGE_CURVE ( 'NONE', #36263, #22451, #66087, .T. ) ;
#9038=DIRECTION ( 'NONE',  ( -0.7071067811865476838, 0.4999999999999997780, 0.4999999999999997780 ) ) ;
#9045=ORIENTED_EDGE ( 'NONE', *, *, #1620, .F. ) ;
#9047=CARTESIAN_POINT ( 'NONE',  ( 41.09999999999999432, -21.00000000000000000, 13.86939075806900057 ) ) ;
#9049=CARTESIAN_POINT ( 'NONE',  ( 41.09999999999999432, -21.00000000000000000, 13.86939075806900057 ) ) ;
#9063=VECTOR ( 'NONE', #39227, 1000.000000000000000 ) ;
#9067=( LENGTH_UNIT ( ) NAMED_UNIT ( * ) SI_UNIT ( .MILLI., .METRE. ) );
#9077=LINE ( 'NONE', #57858, #9402 ) ;
#9085=VECTOR ( 'NONE', #1084, 1000.000000000000000 ) ;
#9089=EDGE_LOOP ( 'NONE', ( #63569, #68005, #55821, #3683, #38319, #32559, #62038, #14291 ) ) ;
#9112=DIRECTION ( 'NONE',  ( 0.000000000000000000, -1.000000000000000000, 0.000000000000000000 ) ) ;
#9116=LINE ( 'NONE', #13712, #45246 ) ;
#9120=FACE_OUTER_BOUND ( 'NONE', #46597, .T. ) ;
#9127=DIRECTION ( 'NONE',  ( 0.000000000000000000, 0.000000000000000000, -1.000000000000000000 ) ) ;
#9130=DIRECTION ( 'NONE',  ( 0.000000000000000000, 0.000000000000000000, -1.000000000000000000 ) ) ;
#9131=ORIENTED_EDGE ( 'NONE', *, *, #14840, .T. ) ;
#9148=DIRECTION ( 'NONE',  ( 1.000000000000000000, 0.000000000000000000, 0.000000000000000000 ) ) ;
#9153=EDGE_CURVE ( 'NONE', #42535, #59658, #7381, .T. ) ;
#9175=CARTESIAN_POINT ( 'NONE',  ( 41.09999999999999432, -0.2000000000000000111, 0.000000000000000000 ) ) ;
#9181=EDGE_LOOP ( 'NONE', ( #21172, #51234, #3717, #13637 ) ) ;
#9182=CARTESIAN_POINT ( 'NONE',  ( 13.90000000000000213, -0.1999999999911795112, 8.826273045769999343E-12 ) ) ;
#9197=ADVANCED_FACE ( 'NONE', ( #51586 ), #3151, .F. ) ;
#9199=VECTOR ( 'NONE', #64495, 1000.000000000000114 ) ;
#9217=CARTESIAN_POINT ( 'NONE',  ( 15.89999999999999680, 13.66939075806899240, 20.79999999999999361 ) ) ;
#9222=EDGE_LOOP ( 'NONE', ( #13000, #12226, #32531, #57985 ) ) ;
#9236=FACE_BOUND ( 'NONE', #3148, .T. ) ;
#9243=DIRECTION ( 'NONE',  ( 1.000000000000000000, -0.000000000000000000, 0.000000000000000000 ) ) ;
#9246=VERTEX_POINT ( 'NONE', #42715 ) ;
#9250=CYLINDRICAL_SURFACE ( 'NONE', #49889, 2.458500000000000796 ) ;
#9255=APPLICATION_CONTEXT ( 'automotive_design' ) ;
#9258=LINE ( 'NONE', #30818, #59755 ) ;
#9267=CARTESIAN_POINT ( 'NONE',  ( 25.90000000000000213, 20.60000000000000142, 13.86939075806899702 ) ) ;
#9270=PLANE ( 'NONE',  #36859 ) ;
#9282=DIRECTION ( 'NONE',  ( -1.000000000000000000, 0.000000000000000000, 0.000000000000000000 ) ) ;
#9296=AXIS2_PLACEMENT_3D ( 'NONE', #9175, #25440, #16580 ) ;
#9300=ORIENTED_EDGE ( 'NONE', *, *, #14781, .T. ) ;
#9304=CYLINDRICAL_SURFACE ( 'NONE', #55922, 24.99999999998794920 ) ;
#9317=AXIS2_PLACEMENT_3D ( 'NONE', #41964, #47618, #31006 ) ;
#9322=DIRECTION ( 'NONE',  ( 1.000000000000000000, -0.000000000000000000, 0.000000000000000000 ) ) ;
#9323=ORIENTED_EDGE ( 'NONE', *, *, #27139, .T. ) ;
#9333=CARTESIAN_POINT ( 'NONE',  ( 39.00000000000000000, 21.00000000000000000, -16.96999999999999886 ) ) ;
#9335=DIRECTION ( 'NONE',  ( 0.000000000000000000, 0.000000000000000000, -1.000000000000000000 ) ) ;
#9337=VERTEX_POINT ( 'NONE', #6620 ) ;
#9341=( LENGTH_UNIT ( ) NAMED_UNIT ( * ) SI_UNIT ( .MILLI., .METRE. ) );
#9350=DIRECTION ( 'NONE',  ( 0.000000000000000000, -0.8320000000000487006, -0.5547756303226729635 ) ) ;
#9352=DIRECTION ( 'NONE',  ( 0.000000000000000000, 0.000000000000000000, -1.000000000000000000 ) ) ;
#9374=CARTESIAN_POINT ( 'NONE',  ( 40.90000000000000568, 21.00000000000000000, 16.96999999999999886 ) ) ;
#9376=EDGE_CURVE ( 'NONE', #20422, #61702, #14421, .T. ) ;
#9380=ORIENTED_EDGE ( 'NONE', *, *, #45389, .F. ) ;
#9384=CARTESIAN_POINT ( 'NONE',  ( 34.89999999999999858, -21.00000000000000000, 13.86939075806900057 ) ) ;
#9389=CARTESIAN_POINT ( 'NONE',  ( 10.90000000000000036, 20.60000000000000142, -13.86939075806900057 ) ) ;
#9396=ORIENTED_EDGE ( 'NONE', *, *, #64847, .F. ) ;
#9402=VECTOR ( 'NONE', #30644, 1000.000000000000000 ) ;
#9408=CYLINDRICAL_SURFACE ( 'NONE', #60653, 24.99999999998794920 ) ;
#9411=VECTOR ( 'NONE', #63023, 1000.000000000000000 ) ;
#9412=ADVANCED_FACE ( 'NONE', ( #66002 ), #37768, .F. ) ;
#9416=ORIENTED_EDGE ( 'NONE', *, *, #64770, .F. ) ;
#9435=PLANE ( 'NONE',  #39798 ) ;
#9438=CYLINDRICAL_SURFACE ( 'NONE', #9317, 25.39999999999999858 ) ;
#9441=AXIS2_PLACEMENT_3D ( 'NONE', #41485, #56343, #7887 ) ;
#9457=EDGE_CURVE ( 'NONE', #40436, #56320, #12944, .T. ) ;
#9458=LINE ( 'NONE', #15115, #38991 ) ;
#9462=DIRECTION ( 'NONE',  ( 1.000000000000000000, -0.000000000000000000, 0.000000000000000000 ) ) ;
#9470=ORIENTED_EDGE ( 'NONE', *, *, #3218, .T. ) ;
#9479=DIRECTION ( 'NONE',  ( 0.000000000000000000, 1.000000000000000000, 0.000000000000000000 ) ) ;
#9494=ORIENTED_EDGE ( 'NONE', *, *, #29710, .T. ) ;
#9510=AXIS2_PLACEMENT_3D ( 'NONE', #37227, #53154, #4695 ) ;
#9511=CARTESIAN_POINT ( 'NONE',  ( 41.09999999999999432, 13.66939075806899950, -20.80000000000000426 ) ) ;
#9515=FACE_OUTER_BOUND ( 'NONE', #41752, .T. ) ;
#9521=FILL_AREA_STYLE_COLOUR ( '', #50374 ) ;
#9522=DIRECTION ( 'NONE',  ( 0.000000000000000000, 0.000000000000000000, -1.000000000000000000 ) ) ;
#9525=CARTESIAN_POINT ( 'NONE',  ( -6.661338147750939243E-15, -20.50000000000000000, 17.79289321881346808 ) ) ;
#9526=EDGE_CURVE ( 'NONE', #49662, #34559, #8928, .T. ) ;
#9536=ADVANCED_FACE ( 'NONE', ( #23568 ), #8709, .F. ) ;
#9539=FACE_OUTER_BOUND ( 'NONE', #16889, .T. ) ;
#9553=AXIS2_PLACEMENT_3D ( 'NONE', #57294, #46329, #63305 ) ;
#9562=DIRECTION ( 'NONE',  ( -1.000000000000000000, 0.000000000000000000, 0.000000000000000000 ) ) ;
#9564=CARTESIAN_POINT ( 'NONE',  ( 29.89999999999999858, -21.00000000000000000, 13.86939075806900057 ) ) ;
#9571=ORIENTED_EDGE ( 'NONE', *, *, #36542, .F. ) ;
#9585=DIRECTION ( 'NONE',  ( 0.000000000000000000, 0.7071067811865475727, -0.7071067811865475727 ) ) ;
#9586=ORIENTED_EDGE ( 'NONE', *, *, #385, .F. ) ;
#9608=CARTESIAN_POINT ( 'NONE',  ( 16.89999999999999858, 13.66939075806899240, 20.79999999999999361 ) ) ;
#9615=CARTESIAN_POINT ( 'NONE',  ( 13.90000000000000213, 13.66939075806899240, 20.79999999999999361 ) ) ;
#9623=EDGE_LOOP ( 'NONE', ( #49197, #33738, #24529, #42065, #41156, #21144, #46090, #61890 ) ) ;
#9625=CARTESIAN_POINT ( 'NONE',  ( 19.90000000000000213, 20.60000000000000142, -13.86939075806900057 ) ) ;
#9634=AXIS2_PLACEMENT_3D ( 'NONE', #16416, #37990, #53218 ) ;
#9635=FACE_OUTER_BOUND ( 'NONE', #21895, .T. ) ;
#9642=ORIENTED_EDGE ( 'NONE', *, *, #4244, .T. ) ;
#9649=DIRECTION ( 'NONE',  ( 0.000000000000000000, 0.000000000000000000, 1.000000000000000000 ) ) ;
#9654=CARTESIAN_POINT ( 'NONE',  ( 31.89999999999999858, 0.000000000000000000, 2.585923194002694273E-15 ) ) ;
#9655=LINE ( 'NONE', #31921, #24427 ) ;
#9657=ORIENTED_EDGE ( 'NONE', *, *, #12767, .T. ) ;
#9666=CARTESIAN_POINT ( 'NONE',  ( 9.899999999999998579, -0.2000000000000000111, 0.000000000000000000 ) ) ;
#9669=ORIENTED_EDGE ( 'NONE', *, *, #59209, .T. ) ;
#9679=VERTEX_POINT ( 'NONE', #31611 ) ;
#9683=CARTESIAN_POINT ( 'NONE',  ( 55.00000000000000000, 0.000000000000000000, 0.000000000000000000 ) ) ;
#9690=CARTESIAN_POINT ( 'NONE',  ( 9.900000000000000355, -0.000000000000000000, 20.80000000000000426 ) ) ;
#9707=AXIS2_PLACEMENT_3D ( 'NONE', #50242, #50597, #13458 ) ;
#9715=CARTESIAN_POINT ( 'NONE',  ( 41.09999999999999432, -14.06939075806901940, -20.80000000000000426 ) ) ;
#9733=MECHANICAL_DESIGN_GEOMETRIC_PRESENTATION_REPRESENTATION('',(#53749),#23227);
#9741=ORIENTED_EDGE ( 'NONE', *, *, #48472, .T. ) ;
#9743=CIRCLE ( 'NONE', #14277, 24.99999999998784972 ) ;
#9747=DIRECTION ( 'NONE',  ( 0.000000000000000000, 0.7071067811865474617, -0.7071067811865474617 ) ) ;
#9748=VECTOR ( 'NONE', #45247, 1000.000000000000000 ) ;
#9766=PLANE ( 'NONE',  #33420 ) ;
#9793=ORIENTED_EDGE ( 'NONE', *, *, #60442, .T. ) ;
#9794=DIRECTION ( 'NONE',  ( 1.000000000000000000, -0.000000000000000000, 0.000000000000000000 ) ) ;
#9796=CARTESIAN_POINT ( 'NONE',  ( 37.90000000000000568, -0.2000000000089119934, 8.909539772616881237E-12 ) ) ;
#9808=VERTEX_POINT ( 'NONE', #23414 ) ;
#9812=AXIS2_PLACEMENT_3D ( 'NONE', #62177, #8078, #3499 ) ;
#9815=FACE_OUTER_BOUND ( 'NONE', #50868, .T. ) ;
#9821=ORIENTED_EDGE ( 'NONE', *, *, #5310, .T. ) ;
#9825=CARTESIAN_POINT ( 'NONE',  ( 39.90000000000000568, -16.96999999999999886, -21.00000000000000000 ) ) ;
#9833=CIRCLE ( 'NONE', #33488, 24.99999999998794920 ) ;
#9841=CIRCLE ( 'NONE', #58226, 0.5000000000000000000 ) ;
#9846=EDGE_CURVE ( 'NONE', #45732, #37491, #33334, .T. ) ;
#9860=ORIENTED_EDGE ( 'NONE', *, *, #37274, .T. ) ;
#9871=EDGE_LOOP ( 'NONE', ( #9741, #21259, #52185, #9416 ) ) ;
#9872=DIRECTION ( 'NONE',  ( 0.000000000000000000, 0.000000000000000000, 1.000000000000000000 ) ) ;
#9874=DIRECTION ( 'NONE',  ( -0.7071067811865472397, 0.5000000000000002220, 0.5000000000000002220 ) ) ;
#9887=VECTOR ( 'NONE', #56732, 1000.000000000000000 ) ;
#9891=EDGE_LOOP ( 'NONE', ( #49428, #67009, #7394, #41708, #69975, #41034, #22385, #16285 ) ) ;
#9892=DIRECTION ( 'NONE',  ( 1.000000000000000000, 0.000000000000000000, 0.000000000000000000 ) ) ;
#9895=ORIENTED_EDGE ( 'NONE', *, *, #66531, .F. ) ;
#9904=VERTEX_POINT ( 'NONE', #56965 ) ;
#9907=PLANE ( 'NONE',  #11485 ) ;
#9910=DIRECTION ( 'NONE',  ( 0.000000000000000000, 0.000000000000000000, 1.000000000000000000 ) ) ;
#9916=VERTEX_POINT ( 'NONE', #13135 ) ;
#9949=ORIENTED_EDGE ( 'NONE', *, *, #20405, .T. ) ;
#9963=DIRECTION ( 'NONE',  ( 1.000000000000000000, 0.000000000000000000, 0.000000000000000000 ) ) ;
#9964=CARTESIAN_POINT ( 'NONE',  ( 9.900000000000000355, 18.00000000000000355, -21.00000000000000000 ) ) ;
#9965=EDGE_CURVE ( 'NONE', #20590, #57421, #47477, .T. ) ;
#9968=CARTESIAN_POINT ( 'NONE',  ( 41.09999999999999432, -14.06939075806900163, 20.80000000000000426 ) ) ;
#9969=EDGE_CURVE ( 'NONE', #44485, #57134, #61928, .T. ) ;
#9980=CARTESIAN_POINT ( 'NONE',  ( 39.00000000000000000, -14.48845687959340012, 21.00000000000000000 ) ) ;
#9988=FACE_BOUND ( 'NONE', #12041, .T. ) ;
#9991=DIRECTION ( 'NONE',  ( 1.000000000000000000, -0.000000000000000000, 0.000000000000000000 ) ) ;
#10007=CARTESIAN_POINT ( 'NONE',  ( 40.90000000000000568, 14.08845687959340154, 20.99999999999999645 ) ) ;
#10030=EDGE_LOOP ( 'NONE', ( #16161, #8483, #29888, #49608 ) ) ;
#10033=DIRECTION ( 'NONE',  ( -1.000000000000000000, 0.000000000000000000, 0.000000000000000000 ) ) ;
#10037=FACE_OUTER_BOUND ( 'NONE', #11030, .T. ) ;
#10050=EDGE_CURVE ( 'NONE', #33306, #66802, #48829, .T. ) ;
#10065=DIRECTION ( 'NONE',  ( -1.000000000000000000, 0.000000000000000000, 0.000000000000000000 ) ) ;
#10071=DIRECTION ( 'NONE',  ( 1.000000000000000000, -0.000000000000000000, 0.000000000000000000 ) ) ;
#10072=DIRECTION ( 'NONE',  ( -1.000000000000000000, 0.000000000000000000, 0.000000000000000000 ) ) ;
#10074=ORIENTED_EDGE ( 'NONE', *, *, #8533, .T. ) ;
#10080=DIRECTION ( 'NONE',  ( 0.000000000000000000, -0.7071067811865474617, -0.7071067811865474617 ) ) ;
#10081=ORIENTED_EDGE ( 'NONE', *, *, #5160, .F. ) ;
#10084=ADVANCED_FACE ( 'NONE', ( #31872 ), #5694, .F. ) ;
#10085=ORIENTED_EDGE ( 'NONE', *, *, #43239, .T. ) ;
#10089=ORIENTED_EDGE ( 'NONE', *, *, #60608, .F. ) ;
#10092=CARTESIAN_POINT ( 'NONE',  ( 37.90000000000000568, -0.000000000000000000, 20.80000000000000426 ) ) ;
#10093=AXIS2_PLACEMENT_3D ( 'NONE', #13185, #19536, #30502 ) ;
#10112=ORIENTED_EDGE ( 'NONE', *, *, #37162, .F. ) ;
#10116=CARTESIAN_POINT ( 'NONE',  ( 25.57999999999999829, 0.000000000000000000, 2.458500000000000796 ) ) ;
#10117=VERTEX_POINT ( 'NONE', #4312 ) ;
#10118=DIRECTION ( 'NONE',  ( 1.000000000000000000, -0.000000000000000000, 0.000000000000000000 ) ) ;
#10147=PLANE ( 'NONE',  #61482 ) ;
#10148=CARTESIAN_POINT ( 'NONE',  ( 26.90000000000000213, -14.06939075806900874, 20.80000000000001137 ) ) ;
#10155=PLANE ( 'NONE',  #49503 ) ;
#10175=LINE ( 'NONE', #69222, #51426 ) ;
#10189=DIRECTION ( 'NONE',  ( 1.000000000000000000, -0.000000000000000000, 0.000000000000000000 ) ) ;
#10199=VECTOR ( 'NONE', #7901, 1000.000000000000000 ) ;
#10202=FILL_AREA_STYLE_COLOUR ( '', #5302 ) ;
#10204=SURFACE_STYLE_FILL_AREA ( #10899 ) ;
#10210=CIRCLE ( 'NONE', #19237, 24.99999999998784972 ) ;
#10214=EDGE_CURVE ( 'NONE', #32725, #66079, #34262, .T. ) ;
#10216=ORIENTED_EDGE ( 'NONE', *, *, #2106, .T. ) ;
#10232=DIRECTION ( 'NONE',  ( 0.000000000000000000, 1.000000000000000000, -0.000000000000000000 ) ) ;
#10234=DIRECTION ( 'NONE',  ( -1.000000000000000000, 0.000000000000000000, 0.000000000000000000 ) ) ;
#10253=CYLINDRICAL_SURFACE ( 'NONE', #27363, 24.99999999998784972 ) ;
#10260=CARTESIAN_POINT ( 'NONE',  ( 32.89999999999999858, 13.66939075806899240, -20.79999999999999361 ) ) ;
#10261=ADVANCED_FACE ( 'NONE', ( #738 ), #55509, .F. ) ;
#10265=VECTOR ( 'NONE', #54051, 1000.000000000000000 ) ;
#10275=EDGE_CURVE ( 'NONE', #22897, #21838, #38890, .T. ) ;
#10276=LINE ( 'NONE', #10614, #57500 ) ;
#10279=DIRECTION ( 'NONE',  ( 1.000000000000000000, 0.000000000000000000, 0.000000000000000000 ) ) ;
#10287=STYLED_ITEM ( 'NONE', ( #2877 ), #42462 ) ;
#10299=CARTESIAN_POINT ( 'NONE',  ( 37.90000000000000568, 13.66939075806899240, 20.79999999999999361 ) ) ;
#10312=DIRECTION ( 'NONE',  ( 0.000000000000000000, -1.000000000000000000, 0.000000000000000000 ) ) ;
#10316=LINE ( 'NONE', #63718, #28342 ) ;
#10318=LINE ( 'NONE', #9980, #19930 ) ;
#10327=ORIENTED_EDGE ( 'NONE', *, *, #49198, .F. ) ;
#10338=AXIS2_PLACEMENT_3D ( 'NONE', #41508, #19585, #14295 ) ;
#10356=CLOSED_SHELL ( 'NONE', ( #60776, #47861, #55838, #13903, #29892, #53287, #10385, #25898, #26098, #27068 ) ) ;
#10364=ORIENTED_EDGE ( 'NONE', *, *, #11148, .T. ) ;
#10365=ORIENTED_EDGE ( 'NONE', *, *, #10050, .F. ) ;
#10371=ORIENTED_EDGE ( 'NONE', *, *, #12455, .F. ) ;
#10373=LINE ( 'NONE', #65504, #654 ) ;
#10379=ORIENTED_EDGE ( 'NONE', *, *, #1370, .T. ) ;
#10385=ADVANCED_FACE ( 'NONE', ( #24370 ), #2449, .T. ) ;
#10398=EDGE_CURVE ( 'NONE', #58826, #43972, #58307, .T. ) ;
#10416=LINE ( 'NONE', #53557, #46972 ) ;
#10438=EDGE_LOOP ( 'NONE', ( #15431, #69587, #10085, #49110, #25816, #61554, #12671, #54765 ) ) ;
#10445=ORIENTED_EDGE ( 'NONE', *, *, #66823, .T. ) ;
#10446=LINE ( 'NONE', #15755, #63211 ) ;
#10447=CARTESIAN_POINT ( 'NONE',  ( 0.5000000000000000000, 21.00000000000000000, -18.00000000000000355 ) ) ;
#10458=LINE ( 'NONE', #10116, #60899 ) ;
#10462=FILL_AREA_STYLE ('',( #21419 ) ) ;
#10463=CARTESIAN_POINT ( 'NONE',  ( 23.90000000000000213, 0.000000000000000000, 1.723948796001796511E-15 ) ) ;
#10469=EDGE_CURVE ( 'NONE', #64055, #62485, #14818, .T. ) ;
#10474=CARTESIAN_POINT ( 'NONE',  ( 13.90000000000000213, -0.1999999999911430404, -8.864436962241481021E-12 ) ) ;
#10477=AXIS2_PLACEMENT_3D ( 'NONE', #8356, #3081, #63872 ) ;
#10480=EDGE_CURVE ( 'NONE', #24611, #39384, #5264, .T. ) ;
#10482=CYLINDRICAL_SURFACE ( 'NONE', #21361, 24.99999999998784972 ) ;
#10489=PLANE ( 'NONE',  #48102 ) ;
#10490=CARTESIAN_POINT ( 'NONE',  ( 55.00000000000000000, -0.1999999999911795112, 8.826273045769999343E-12 ) ) ;
#10496=CYLINDRICAL_SURFACE ( 'NONE', #67708, 24.99999999998789946 ) ;
#10510=DIRECTION ( 'NONE',  ( 1.000000000000000000, -0.000000000000000000, 0.000000000000000000 ) ) ;
#10513=ADVANCED_FACE ( 'NONE', ( #47688 ), #69255, .T. ) ;
#10518=DIRECTION ( 'NONE',  ( 0.000000000000000000, 0.000000000000000000, 1.000000000000000000 ) ) ;
#10522=VERTEX_POINT ( 'NONE', #15172 ) ;
#10530=CARTESIAN_POINT ( 'NONE',  ( 25.57999999999999829, 6.429395695523604153E-16, -5.250000000000000000 ) ) ;
#10537=FACE_OUTER_BOUND ( 'NONE', #40215, .T. ) ;
#10543=EDGE_CURVE ( 'NONE', #13405, #30457, #28659, .T. ) ;
#10547=ORIENTED_EDGE ( 'NONE', *, *, #29465, .T. ) ;
#10548=ORIENTED_EDGE ( 'NONE', *, *, #46218, .T. ) ;
#10550=CARTESIAN_POINT ( 'NONE',  ( 40.90000000000000568, 21.00000000000000000, -16.96999999999999886 ) ) ;
#10558=VERTEX_POINT ( 'NONE', #64998 ) ;
#10561=DIRECTION ( 'NONE',  ( 0.000000000000000000, 0.000000000000000000, -1.000000000000000000 ) ) ;
#10565=FILL_AREA_STYLE ('',( #59006 ) ) ;
#10571=DIRECTION ( 'NONE',  ( 0.000000000000000000, 0.000000000000000000, -1.000000000000000000 ) ) ;
#10573=EDGE_LOOP ( 'NONE', ( #66684, #35800, #43769, #46663, #25940, #59232, #19418, #44591 ) ) ;
#10580=EDGE_LOOP ( 'NONE', ( #69419, #36798 ) ) ;
#10582=CARTESIAN_POINT ( 'NONE',  ( 37.90000000000000568, -0.2000000000089119934, -8.913009219568841313E-12 ) ) ;
#10593=VERTEX_POINT ( 'NONE', #38138 ) ;
#10595=DIRECTION ( 'NONE',  ( 0.000000000000000000, -0.7071067811865475727, 0.7071067811865475727 ) ) ;
#10604=VECTOR ( 'NONE', #53911, 1000.000000000000000 ) ;
#10607=CARTESIAN_POINT ( 'NONE',  ( 47.00000000000000000, 0.7500000000000000000, -4.943429983321300014 ) ) ;
#10611=CIRCLE ( 'NONE', #34299, 24.99999999998784972 ) ;
#10614=CARTESIAN_POINT ( 'NONE',  ( 20.90000000000000213, -14.06939075806900163, -20.80000000000000426 ) ) ;
#10619=ORIENTED_EDGE ( 'NONE', *, *, #51588, .T. ) ;
#10620=VERTEX_POINT ( 'NONE', #1331 ) ;
#10621=DIRECTION ( 'NONE',  ( -1.000000000000000000, 0.000000000000000000, 0.000000000000000000 ) ) ;
#10626=CARTESIAN_POINT ( 'NONE',  ( 41.09999999999999432, 20.60000000000000142, -13.86939075806900057 ) ) ;
#10627=CARTESIAN_POINT ( 'NONE',  ( 14.89999999999999680, 20.60000000000000142, -13.86939075806900057 ) ) ;
#10631=ORIENTED_EDGE ( 'NONE', *, *, #3204, .T. ) ;
#10651=CARTESIAN_POINT ( 'NONE',  ( 8.900000000000005684, 21.00000000000000355, -13.98999642601812354 ) ) ;
#10652=VECTOR ( 'NONE', #4622, 1000.000000000000000 ) ;
#10654=AXIS2_PLACEMENT_3D ( 'NONE', #52849, #31282, #24900 ) ;
#10665=EDGE_CURVE ( 'NONE', #45716, #44206, #60718, .T. ) ;
#10676=VERTEX_POINT ( 'NONE', #43415 ) ;
#10680=ORIENTED_EDGE ( 'NONE', *, *, #10543, .T. ) ;
#10685=DIRECTION ( 'NONE',  ( 0.000000000000000000, 0.000000000000000000, -1.000000000000000000 ) ) ;
#10693=VERTEX_POINT ( 'NONE', #28534 ) ;
#10730=VERTEX_POINT ( 'NONE', #51861 ) ;
#10736=DIRECTION ( 'NONE',  ( -1.000000000000000000, 0.000000000000000000, 0.000000000000000000 ) ) ;
#10754=CARTESIAN_POINT ( 'NONE',  ( 38.90000000000000568, -0.2000000000089119934, 8.909539772616881237E-12 ) ) ;
#10757=EDGE_LOOP ( 'NONE', ( #44146, #28883, #64648, #58472 ) ) ;
#10760=COLOUR_RGB ( '', 0.31764706, 0.68627451, 0.89019608) ;
#10765=( GEOMETRIC_REPRESENTATION_CONTEXT ( 3 ) GLOBAL_UNCERTAINTY_ASSIGNED_CONTEXT ( ( #47238 ) ) GLOBAL_UNIT_ASSIGNED_CONTEXT ( ( #41232, #62440, #35943 ) ) REPRESENTATION_CONTEXT ( 'NONE', 'WORKASPACE' ) );
#10768=ORIENTED_EDGE ( 'NONE', *, *, #62259, .T. ) ;
#10772=DIRECTION ( 'NONE',  ( 0.000000000000000000, 0.000000000000000000, 1.000000000000000000 ) ) ;
#10773=EDGE_CURVE ( 'NONE', #13118, #9808, #19322, .T. ) ;
#10779=VERTEX_POINT ( 'NONE', #2021 ) ;
#10782=EDGE_LOOP ( 'NONE', ( #38869, #34834, #58546, #50138 ) ) ;
#10784=ORIENTED_EDGE ( 'NONE', *, *, #8487, .F. ) ;
#10789=ORIENTED_EDGE ( 'NONE', *, *, #33995, .F. ) ;
#10791=VECTOR ( 'NONE', #55743, 1000.000000000000000 ) ;
#10793=VECTOR ( 'NONE', #50083, 1000.000000000000114 ) ;
#10802=EDGE_CURVE ( 'NONE', #33525, #22414, #40537, .T. ) ;
#10809=STYLED_ITEM ( 'NONE', ( #42055 ), #44878 ) ;
#10815=CARTESIAN_POINT ( 'NONE',  ( 22.90000000000000213, -0.1999999999911795112, 8.826273045769999343E-12 ) ) ;
#10825=PLANE ( 'NONE',  #4463 ) ;
#10832=CARTESIAN_POINT ( 'NONE',  ( 31.89999999999999858, -0.000000000000000000, 20.80000000000000426 ) ) ;
#10865=ORIENTED_EDGE ( 'NONE', *, *, #16767, .T. ) ;
#10871=EDGE_LOOP ( 'NONE', ( #17376, #64731, #15028, #3104, #69163, #19201, #23693, #42706 ) ) ;
#10880=DIRECTION ( 'NONE',  ( -1.000000000000000000, 0.000000000000000000, 0.000000000000000000 ) ) ;
#10899=FILL_AREA_STYLE ('',( #58302 ) ) ;
#10901=ORIENTED_EDGE ( 'NONE', *, *, #5072, .F. ) ;
#10902=DIRECTION ( 'NONE',  ( -1.000000000000000000, 0.000000000000000000, 0.000000000000000000 ) ) ;
#10907=CARTESIAN_POINT ( 'NONE',  ( 8.900000000000002132, 0.000000000000000000, 0.000000000000000000 ) ) ;
#10908=AXIS2_PLACEMENT_3D ( 'NONE', #22628, #33235, #45214 ) ;
#10921=FACE_BOUND ( 'NONE', #21806, .T. ) ;
#10930=CARTESIAN_POINT ( 'NONE',  ( 40.90000000000000568, -14.06939075806900163, -20.80000000000000426 ) ) ;
#10932=ORIENTED_EDGE ( 'NONE', *, *, #57568, .F. ) ;
#10934=CARTESIAN_POINT ( 'NONE',  ( 0.000000000000000000, -0.7500000000000000000, 0.000000000000000000 ) ) ;
#10940=CARTESIAN_POINT ( 'NONE',  ( 49.00000000000000000, -0.2000000000089119934, -8.913009219568841313E-12 ) ) ;
#10945=ORIENTED_EDGE ( 'NONE', *, *, #53930, .F. ) ;
#10946=CARTESIAN_POINT ( 'NONE',  ( 46.39999999999999858, 33.00000000000000000, 2.750000000000000444 ) ) ;
#10952=CARTESIAN_POINT ( 'NONE',  ( 41.09999999999999432, -14.06939075806901940, -20.80000000000000426 ) ) ;
#10956=CARTESIAN_POINT ( 'NONE',  ( 39.90000000000000568, 6.123233995736766282E-16, -5.000000000000000000 ) ) ;
#10977=LINE ( 'NONE', #32553, #54926 ) ;
#10979=ORIENTED_EDGE ( 'NONE', *, *, #44899, .F. ) ;
#10986=AXIS2_PLACEMENT_3D ( 'NONE', #68218, #30035, #51961 ) ;
#10990=ORIENTED_EDGE ( 'NONE', *, *, #6094, .F. ) ;
#11005=VERTEX_POINT ( 'NONE', #13906 ) ;
#11017=DIRECTION ( 'NONE',  ( 0.000000000000000000, 1.000000000000000000, 0.000000000000000000 ) ) ;
#11030=EDGE_LOOP ( 'NONE', ( #45869, #2636, #26206, #66511 ) ) ;
#11032=VERTEX_POINT ( 'NONE', #23819 ) ;
#11033=ORIENTED_EDGE ( 'NONE', *, *, #56025, .F. ) ;
#11051=DIRECTION ( 'NONE',  ( 0.000000000000000000, 0.000000000000000000, -1.000000000000000000 ) ) ;
#11070=ADVANCED_FACE ( 'NONE', ( #68358 ), #34767, .F. ) ;
#11073=CARTESIAN_POINT ( 'NONE',  ( 41.09999999999999432, -21.00000000000000000, -13.86939075806900057 ) ) ;
#11078=LINE ( 'NONE', #53525, #22156 ) ;
#11101=DIRECTION ( 'NONE',  ( 1.000000000000000000, 0.000000000000000000, 0.000000000000000000 ) ) ;
#11103=EDGE_CURVE ( 'NONE', #36169, #54230, #24167, .T. ) ;
#11113=AXIS2_PLACEMENT_3D ( 'NONE', #15004, #52855, #41867 ) ;
#11148=EDGE_CURVE ( 'NONE', #61739, #59143, #47482, .T. ) ;
#11161=DIRECTION ( 'NONE',  ( 0.000000000000000000, 0.000000000000000000, -1.000000000000000000 ) ) ;
#11171=DIRECTION ( 'NONE',  ( 0.000000000000000000, 0.000000000000000000, 1.000000000000000000 ) ) ;
#11178=CARTESIAN_POINT ( 'NONE',  ( 41.09999999999999432, 14.08845687959340331, -21.00000000000000000 ) ) ;
#11179=CARTESIAN_POINT ( 'NONE',  ( 41.09999999999999432, -21.00000000000000000, -13.86939075806900057 ) ) ;
#11182=ORIENTED_EDGE ( 'NONE', *, *, #2106, .F. ) ;
#11187=EDGE_CURVE ( 'NONE', #3626, #9916, #28606, .T. ) ;
#11201=PLANE ( 'NONE',  #11690 ) ;
#11202=EDGE_CURVE ( 'NONE', #61739, #53333, #8266, .T. ) ;
#11204=AXIS2_PLACEMENT_3D ( 'NONE', #7296, #62433, #55750 ) ;
#11211=EDGE_CURVE ( 'NONE', #5469, #4613, #46686, .T. ) ;
#11217=LINE ( 'NONE', #35468, #17545 ) ;
#11218=ADVANCED_FACE ( 'NONE', ( #59492 ), #37933, .F. ) ;
#11219=CARTESIAN_POINT ( 'NONE',  ( 23.90000000000000213, 20.60000000000000142, -13.86939075806900057 ) ) ;
#11220=EDGE_LOOP ( 'NONE', ( #22106, #105, #44082, #60312 ) ) ;
#11227=EDGE_LOOP ( 'NONE', ( #43818, #52856, #51133, #48174, #47742, #64267, #41310, #20419 ) ) ;
#11233=ORIENTED_EDGE ( 'NONE', *, *, #39315, .F. ) ;
#11240=DIRECTION ( 'NONE',  ( 1.000000000000000000, -0.000000000000000000, 0.000000000000000000 ) ) ;
#11246=EDGE_CURVE ( 'NONE', #29427, #62756, #22959, .T. ) ;
#11266=ORIENTED_EDGE ( 'NONE', *, *, #5160, .T. ) ;
#11282=VECTOR ( 'NONE', #33118, 1000.000000000000000 ) ;
#11283=ORIENTED_EDGE ( 'NONE', *, *, #58630, .F. ) ;
#11291=LINE ( 'NONE', #50158, #17502 ) ;
#11292=VERTEX_POINT ( 'NONE', #49570 ) ;
#11301=VECTOR ( 'NONE', #12123, 1000.000000000000000 ) ;
#11312=CARTESIAN_POINT ( 'NONE',  ( 41.09999999999999432, 13.66939075806899950, 20.80000000000000426 ) ) ;
#11332=VECTOR ( 'NONE', #20886, 1000.000000000000000 ) ;
#11333=CARTESIAN_POINT ( 'NONE',  ( 17.89999999999999858, 13.66939075806899240, 20.79999999999999361 ) ) ;
#11350=CARTESIAN_POINT ( 'NONE',  ( 49.00000000000000000, -21.00000000000000000, 13.86939075806900057 ) ) ;
#11364=DIRECTION ( 'NONE',  ( 1.000000000000000000, -0.000000000000000000, 0.000000000000000000 ) ) ;
#11383=ORIENTED_EDGE ( 'NONE', *, *, #23174, .T. ) ;
#11389=DIRECTION ( 'NONE',  ( 0.000000000000000000, 0.000000000000000000, -1.000000000000000000 ) ) ;
#11404=DIRECTION ( 'NONE',  ( -1.000000000000000000, 0.000000000000000000, 0.000000000000000000 ) ) ;
#11418=EDGE_LOOP ( 'NONE', ( #19444, #30253, #30061, #32365 ) ) ;
#11420=VERTEX_POINT ( 'NONE', #13044 ) ;
#11429=DIRECTION ( 'NONE',  ( 0.000000000000000000, 0.000000000000000000, -1.000000000000000000 ) ) ;
#11433=EDGE_CURVE ( 'NONE', #63779, #19378, #14468, .T. ) ;
#11436=LINE ( 'NONE', #21008, #51248 ) ;
#11440=ORIENTED_EDGE ( 'NONE', *, *, #25115, .T. ) ;
#11442=DIRECTION ( 'NONE',  ( -1.000000000000000000, 0.000000000000000000, 0.000000000000000000 ) ) ;
#11443=AXIS2_PLACEMENT_3D ( 'NONE', #33630, #6747, #49886 ) ;
#11463=CARTESIAN_POINT ( 'NONE',  ( 9.899999999999998579, 13.66939075806899240, -20.79999999999999361 ) ) ;
#11465=ORIENTED_EDGE ( 'NONE', *, *, #9969, .T. ) ;
#11472=ADVANCED_FACE ( 'NONE', ( #57592 ), #30017, .T. ) ;
#11485=AXIS2_PLACEMENT_3D ( 'NONE', #10934, #20842, #63643 ) ;
#11487=EDGE_CURVE ( 'NONE', #35639, #61702, #3160, .T. ) ;
#11497=CARTESIAN_POINT ( 'NONE',  ( 17.89999999999999858, 0.000000000000000000, 1.077467997501122647E-15 ) ) ;
#11522=ADVANCED_FACE ( 'NONE', ( #33070 ), #5859, .T. ) ;
#11538=LINE ( 'NONE', #1624, #68603 ) ;
#11539=VECTOR ( 'NONE', #39856, 1000.000000000000000 ) ;
#11546=VERTEX_POINT ( 'NONE', #63960 ) ;
#11552=CARTESIAN_POINT ( 'NONE',  ( 25.57999999999999829, 0.000000000000000000, 0.000000000000000000 ) ) ;
#11562=VERTEX_POINT ( 'NONE', #553 ) ;
#11565=ADVANCED_FACE ( 'NONE', ( #46984 ), #27423, .T. ) ;
#11585=ADVANCED_FACE ( 'NONE', ( #58304 ), #47334, .F. ) ;
#11590=CARTESIAN_POINT ( 'NONE',  ( 0.000000000000000000, -17.79289321881345032, -20.50000000000000000 ) ) ;
#11594=CARTESIAN_POINT ( 'NONE',  ( 39.00000000000000000, 4.286263797015736595E-16, -3.500000000000000000 ) ) ;
#11602=DIRECTION ( 'NONE',  ( 0.000000000000000000, 0.000000000000000000, -1.000000000000000000 ) ) ;
#11616=DIRECTION ( 'NONE',  ( 0.000000000000000000, 0.000000000000000000, 1.000000000000000000 ) ) ;
#11619=LINE ( 'NONE', #16616, #3320 ) ;
#11630=EDGE_LOOP ( 'NONE', ( #16909, #53940, #31683, #27769 ) ) ;
#11648=STYLED_ITEM ( 'NONE', ( #49432 ), #43151 ) ;
#11654=LINE ( 'NONE', #55504, #50894 ) ;
#11665=EDGE_CURVE ( 'NONE', #20267, #14942, #7922, .T. ) ;
#11666=EDGE_CURVE ( 'NONE', #31019, #856, #43349, .T. ) ;
#11675=DIRECTION ( 'NONE',  ( -1.000000000000000000, 0.000000000000000000, 0.000000000000000000 ) ) ;
#11677=CARTESIAN_POINT ( 'NONE',  ( 30.90000000000000213, -14.06939075806900163, -20.80000000000000426 ) ) ;
#11678=CARTESIAN_POINT ( 'NONE',  ( 20.90000000000000213, -14.06939075806900874, 20.80000000000001137 ) ) ;
#11682=ORIENTED_EDGE ( 'NONE', *, *, #9020, .F. ) ;
#11688=DIRECTION ( 'NONE',  ( 0.000000000000000000, 0.000000000000000000, -1.000000000000000000 ) ) ;
#11690=AXIS2_PLACEMENT_3D ( 'NONE', #37738, #27471, #49042 ) ;
#11699=AXIS2_PLACEMENT_3D ( 'NONE', #33424, #68563, #41675 ) ;
#11712=SURFACE_STYLE_USAGE ( .BOTH. , #32951 ) ;
#11714=LINE ( 'NONE', #12743, #28895 ) ;
#11715=ORIENTED_EDGE ( 'NONE', *, *, #38484, .F. ) ;
#11721=DIRECTION ( 'NONE',  ( -1.000000000000000000, 0.000000000000000000, 0.000000000000000000 ) ) ;
#11723=DIRECTION ( 'NONE',  ( 0.000000000000000000, 0.000000000000000000, -1.000000000000000000 ) ) ;
#11733=ADVANCED_FACE ( 'NONE', ( #36556 ), #35857, .F. ) ;
#11737=EDGE_CURVE ( 'NONE', #13215, #25374, #15155, .T. ) ;
#11743=DIRECTION ( 'NONE',  ( 0.000000000000000000, 1.000000000000000000, 0.000000000000000000 ) ) ;
#11757=( NAMED_UNIT ( * ) PLANE_ANGLE_UNIT ( ) SI_UNIT ( $, .RADIAN. ) );
#11761=FACE_OUTER_BOUND ( 'NONE', #18307, .T. ) ;
#11762=PLANE ( 'NONE',  #58470 ) ;
#11779=ORIENTED_EDGE ( 'NONE', *, *, #41450, .T. ) ;
#11781=AXIS2_PLACEMENT_3D ( 'NONE', #21880, #16227, #48064 ) ;
#11796=DIRECTION ( 'NONE',  ( 0.000000000000000000, 1.000000000000000000, -0.000000000000000000 ) ) ;
#11808=EDGE_LOOP ( 'NONE', ( #843, #20089, #24473, #15328 ) ) ;
#11838=ORIENTED_EDGE ( 'NONE', *, *, #50731, .T. ) ;
#11849=STYLED_ITEM ( 'NONE', ( #52212 ), #44181 ) ;
#11867=ORIENTED_EDGE ( 'NONE', *, *, #65444, .F. ) ;
#11869=CARTESIAN_POINT ( 'NONE',  ( 49.00000000000000000, -0.1999999999911795112, 8.826273045769999343E-12 ) ) ;
#11895=DIRECTION ( 'NONE',  ( 0.000000000000000000, -1.000000000000000000, 0.000000000000000000 ) ) ;
#11896=DIRECTION ( 'NONE',  ( 0.000000000000000000, 0.000000000000000000, -1.000000000000000000 ) ) ;
#11923=FACE_OUTER_BOUND ( 'NONE', #1533, .T. ) ;
#11932=DIRECTION ( 'NONE',  ( 0.000000000000000000, 0.000000000000000000, 1.000000000000000000 ) ) ;
#11947=CIRCLE ( 'NONE', #18724, 24.99999999998794920 ) ;
#11966=AXIS2_PLACEMENT_3D ( 'NONE', #22730, #22398, #32999 ) ;
#11980=CIRCLE ( 'NONE', #38016, 25.39999999999999858 ) ;
#11985=VERTEX_POINT ( 'NONE', #38312 ) ;
#11987=VECTOR ( 'NONE', #7964, 1000.000000000000000 ) ;
#11991=EDGE_LOOP ( 'NONE', ( #36528, #137, #32596, #14612 ) ) ;
#11993=CARTESIAN_POINT ( 'NONE',  ( 14.89999999999999680, -14.06939075806900874, 20.80000000000001137 ) ) ;
#12007=EDGE_CURVE ( 'NONE', #37330, #66031, #49272, .T. ) ;
#12041=EDGE_LOOP ( 'NONE', ( #60548, #32152 ) ) ;
#12047=VECTOR ( 'NONE', #18608, 1000.000000000000000 ) ;
#12050=DIRECTION ( 'NONE',  ( 0.000000000000000000, 0.000000000000000000, -1.000000000000000000 ) ) ;
#12055=ORIENTED_EDGE ( 'NONE', *, *, #69952, .T. ) ;
#12063=CARTESIAN_POINT ( 'NONE',  ( 41.09999999999999432, -14.06939075806901940, -20.80000000000000426 ) ) ;
#12077=DIRECTION ( 'NONE',  ( 0.000000000000000000, 0.000000000000000000, 1.000000000000000000 ) ) ;
#12078=ORIENTED_EDGE ( 'NONE', *, *, #9153, .T. ) ;
#12087=DIRECTION ( 'NONE',  ( 0.000000000000000000, -0.5625376724249369076, -0.8267716535433071723 ) ) ;
#12098=VERTEX_POINT ( 'NONE', #66553 ) ;
#12106=DIRECTION ( 'NONE',  ( 0.000000000000000000, 0.000000000000000000, -1.000000000000000000 ) ) ;
#12117=VERTEX_POINT ( 'NONE', #40011 ) ;
#12122=VERTEX_POINT ( 'NONE', #54927 ) ;
#12123=DIRECTION ( 'NONE',  ( -0.000000000000000000, -1.000000000000000000, 0.000000000000000000 ) ) ;
#12126=EDGE_LOOP ( 'NONE', ( #40582, #68051 ) ) ;
#12135=CARTESIAN_POINT ( 'NONE',  ( 37.90000000000000568, -21.00000000000000000, 13.86939075806900057 ) ) ;
#12161=CARTESIAN_POINT ( 'NONE',  ( 39.90000000000000568, -14.06939075806902117, -20.80000000000000426 ) ) ;
#12175=EDGE_CURVE ( 'NONE', #7253, #4233, #35466, .T. ) ;
#12180=VERTEX_POINT ( 'NONE', #25530 ) ;
#12183=CARTESIAN_POINT ( 'NONE',  ( 40.90000000000000568, -14.06939075806902117, -20.80000000000000426 ) ) ;
#12191=CIRCLE ( 'NONE', #37060, 24.99999999998784972 ) ;
#12193=CARTESIAN_POINT ( 'NONE',  ( 48.50000000000000000, -0.7500000000000000000, -3.418698582794335028 ) ) ;
#12194=ORIENTED_EDGE ( 'NONE', *, *, #63011, .F. ) ;
#12201=ORIENTED_EDGE ( 'NONE', *, *, #30115, .T. ) ;
#12218=EDGE_CURVE ( 'NONE', #46458, #64694, #62287, .T. ) ;
#12219=CARTESIAN_POINT ( 'NONE',  ( 26.90000000000000213, 0.000000000000000000, 0.000000000000000000 ) ) ;
#12226=ORIENTED_EDGE ( 'NONE', *, *, #55740, .T. ) ;
#12231=DIRECTION ( 'NONE',  ( -1.000000000000000000, 0.000000000000000000, 0.000000000000000000 ) ) ;
#12238=VERTEX_POINT ( 'NONE', #61940 ) ;
#12242=DIRECTION ( 'NONE',  ( -1.000000000000000000, 0.000000000000000000, 0.000000000000000000 ) ) ;
#12247=ORIENTED_EDGE ( 'NONE', *, *, #30115, .F. ) ;
#12250=ADVANCED_FACE ( 'NONE', ( #3958 ), #68665, .T. ) ;
#12263=CARTESIAN_POINT ( 'NONE',  ( 49.00000000000000000, 13.66939075806899950, 20.80000000000000426 ) ) ;
#12272=CARTESIAN_POINT ( 'NONE',  ( 10.00000000000000000, -21.00000000000000000, 14.57806571531351914 ) ) ;
#12274=VECTOR ( 'NONE', #45667, 1000.000000000000000 ) ;
#12286=EDGE_CURVE ( 'NONE', #29958, #11292, #19762, .T. ) ;
#12287=ORIENTED_EDGE ( 'NONE', *, *, #43450, .F. ) ;
#12303=EDGE_CURVE ( 'NONE', #32276, #36995, #21620, .T. ) ;
#12316=ORIENTED_EDGE ( 'NONE', *, *, #30884, .T. ) ;
#12318=( LENGTH_UNIT ( ) NAMED_UNIT ( * ) SI_UNIT ( .MILLI., .METRE. ) );
#12322=ORIENTED_EDGE ( 'NONE', *, *, #61874, .T. ) ;
#12336=AXIS2_PLACEMENT_3D ( 'NONE', #7239, #3006, #35156 ) ;
#12340=DIRECTION ( 'NONE',  ( 0.000000000000000000, 0.000000000000000000, -1.000000000000000000 ) ) ;
#12349=LINE ( 'NONE', #13415, #19081 ) ;
#12383=SURFACE_STYLE_USAGE ( .BOTH. , #18747 ) ;
#12396=( NAMED_UNIT ( * ) PLANE_ANGLE_UNIT ( ) SI_UNIT ( $, .RADIAN. ) );
#12400=DIRECTION ( 'NONE',  ( 1.000000000000000000, -0.000000000000000000, 0.000000000000000000 ) ) ;
#12411=ORIENTED_EDGE ( 'NONE', *, *, #23174, .F. ) ;
#12425=CARTESIAN_POINT ( 'NONE',  ( 10.00000000000000000, -21.00000000000000000, 18.00000000000000355 ) ) ;
#12428=VECTOR ( 'NONE', #32403, 1000.000000000000000 ) ;
#12435=FACE_BOUND ( 'NONE', #25230, .T. ) ;
#12437=AXIS2_PLACEMENT_3D ( 'NONE', #17059, #7120, #43582 ) ;
#12443=DIRECTION ( 'NONE',  ( 0.000000000000000000, 0.000000000000000000, -1.000000000000000000 ) ) ;
#12446=FACE_OUTER_BOUND ( 'NONE', #13988, .T. ) ;
#12450=VECTOR ( 'NONE', #56347, 1000.000000000000000 ) ;
#12455=EDGE_CURVE ( 'NONE', #16007, #63302, #45703, .T. ) ;
#12475=EDGE_CURVE ( 'NONE', #14272, #13993, #50562, .T. ) ;
#12493=VECTOR ( 'NONE', #48085, 1000.000000000000114 ) ;
#12494=EDGE_LOOP ( 'NONE', ( #14876, #14163, #52084, #9949 ) ) ;
#12496=CARTESIAN_POINT ( 'NONE',  ( 46.39999999999999858, 33.00000000000000000, 1.750000000000000222 ) ) ;
#12497=CIRCLE ( 'NONE', #15909, 24.99999999998784972 ) ;
#12504=DIRECTION ( 'NONE',  ( -1.000000000000000000, 0.000000000000000000, 0.000000000000000000 ) ) ;
#12514=CYLINDRICAL_SURFACE ( 'NONE', #34554, 0.5000000000000000000 ) ;
#12534=LINE ( 'NONE', #5865, #29059 ) ;
#12542=DIRECTION ( 'NONE',  ( 0.000000000000000000, 0.7071067811865475727, 0.7071067811865475727 ) ) ;
#12554=LINE ( 'NONE', #6585, #23190 ) ;
#12563=DIRECTION ( 'NONE',  ( 0.000000000000000000, 0.000000000000000000, 1.000000000000000000 ) ) ;
#12569=ORIENTED_EDGE ( 'NONE', *, *, #31305, .F. ) ;
#12571=DIRECTION ( 'NONE',  ( 0.000000000000000000, 0.5625376724249369076, 0.8267716535433071723 ) ) ;
#12582=CLOSED_SHELL ( 'NONE', ( #68626, #42533, #3458, #40407, #40882, #21905, #58306, #47250, #23960, #13811 ) ) ;
#12593=ORIENTED_EDGE ( 'NONE', *, *, #47215, .T. ) ;
#12601=CARTESIAN_POINT ( 'NONE',  ( 41.09999999999999432, 13.66939075806899950, 20.80000000000000426 ) ) ;
#12606=ORIENTED_EDGE ( 'NONE', *, *, #51742, .F. ) ;
#12621=DIRECTION ( 'NONE',  ( 1.000000000000000000, -0.000000000000000000, 0.000000000000000000 ) ) ;
#12622=CARTESIAN_POINT ( 'NONE',  ( 47.00000000000000000, 0.000000000000000000, 0.000000000000000000 ) ) ;
#12627=CARTESIAN_POINT ( 'NONE',  ( 41.09999999999999432, 20.60000000000000142, 13.86939075806900057 ) ) ;
#12632=CARTESIAN_POINT ( 'NONE',  ( 39.90000000000000568, -0.2000000000000000111, 0.000000000000000000 ) ) ;
#12639=ORIENTED_EDGE ( 'NONE', *, *, #22905, .T. ) ;
#12654=CARTESIAN_POINT ( 'NONE',  ( 38.90000000000000568, 0.000000000000000000, 0.000000000000000000 ) ) ;
#12656=CARTESIAN_POINT ( 'NONE',  ( 3.552713678800500929E-15, 17.79289321881343255, -20.50000000000000355 ) ) ;
#12669=DIRECTION ( 'NONE',  ( -1.000000000000000000, 0.000000000000000000, 0.000000000000000000 ) ) ;
#12671=ORIENTED_EDGE ( 'NONE', *, *, #5930, .T. ) ;
#12676=AXIS2_PLACEMENT_3D ( 'NONE', #17456, #48609, #38004 ) ;
#12688=FILL_AREA_STYLE ('',( #60794 ) ) ;
#12692=VECTOR ( 'NONE', #1595, 1000.000000000000000 ) ;
#12717=VECTOR ( 'NONE', #62813, 1000.000000000000114 ) ;
#12721=FACE_OUTER_BOUND ( 'NONE', #43651, .T. ) ;
#12730=( NAMED_UNIT ( * ) SI_UNIT ( $, .STERADIAN. ) SOLID_ANGLE_UNIT ( ) );
#12743=CARTESIAN_POINT ( 'NONE',  ( 41.09999999999999432, 13.66939075806899950, -20.80000000000000426 ) ) ;
#12746=DIRECTION ( 'NONE',  ( -0.7071067811865474617, 0.000000000000000000, 0.7071067811865474617 ) ) ;
#12747=EDGE_LOOP ( 'NONE', ( #50686, #5673, #27575, #25943 ) ) ;
#12764=AXIS2_PLACEMENT_3D ( 'NONE', #65991, #59670, #11896 ) ;
#12766=EDGE_LOOP ( 'NONE', ( #37925, #43116, #23813, #21541, #14200, #63207, #18099, #5353 ) ) ;
#12767=EDGE_CURVE ( 'NONE', #53797, #17980, #53022, .T. ) ;
#12773=ORIENTED_EDGE ( 'NONE', *, *, #2427, .F. ) ;
#12781=EDGE_CURVE ( 'NONE', #56261, #40969, #57954, .T. ) ;
#12790=VECTOR ( 'NONE', #44547, 1000.000000000000000 ) ;
#12791=VECTOR ( 'NONE', #39791, 1000.000000000000000 ) ;
#12795=DIRECTION ( 'NONE',  ( -1.000000000000000000, 0.000000000000000000, 0.000000000000000000 ) ) ;
#12798=AXIS2_PLACEMENT_3D ( 'NONE', #22698, #33313, #11051 ) ;
#12801=VECTOR ( 'NONE', #6961, 1000.000000000000000 ) ;
#12812=VERTEX_POINT ( 'NONE', #25797 ) ;
#12819=VERTEX_POINT ( 'NONE', #15542 ) ;
#12832=DIRECTION ( 'NONE',  ( 0.000000000000000000, 0.000000000000000000, 1.000000000000000000 ) ) ;
#12834=DIRECTION ( 'NONE',  ( -1.000000000000000000, 0.000000000000000000, 0.000000000000000000 ) ) ;
#12846=ORIENTED_EDGE ( 'NONE', *, *, #29796, .T. ) ;
#12849=ORIENTED_EDGE ( 'NONE', *, *, #47980, .F. ) ;
#12859=ORIENTED_EDGE ( 'NONE', *, *, #51764, .T. ) ;
#12874=DIRECTION ( 'NONE',  ( 0.000000000000000000, 0.000000000000000000, -1.000000000000000000 ) ) ;
#12879=DIRECTION ( 'NONE',  ( -1.000000000000000000, 0.000000000000000000, 0.000000000000000000 ) ) ;
#12882=FACE_OUTER_BOUND ( 'NONE', #53931, .T. ) ;
#12900=DIRECTION ( 'NONE',  ( -1.000000000000000000, 0.000000000000000000, 0.000000000000000000 ) ) ;
#12902=DIRECTION ( 'NONE',  ( -0.7071067811865472397, 0.5000000000000002220, -0.5000000000000002220 ) ) ;
#12919=CARTESIAN_POINT ( 'NONE',  ( 39.00000000000000000, 21.00000000000000000, -16.96999999999999886 ) ) ;
#12922=EDGE_CURVE ( 'NONE', #50270, #5931, #33169, .T. ) ;
#12935=ORIENTED_EDGE ( 'NONE', *, *, #7023, .F. ) ;
#12944=LINE ( 'NONE', #24272, #60858 ) ;
#12947=EDGE_CURVE ( 'NONE', #1574, #61299, #50470, .T. ) ;
#12954=CARTESIAN_POINT ( 'NONE',  ( 55.00000000000000000, -16.96999999999999886, 21.00000000000000000 ) ) ;
#12966=DIRECTION ( 'NONE',  ( 0.000000000000000000, -1.000000000000000000, 0.000000000000000000 ) ) ;
#12978=AXIS2_PLACEMENT_3D ( 'NONE', #17260, #54755, #44816 ) ;
#12987=ORIENTED_EDGE ( 'NONE', *, *, #54420, .F. ) ;
#13000=ORIENTED_EDGE ( 'NONE', *, *, #43928, .T. ) ;
#13004=ORIENTED_EDGE ( 'NONE', *, *, #21036, .T. ) ;
#13009=VECTOR ( 'NONE', #8101, 1000.000000000000000 ) ;
#13010=PLANE ( 'NONE',  #66218 ) ;
#13012=LINE ( 'NONE', #14070, #7344 ) ;
#13023=AXIS2_PLACEMENT_3D ( 'NONE', #2359, #18612, #62090 ) ;
#13031=CIRCLE ( 'NONE', #5198, 24.99999999998794920 ) ;
#13032=DIRECTION ( 'NONE',  ( 1.000000000000000000, -0.000000000000000000, 0.000000000000000000 ) ) ;
#13038=AXIS2_PLACEMENT_3D ( 'NONE', #2173, #18783, #23739 ) ;
#13044=CARTESIAN_POINT ( 'NONE',  ( 9.900000000000000355, -14.48845687959340012, -21.00000000000000000 ) ) ;
#13049=VECTOR ( 'NONE', #65815, 1000.000000000000000 ) ;
#13058=FACE_OUTER_BOUND ( 'NONE', #11220, .T. ) ;
#13067=DIRECTION ( 'NONE',  ( 0.000000000000000000, 0.000000000000000000, -1.000000000000000000 ) ) ;
#13068=LINE ( 'NONE', #44548, #21546 ) ;
#13085=EDGE_CURVE ( 'NONE', #40022, #43129, #29942, .T. ) ;
#13099=CARTESIAN_POINT ( 'NONE',  ( 15.89999999999999680, -21.00000000000000000, 13.86939075806900057 ) ) ;
#13113=VERTEX_POINT ( 'NONE', #61775 ) ;
#13114=AXIS2_PLACEMENT_3D ( 'NONE', #7569, #56358, #29135 ) ;
#13118=VERTEX_POINT ( 'NONE', #3431 ) ;
#13129=AXIS2_PLACEMENT_3D ( 'NONE', #60890, #24478, #12443 ) ;
#13135=CARTESIAN_POINT ( 'NONE',  ( 9.899999999999998579, -21.00000000000000355, 14.57806571531352269 ) ) ;
#13142=FACE_OUTER_BOUND ( 'NONE', #18161, .T. ) ;
#13144=AXIS2_PLACEMENT_3D ( 'NONE', #33239, #22631, #44877 ) ;
#13147=CARTESIAN_POINT ( 'NONE',  ( 41.09999999999999432, -14.06939075806902117, -20.80000000000000426 ) ) ;
#13151=AXIS2_PLACEMENT_3D ( 'NONE', #43097, #15195, #68932 ) ;
#13159=DIRECTION ( 'NONE',  ( 0.000000000000000000, 0.000000000000000000, 1.000000000000000000 ) ) ;
#13166=AXIS2_PLACEMENT_3D ( 'NONE', #62993, #14545, #36109 ) ;
#13176=LINE ( 'NONE', #24142, #45608 ) ;
#13185=CARTESIAN_POINT ( 'NONE',  ( 46.39999999999999858, 21.00000000000000000, 0.7500000000000000000 ) ) ;
#13186=DIRECTION ( 'NONE',  ( 0.000000000000000000, -0.7071067811865474617, -0.7071067811865474617 ) ) ;
#13191=( NAMED_UNIT ( * ) PLANE_ANGLE_UNIT ( ) SI_UNIT ( $, .RADIAN. ) );
#13214=ORIENTED_EDGE ( 'NONE', *, *, #53936, .F. ) ;
#13215=VERTEX_POINT ( 'NONE', #31713 ) ;
#13222=CYLINDRICAL_SURFACE ( 'NONE', #13114, 24.99999999998789946 ) ;
#13225=DIRECTION ( 'NONE',  ( 0.000000000000000000, 1.000000000000000000, 0.000000000000000000 ) ) ;
#13232=FACE_OUTER_BOUND ( 'NONE', #20507, .T. ) ;
#13245=AXIS2_PLACEMENT_3D ( 'NONE', #59951, #564, #32402 ) ;
#13256=VECTOR ( 'NONE', #57504, 1000.000000000000000 ) ;
#13268=CARTESIAN_POINT ( 'NONE',  ( 0.5000000000000000000, 18.00000000000000355, -21.00000000000000000 ) ) ;
#13273=DIRECTION ( 'NONE',  ( 1.000000000000000000, -0.000000000000000000, 0.000000000000000000 ) ) ;
#13277=EDGE_CURVE ( 'NONE', #13881, #5466, #16504, .T. ) ;
#13282=PLANE ( 'NONE',  #27358 ) ;
#13288=COLOUR_RGB ( '', 0.66274510, 0.83137255, 0.94901961) ;
#13293=ORIENTED_EDGE ( 'NONE', *, *, #59326, .T. ) ;
#13299=VERTEX_POINT ( 'NONE', #6218 ) ;
#13316=DIRECTION ( 'NONE',  ( 1.000000000000000000, -0.000000000000000000, -0.000000000000000000 ) ) ;
#13323=DIRECTION ( 'NONE',  ( 1.000000000000000000, -0.000000000000000000, 0.000000000000000000 ) ) ;
#13333=FACE_OUTER_BOUND ( 'NONE', #47793, .T. ) ;
#13337=CYLINDRICAL_SURFACE ( 'NONE', #42168, 24.99999999998784972 ) ;
#13347=PLANE ( 'NONE',  #43434 ) ;
#13363=EDGE_LOOP ( 'NONE', ( #41323, #19399, #13385, #2818 ) ) ;
#13368=EDGE_LOOP ( 'NONE', ( #7158, #58684, #20527, #19337, #50812, #59875, #3648, #40452 ) ) ;
#13370=VECTOR ( 'NONE', #69271, 999.9999999999998863 ) ;
#13379=LINE ( 'NONE', #17637, #53454 ) ;
#13381=EDGE_CURVE ( 'NONE', #7564, #13118, #61683, .T. ) ;
#13385=ORIENTED_EDGE ( 'NONE', *, *, #22597, .T. ) ;
#13388=EDGE_LOOP ( 'NONE', ( #67804, #3963, #63810, #23555 ) ) ;
#13398=VECTOR ( 'NONE', #45356, 1000.000000000000000 ) ;
#13405=VERTEX_POINT ( 'NONE', #56041 ) ;
#13406=ADVANCED_FACE ( 'NONE', ( #14566 ), #34806, .F. ) ;
#13413=VECTOR ( 'NONE', #68596, 1000.000000000000114 ) ;
#13415=CARTESIAN_POINT ( 'NONE',  ( 41.09999999999999432, 20.60000000000000142, 13.86939075806900057 ) ) ;
#13424=CARTESIAN_POINT ( 'NONE',  ( 31.89999999999999858, 3.010794155703768650E-16, -2.458500000000000796 ) ) ;
#13427=EDGE_LOOP ( 'NONE', ( #6112, #7768 ) ) ;
#13430=DIRECTION ( 'NONE',  ( -1.000000000000000000, 0.000000000000000000, 0.000000000000000000 ) ) ;
#13434=FILL_AREA_STYLE_COLOUR ( '', #25323 ) ;
#13436=CARTESIAN_POINT ( 'NONE',  ( 21.90000000000000213, -0.2000000000089119934, 8.909539772616881237E-12 ) ) ;
#13455=DIRECTION ( 'NONE',  ( 0.000000000000000000, 0.000000000000000000, -1.000000000000000000 ) ) ;
#13457=VECTOR ( 'NONE', #20206, 1000.000000000000000 ) ;
#13458=DIRECTION ( 'NONE',  ( 0.000000000000000000, -0.1500000000000000777, 0.9886859966642594921 ) ) ;
#13461=ORIENTED_EDGE ( 'NONE', *, *, #12922, .F. ) ;
#13482=AXIS2_PLACEMENT_3D ( 'NONE', #26895, #15234, #41740 ) ;
#13489=LINE ( 'NONE', #51320, #65121 ) ;
#13493=ADVANCED_FACE ( 'NONE', ( #12882 ), #9270, .F. ) ;
#13512=ORIENTED_EDGE ( 'NONE', *, *, #30285, .F. ) ;
#13532=LINE ( 'NONE', #28397, #47555 ) ;
#13541=EDGE_CURVE ( 'NONE', #49662, #50027, #21630, .T. ) ;
#13543=FILL_AREA_STYLE_COLOUR ( '', #69507 ) ;
#13547=ADVANCED_FACE ( 'NONE', ( #48151 ), #16315, .T. ) ;
#13560=AXIS2_PLACEMENT_3D ( 'NONE', #15539, #37101, #10561 ) ;
#13573=AXIS2_PLACEMENT_3D ( 'NONE', #55192, #44218, #45604 ) ;
#13586=EDGE_CURVE ( 'NONE', #427, #11005, #10318, .T. ) ;
#13591=ADVANCED_FACE ( 'NONE', ( #58425, #17010 ), #21284, .T. ) ;
#13595=DIRECTION ( 'NONE',  ( 0.000000000000000000, 0.000000000000000000, 1.000000000000000000 ) ) ;
#13598=FACE_OUTER_BOUND ( 'NONE', #41574, .T. ) ;
#13606=CARTESIAN_POINT ( 'NONE',  ( 46.39999999999999858, 21.00000000000000000, 2.250000000000000444 ) ) ;
#13617=EDGE_LOOP ( 'NONE', ( #56693, #20647, #12247, #40669, #56065, #42389, #62778, #47296 ) ) ;
#13624=CIRCLE ( 'NONE', #54278, 24.99999999998789946 ) ;
#13627=ADVANCED_FACE ( 'NONE', ( #43179 ), #59795, .F. ) ;
#13629=ORIENTED_EDGE ( 'NONE', *, *, #25802, .T. ) ;
#13631=PLANE ( 'NONE',  #20488 ) ;
#13637=ORIENTED_EDGE ( 'NONE', *, *, #62518, .F. ) ;
#13641=ORIENTED_EDGE ( 'NONE', *, *, #42492, .F. ) ;
#13652=FACE_OUTER_BOUND ( 'NONE', #21314, .T. ) ;
#13657=AXIS2_PLACEMENT_3D ( 'NONE', #64266, #37389, #21468 ) ;
#13663=PLANE ( 'NONE',  #41413 ) ;
#13664=DIRECTION ( 'NONE',  ( -1.000000000000000000, 0.000000000000000000, 0.000000000000000000 ) ) ;
#13680=DIRECTION ( 'NONE',  ( -1.000000000000000000, -0.000000000000000000, -0.000000000000000000 ) ) ;
#13700=ORIENTED_EDGE ( 'NONE', *, *, #19816, .T. ) ;
#13703=EDGE_CURVE ( 'NONE', #21641, #50270, #39261, .T. ) ;
#13706=ORIENTED_EDGE ( 'NONE', *, *, #65120, .F. ) ;
#13712=CARTESIAN_POINT ( 'NONE',  ( 41.09999999999999432, 20.60000000000000142, 13.86939075806900057 ) ) ;
#13729=DIRECTION ( 'NONE',  ( 0.000000000000000000, 0.000000000000000000, 1.000000000000000000 ) ) ;
#13734=ORIENTED_EDGE ( 'NONE', *, *, #37274, .F. ) ;
#13743=CARTESIAN_POINT ( 'NONE',  ( 10.00000000000000000, 18.00000000000000355, -21.00000000000000000 ) ) ;
#13750=CARTESIAN_POINT ( 'NONE',  ( 24.90000000000000213, -0.1999999999911795112, 8.826273045769999343E-12 ) ) ;
#13751=VERTEX_POINT ( 'NONE', #56225 ) ;
#13758=AXIS2_PLACEMENT_3D ( 'NONE', #10582, #53733, #69286 ) ;
#13764=DIRECTION ( 'NONE',  ( 0.000000000000000000, 1.000000000000000000, 0.000000000000000000 ) ) ;
#13767=EDGE_CURVE ( 'NONE', #24647, #31689, #11980, .T. ) ;
#13776=CARTESIAN_POINT ( 'NONE',  ( 49.00000000000000000, -0.1999999999911430404, -8.864436962241481021E-12 ) ) ;
#13778=ORIENTED_EDGE ( 'NONE', *, *, #9846, .T. ) ;
#13791=FACE_OUTER_BOUND ( 'NONE', #51037, .T. ) ;
#13811=ADVANCED_FACE ( 'NONE', ( #6400 ), #27967, .T. ) ;
#13829=ADVANCED_FACE ( 'NONE', ( #40995 ), #68587, .F. ) ;
#13842=LINE ( 'NONE', #15858, #31138 ) ;
#13847=DIRECTION ( 'NONE',  ( 1.000000000000000000, -0.000000000000000000, 0.000000000000000000 ) ) ;
#13851=VERTEX_POINT ( 'NONE', #41703 ) ;
#13852=DIRECTION ( 'NONE',  ( 0.000000000000000000, 0.000000000000000000, -1.000000000000000000 ) ) ;
#13876=VECTOR ( 'NONE', #14040, 1000.000000000000000 ) ;
#13881=VERTEX_POINT ( 'NONE', #52686 ) ;
#13886=FACE_OUTER_BOUND ( 'NONE', #64856, .T. ) ;
#13889=DIRECTION ( 'NONE',  ( 0.000000000000000000, 0.000000000000000000, -1.000000000000000000 ) ) ;
#13890=LINE ( 'NONE', #36508, #44385 ) ;
#13896=ORIENTED_EDGE ( 'NONE', *, *, #60442, .F. ) ;
#13897=VERTEX_POINT ( 'NONE', #14491 ) ;
#13903=ADVANCED_FACE ( 'NONE', ( #14128 ), #56903, .F. ) ;
#13906=CARTESIAN_POINT ( 'NONE',  ( 39.00000000000000000, -16.96999999999999886, 21.00000000000000000 ) ) ;
#13916=DIRECTION ( 'NONE',  ( 0.000000000000000000, 0.000000000000000000, -1.000000000000000000 ) ) ;
#13918=ORIENTED_EDGE ( 'NONE', *, *, #64757, .F. ) ;
#13927=ORIENTED_EDGE ( 'NONE', *, *, #282, .F. ) ;
#13933=VECTOR ( 'NONE', #66011, 1000.000000000000000 ) ;
#13959=DIRECTION ( 'NONE',  ( 1.000000000000000000, -0.000000000000000000, 0.000000000000000000 ) ) ;
#13960=SURFACE_SIDE_STYLE ('',( #25277 ) ) ;
#13977=VECTOR ( 'NONE', #47467, 1000.000000000000000 ) ;
#13982=EDGE_CURVE ( 'NONE', #54230, #65046, #63846, .T. ) ;
#13988=EDGE_LOOP ( 'NONE', ( #41139, #47706, #32058, #15481 ) ) ;
#13993=VERTEX_POINT ( 'NONE', #26157 ) ;
#13996=DIRECTION ( 'NONE',  ( -1.000000000000000000, 0.000000000000000000, 0.000000000000000000 ) ) ;
#14004=DIRECTION ( 'NONE',  ( -1.000000000000000000, 0.000000000000000000, 0.000000000000000000 ) ) ;
#14008=PLANE ( 'NONE',  #55066 ) ;
#14014=CARTESIAN_POINT ( 'NONE',  ( 25.57999999999999829, 3.010794155703768650E-16, -2.458500000000000796 ) ) ;
#14017=CIRCLE ( 'NONE', #8408, 24.99999999998784972 ) ;
#14027=CARTESIAN_POINT ( 'NONE',  ( 15.89999999999999680, -14.06939075806902117, -20.80000000000000426 ) ) ;
#14029=CARTESIAN_POINT ( 'NONE',  ( 14.89999999999999680, -0.1999999999911795112, 8.826273045769999343E-12 ) ) ;
#14036=ORIENTED_EDGE ( 'NONE', *, *, #28352, .F. ) ;
#14040=DIRECTION ( 'NONE',  ( -1.000000000000000000, 0.000000000000000000, 0.000000000000000000 ) ) ;
#14048=VERTEX_POINT ( 'NONE', #47711 ) ;
#14070=CARTESIAN_POINT ( 'NONE',  ( 26.90000000000000213, 13.66939075806899950, 20.80000000000000426 ) ) ;
#14078=VECTOR ( 'NONE', #19711, 1000.000000000000000 ) ;
#14088=ORIENTED_EDGE ( 'NONE', *, *, #48472, .F. ) ;
#14091=FACE_OUTER_BOUND ( 'NONE', #49957, .T. ) ;
#14093=CARTESIAN_POINT ( 'NONE',  ( 40.90000000000000568, 16.96999999999999886, 21.00000000000000000 ) ) ;
#14094=FACE_OUTER_BOUND ( 'NONE', #45722, .T. ) ;
#14096=VERTEX_POINT ( 'NONE', #26496 ) ;
#14116=ORIENTED_EDGE ( 'NONE', *, *, #30675, .F. ) ;
#14125=DIRECTION ( 'NONE',  ( 1.000000000000000000, -0.000000000000000000, 0.000000000000000000 ) ) ;
#14128=FACE_OUTER_BOUND ( 'NONE', #67929, .T. ) ;
#14129=VECTOR ( 'NONE', #35105, 1000.000000000000000 ) ;
#14161=VECTOR ( 'NONE', #1697, 1000.000000000000000 ) ;
#14163=ORIENTED_EDGE ( 'NONE', *, *, #58630, .T. ) ;
#14178=EDGE_CURVE ( 'NONE', #55616, #44242, #58187, .T. ) ;
#14181=FACE_BOUND ( 'NONE', #8872, .T. ) ;
#14191=VECTOR ( 'NONE', #49177, 1000.000000000000000 ) ;
#14194=FACE_OUTER_BOUND ( 'NONE', #67922, .T. ) ;
#14200=ORIENTED_EDGE ( 'NONE', *, *, #54153, .F. ) ;
#14209=CARTESIAN_POINT ( 'NONE',  ( 27.90000000000000213, 0.000000000000000000, 0.000000000000000000 ) ) ;
#14211=ADVANCED_FACE ( 'NONE', ( #39849 ), #44468, .F. ) ;
#14216=ORIENTED_EDGE ( 'NONE', *, *, #43400, .T. ) ;
#14222=CIRCLE ( 'NONE', #49217, 24.99999999998789946 ) ;
#14227=EDGE_CURVE ( 'NONE', #63302, #9904, #1021, .T. ) ;
#14234=AXIS2_PLACEMENT_3D ( 'NONE', #66503, #8856, #61529 ) ;
#14261=EDGE_LOOP ( 'NONE', ( #51194, #39236, #4739, #14036 ) ) ;
#14272=VERTEX_POINT ( 'NONE', #20054 ) ;
#14277=AXIS2_PLACEMENT_3D ( 'NONE', #26679, #21371, #42932 ) ;
#14281=ORIENTED_EDGE ( 'NONE', *, *, #26979, .T. ) ;
#14285=VECTOR ( 'NONE', #6366, 1000.000000000000000 ) ;
#14288=DIRECTION ( 'NONE',  ( -1.000000000000000000, 0.000000000000000000, 0.000000000000000000 ) ) ;
#14291=ORIENTED_EDGE ( 'NONE', *, *, #19516, .T. ) ;
#14295=DIRECTION ( 'NONE',  ( 0.000000000000000000, 0.000000000000000000, -1.000000000000000000 ) ) ;
#14299=ORIENTED_EDGE ( 'NONE', *, *, #2533, .F. ) ;
#14301=ADVANCED_FACE ( 'NONE', ( #23951 ), #19001, .T. ) ;
#14317=FACE_OUTER_BOUND ( 'NONE', #46578, .T. ) ;
#14332=ORIENTED_EDGE ( 'NONE', *, *, #64381, .T. ) ;
#14339=DIRECTION ( 'NONE',  ( 1.000000000000000000, 0.000000000000000000, 0.000000000000000000 ) ) ;
#14341=CIRCLE ( 'NONE', #66266, 3.500000000000000000 ) ;
#14342=DIRECTION ( 'NONE',  ( 0.000000000000000000, 0.000000000000000000, -1.000000000000000000 ) ) ;
#14347=LINE ( 'NONE', #23893, #25124 ) ;
#14351=FACE_OUTER_BOUND ( 'NONE', #38769, .T. ) ;
#14356=EDGE_CURVE ( 'NONE', #69700, #51833, #63895, .T. ) ;
#14365=ORIENTED_EDGE ( 'NONE', *, *, #50731, .F. ) ;
#14375=ADVANCED_FACE ( 'NONE', ( #56477 ), #62838, .F. ) ;
#14385=PLANE ( 'NONE',  #45434 ) ;
#14389=CARTESIAN_POINT ( 'NONE',  ( 41.09999999999999432, -14.06939075806901940, -20.80000000000000426 ) ) ;
#14394=CARTESIAN_POINT ( 'NONE',  ( 27.00000000000000000, 3.010794155703768650E-16, 2.458500000000000796 ) ) ;
#14397=CIRCLE ( 'NONE', #29022, 0.5000000000000000000 ) ;
#14414=LINE ( 'NONE', #24316, #42838 ) ;
#14421=CIRCLE ( 'NONE', #23449, 2.458500000000000796 ) ;
#14432=DIRECTION ( 'NONE',  ( -1.000000000000000000, 0.000000000000000000, 0.000000000000000000 ) ) ;
#14437=ADVANCED_FACE ( 'NONE', ( #42314 ), #26763, .T. ) ;
#14450=DIRECTION ( 'NONE',  ( -1.000000000000000000, 0.000000000000000000, 0.000000000000000000 ) ) ;
#14455=EDGE_LOOP ( 'NONE', ( #43373, #8423, #4713, #62315 ) ) ;
#14462=ORIENTED_EDGE ( 'NONE', *, *, #49090, .T. ) ;
#14466=PRESENTATION_STYLE_ASSIGNMENT (( #14814 ) ) ;
#14468=LINE ( 'NONE', #24008, #39948 ) ;
#14472=CARTESIAN_POINT ( 'NONE',  ( 28.90000000000000213, -21.00000000000001421, -13.86939075806900945 ) ) ;
#14474=CARTESIAN_POINT ( 'NONE',  ( 33.89999999999999858, 13.66939075806899240, 20.79999999999999361 ) ) ;
#14479=( NAMED_UNIT ( * ) SI_UNIT ( $, .STERADIAN. ) SOLID_ANGLE_UNIT ( ) );
#14486=VECTOR ( 'NONE', #34938, 1000.000000000000000 ) ;
#14491=CARTESIAN_POINT ( 'NONE',  ( 8.900000000000002132, -18.00000000000000355, 21.00000000000000000 ) ) ;
#14501=ORIENTED_EDGE ( 'NONE', *, *, #26754, .F. ) ;
#14504=LINE ( 'NONE', #46668, #27643 ) ;
#14509=VERTEX_POINT ( 'NONE', #63548 ) ;
#14522=DIRECTION ( 'NONE',  ( 0.000000000000000000, 0.7071067811865474617, -0.7071067811865474617 ) ) ;
#14533=CARTESIAN_POINT ( 'NONE',  ( 32.89999999999999858, 3.010794155703768650E-16, -2.458500000000000796 ) ) ;
#14534=ADVANCED_FACE ( 'NONE', ( #58934 ), #10489, .F. ) ;
#14539=CARTESIAN_POINT ( 'NONE',  ( 11.90000000000000036, -21.00000000000001421, -13.86939075806900945 ) ) ;
#14542=ORIENTED_EDGE ( 'NONE', *, *, #52068, .T. ) ;
#14545=DIRECTION ( 'NONE',  ( 1.000000000000000000, -0.000000000000000000, 0.000000000000000000 ) ) ;
#14547=CARTESIAN_POINT ( 'NONE',  ( 41.09999999999999432, 20.60000000000000142, 13.86939075806900057 ) ) ;
#14555=CARTESIAN_POINT ( 'NONE',  ( 41.09999999999999432, 14.08845687959340331, -21.00000000000000000 ) ) ;
#14566=FACE_OUTER_BOUND ( 'NONE', #59847, .T. ) ;
#14567=CARTESIAN_POINT ( 'NONE',  ( 29.89999999999999858, 13.66939075806899240, 20.79999999999999361 ) ) ;
#14580=CIRCLE ( 'NONE', #67679, 25.39999999999999858 ) ;
#14581=DIRECTION ( 'NONE',  ( 0.000000000000000000, 0.000000000000000000, -1.000000000000000000 ) ) ;
#14590=FACE_OUTER_BOUND ( 'NONE', #46846, .T. ) ;
#14612=ORIENTED_EDGE ( 'NONE', *, *, #24319, .F. ) ;
#14618=EDGE_CURVE ( 'NONE', #6963, #17758, #13031, .T. ) ;
#14632=CYLINDRICAL_SURFACE ( 'NONE', #60552, 0.5000000000000000000 ) ;
#14638=AXIS2_PLACEMENT_3D ( 'NONE', #36048, #29689, #19777 ) ;
#14639=DIRECTION ( 'NONE',  ( 1.000000000000000000, -0.000000000000000000, 0.000000000000000000 ) ) ;
#14640=EDGE_LOOP ( 'NONE', ( #60533, #29649, #68232, #26240 ) ) ;
#14647=EDGE_CURVE ( 'NONE', #44331, #65063, #12554, .T. ) ;
#14648=DIRECTION ( 'NONE',  ( 1.000000000000000000, -0.000000000000000000, 0.000000000000000000 ) ) ;
#14658=DIRECTION ( 'NONE',  ( 0.000000000000000000, 0.000000000000000000, 1.000000000000000000 ) ) ;
#14663=VERTEX_POINT ( 'NONE', #39773 ) ;
#14666=ADVANCED_FACE ( 'NONE', ( #19611 ), #18564, .F. ) ;
#14680=( NAMED_UNIT ( * ) PLANE_ANGLE_UNIT ( ) SI_UNIT ( $, .RADIAN. ) );
#14687=FACE_OUTER_BOUND ( 'NONE', #43795, .T. ) ;
#14697=AXIS2_PLACEMENT_3D ( 'NONE', #34011, #23421, #12106 ) ;
#14709=ORIENTED_EDGE ( 'NONE', *, *, #41596, .T. ) ;
#14715=EDGE_CURVE ( 'NONE', #38637, #13897, #24228, .T. ) ;
#14719=DIRECTION ( 'NONE',  ( -1.000000000000000000, 0.000000000000000000, 0.000000000000000000 ) ) ;
#14726=FILL_AREA_STYLE_COLOUR ( '', #41235 ) ;
#14730=DIRECTION ( 'NONE',  ( 1.000000000000000000, -0.000000000000000000, 0.000000000000000000 ) ) ;
#14731=DIRECTION ( 'NONE',  ( 0.6785983445458467767, 0.6785983445458462215, -0.2810846377148228381 ) ) ;
#14734=CARTESIAN_POINT ( 'NONE',  ( 8.900000000000002132, 21.00000000000000000, -18.00000000000000355 ) ) ;
#14740=DIRECTION ( 'NONE',  ( 0.000000000000000000, 0.000000000000000000, -1.000000000000000000 ) ) ;
#14743=CARTESIAN_POINT ( 'NONE',  ( 49.00000000000000000, -0.2000000000089119934, 8.909539772616881237E-12 ) ) ;
#14745=VECTOR ( 'NONE', #15957, 1000.000000000000000 ) ;
#14754=DIRECTION ( 'NONE',  ( 0.000000000000000000, 0.000000000000000000, 1.000000000000000000 ) ) ;
#14756=( NAMED_UNIT ( * ) PLANE_ANGLE_UNIT ( ) SI_UNIT ( $, .RADIAN. ) );
#14762=DIRECTION ( 'NONE',  ( 0.000000000000000000, 0.000000000000000000, -1.000000000000000000 ) ) ;
#14764=DIRECTION ( 'NONE',  ( -0.7071067811865472397, -0.5000000000000002220, 0.5000000000000002220 ) ) ;
#14779=ORIENTED_EDGE ( 'NONE', *, *, #27692, .F. ) ;
#14781=EDGE_CURVE ( 'NONE', #62375, #54885, #51514, .T. ) ;
#14789=VERTEX_POINT ( 'NONE', #69818 ) ;
#14790=EDGE_CURVE ( 'NONE', #21838, #30889, #59403, .T. ) ;
#14794=EDGE_CURVE ( 'NONE', #67236, #28, #9743, .T. ) ;
#14808=DIRECTION ( 'NONE',  ( 0.000000000000000000, -0.7071067811865474617, -0.7071067811865474617 ) ) ;
#14812=AXIS2_PLACEMENT_3D ( 'NONE', #36354, #10189, #64288 ) ;
#14814=SURFACE_STYLE_USAGE ( .BOTH. , #30372 ) ;
#14818=LINE ( 'NONE', #10550, #59170 ) ;
#14827=( NAMED_UNIT ( * ) PLANE_ANGLE_UNIT ( ) SI_UNIT ( $, .RADIAN. ) );
#14830=ADVANCED_FACE ( 'NONE', ( #25988 ), #37641, .F. ) ;
#14833=ADVANCED_FACE ( 'NONE', ( #63108 ), #42586, .T. ) ;
#14836=CARTESIAN_POINT ( 'NONE',  ( 34.89999999999999858, 13.66939075806899240, -20.79999999999999361 ) ) ;
#14840=EDGE_CURVE ( 'NONE', #23983, #427, #47546, .T. ) ;
#14847=LINE ( 'NONE', #4248, #16291 ) ;
#14854=EDGE_LOOP ( 'NONE', ( #66415, #64987, #61117, #24936 ) ) ;
#14861=VERTEX_POINT ( 'NONE', #42232 ) ;
#14867=PLANE ( 'NONE',  #41492 ) ;
#14876=ORIENTED_EDGE ( 'NONE', *, *, #43802, .F. ) ;
#14879=EDGE_CURVE ( 'NONE', #16920, #7564, #52504, .T. ) ;
#14882=LINE ( 'NONE', #42447, #32683 ) ;
#14883=( GEOMETRIC_REPRESENTATION_CONTEXT ( 3 ) GLOBAL_UNCERTAINTY_ASSIGNED_CONTEXT ( ( #58553 ) ) GLOBAL_UNIT_ASSIGNED_CONTEXT ( ( #39233, #60449, #7044 ) ) REPRESENTATION_CONTEXT ( 'NONE', 'WORKASPACE' ) );
#14884=EDGE_CURVE ( 'NONE', #51374, #33533, #10416, .T. ) ;
#14888=PLANE ( 'NONE',  #62777 ) ;
#14891=CLOSED_SHELL ( 'NONE', ( #58479, #12250, #9536, #59911, #24618, #35601 ) ) ;
#14899=FILL_AREA_STYLE ('',( #53092 ) ) ;
#14902=ORIENTED_EDGE ( 'NONE', *, *, #41935, .F. ) ;
#14905=DIRECTION ( 'NONE',  ( -1.000000000000000000, 0.000000000000000000, 0.000000000000000000 ) ) ;
#14915=DIRECTION ( 'NONE',  ( 0.000000000000000000, 0.7071067811865474617, 0.7071067811865474617 ) ) ;
#14916=CARTESIAN_POINT ( 'NONE',  ( 25.90000000000000213, -0.2000000000089119934, 8.909539772616881237E-12 ) ) ;
#14936=DIRECTION ( 'NONE',  ( 1.000000000000000000, -0.000000000000000000, 0.000000000000000000 ) ) ;
#14942=VERTEX_POINT ( 'NONE', #27376 ) ;
#14980=EDGE_CURVE ( 'NONE', #16596, #62948, #54952, .T. ) ;
#15004=CARTESIAN_POINT ( 'NONE',  ( 22.90000000000000213, -0.2000000000089119934, -8.913009219568841313E-12 ) ) ;
#15007=FACE_OUTER_BOUND ( 'NONE', #65051, .T. ) ;
#15014=CARTESIAN_POINT ( 'NONE',  ( 24.90000000000000213, -14.06939075806902117, -20.80000000000000426 ) ) ;
#15016=EDGE_CURVE ( 'NONE', #4682, #38301, #33021, .T. ) ;
#15021=CARTESIAN_POINT ( 'NONE',  ( 49.00000000000000000, -0.2000000000089119934, -8.913009219568841313E-12 ) ) ;
#15028=ORIENTED_EDGE ( 'NONE', *, *, #66371, .T. ) ;
#15036=CARTESIAN_POINT ( 'NONE',  ( 21.90000000000000213, -0.2000000000089119934, -8.913009219568841313E-12 ) ) ;
#15043=FACE_OUTER_BOUND ( 'NONE', #42908, .T. ) ;
#15045=ADVANCED_FACE ( 'NONE', ( #21939 ), #47766, .F. ) ;
#15049=AXIS2_PLACEMENT_3D ( 'NONE', #36570, #38587, #65458 ) ;
#15055=ORIENTED_EDGE ( 'NONE', *, *, #57793, .F. ) ;
#15061=ORIENTED_EDGE ( 'NONE', *, *, #52068, .F. ) ;
#15068=AXIS2_PLACEMENT_3D ( 'NONE', #42847, #11364, #5729 ) ;
#15086=DIRECTION ( 'NONE',  ( 0.000000000000000000, 0.000000000000000000, -1.000000000000000000 ) ) ;
#15092=VECTOR ( 'NONE', #29187, 1000.000000000000000 ) ;
#15111=CARTESIAN_POINT ( 'NONE',  ( 49.00000000000000000, -21.00000000000000000, 13.86939075806900057 ) ) ;
#15115=CARTESIAN_POINT ( 'NONE',  ( 29.89999999999999858, 20.60000000000000142, 2.370429594502469981E-15 ) ) ;
#15122=EDGE_CURVE ( 'NONE', #9679, #32778, #37863, .T. ) ;
#15127=CARTESIAN_POINT ( 'NONE',  ( 14.89999999999999680, -14.06939075806902117, -20.80000000000000426 ) ) ;
#15130=DIRECTION ( 'NONE',  ( 1.000000000000000000, -0.000000000000000000, 0.000000000000000000 ) ) ;
#15131=LINE ( 'NONE', #63921, #15572 ) ;
#15137=ORIENTED_EDGE ( 'NONE', *, *, #18936, .T. ) ;
#15144=EDGE_CURVE ( 'NONE', #66965, #55486, #54970, .T. ) ;
#15151=DIRECTION ( 'NONE',  ( 0.000000000000000000, 0.000000000000000000, 1.000000000000000000 ) ) ;
#15155=CIRCLE ( 'NONE', #10654, 3.500000000000000000 ) ;
#15156=DIRECTION ( 'NONE',  ( -1.000000000000000000, 0.000000000000000000, 0.000000000000000000 ) ) ;
#15159=LINE ( 'NONE', #43407, #35782 ) ;
#15166=LINE ( 'NONE', #26126, #19973 ) ;
#15170=ORIENTED_EDGE ( 'NONE', *, *, #23572, .F. ) ;
#15172=CARTESIAN_POINT ( 'NONE',  ( 34.89999999999999858, 13.66939075806899240, 20.79999999999999361 ) ) ;
#15174=DIRECTION ( 'NONE',  ( 0.000000000000000000, -1.000000000000000000, 0.000000000000000000 ) ) ;
#15175=DIRECTION ( 'NONE',  ( 1.000000000000000000, -0.000000000000000000, 0.000000000000000000 ) ) ;
#15182=CARTESIAN_POINT ( 'NONE',  ( 41.09999999999999432, -21.00000000000000000, 14.57806571531351914 ) ) ;
#15183=ORIENTED_EDGE ( 'NONE', *, *, #20329, .F. ) ;
#15188=CARTESIAN_POINT ( 'NONE',  ( 41.09999999999999432, -14.06939075806900163, 20.80000000000000426 ) ) ;
#15189=ORIENTED_EDGE ( 'NONE', *, *, #10543, .F. ) ;
#15195=DIRECTION ( 'NONE',  ( 1.000000000000000000, -0.000000000000000000, 0.000000000000000000 ) ) ;
#15197=EDGE_CURVE ( 'NONE', #38472, #51495, #67215, .T. ) ;
#15198=CARTESIAN_POINT ( 'NONE',  ( 22.90000000000000213, 0.000000000000000000, 1.508455196501571824E-15 ) ) ;
#15215=ORIENTED_EDGE ( 'NONE', *, *, #46151, .T. ) ;
#15226=CARTESIAN_POINT ( 'NONE',  ( 36.90000000000000568, -21.00000000000000000, 13.86939075806900057 ) ) ;
#15234=DIRECTION ( 'NONE',  ( 1.000000000000000000, -0.000000000000000000, 0.000000000000000000 ) ) ;
#15241=ORIENTED_EDGE ( 'NONE', *, *, #51903, .F. ) ;
#15243=LINE ( 'NONE', #52741, #28563 ) ;
#15250=CARTESIAN_POINT ( 'NONE',  ( 18.89999999999999858, -14.06939075806900874, 20.80000000000001137 ) ) ;
#15266=EDGE_CURVE ( 'NONE', #18370, #427, #33493, .T. ) ;
#15269=DIRECTION ( 'NONE',  ( 0.000000000000000000, 0.000000000000000000, -1.000000000000000000 ) ) ;
#15276=ORIENTED_EDGE ( 'NONE', *, *, #68542, .F. ) ;
#15277=DIRECTION ( 'NONE',  ( 1.000000000000000000, 0.000000000000000000, 0.000000000000000000 ) ) ;
#15279=ADVANCED_FACE ( 'NONE', ( #1407 ), #68481, .F. ) ;
#15291=CARTESIAN_POINT ( 'NONE',  ( 49.00000000000000000, -0.1999999999911430404, -8.864436962241481021E-12 ) ) ;
#15295=ORIENTED_EDGE ( 'NONE', *, *, #28569, .T. ) ;
#15302=PLANE ( 'NONE',  #2922 ) ;
#15304=CARTESIAN_POINT ( 'NONE',  ( 0.000000000000000000, 0.7500000000000000000, 0.000000000000000000 ) ) ;
#15320=DIRECTION ( 'NONE',  ( 1.000000000000000000, -0.000000000000000000, 0.000000000000000000 ) ) ;
#15328=ORIENTED_EDGE ( 'NONE', *, *, #7516, .F. ) ;
#15330=DIRECTION ( 'NONE',  ( 0.000000000000000000, 0.000000000000000000, -1.000000000000000000 ) ) ;
#15335=EDGE_LOOP ( 'NONE', ( #46690, #62159, #55508, #13641 ) ) ;
#15349=CARTESIAN_POINT ( 'NONE',  ( 0.5000000000000000000, 18.00000000000000355, 21.00000000000000000 ) ) ;
#15350=FILL_AREA_STYLE_COLOUR ( '', #44722 ) ;
#15355=VECTOR ( 'NONE', #10685, 1000.000000000000000 ) ;
#15358=CIRCLE ( 'NONE', #22168, 24.99999999998794920 ) ;
#15361=( LENGTH_UNIT ( ) NAMED_UNIT ( * ) SI_UNIT ( .MILLI., .METRE. ) );
#15371=CARTESIAN_POINT ( 'NONE',  ( 27.00000000000000000, 0.000000000000000000, 0.000000000000000000 ) ) ;
#15377=FILL_AREA_STYLE_COLOUR ( '', #57999 ) ;
#15380=ORIENTED_EDGE ( 'NONE', *, *, #38715, .F. ) ;
#15384=CARTESIAN_POINT ( 'NONE',  ( 41.09999999999999432, 13.66939075806899950, 20.80000000000000426 ) ) ;
#15393=VERTEX_POINT ( 'NONE', #67157 ) ;
#15397=DIRECTION ( 'NONE',  ( 0.000000000000000000, 0.000000000000000000, 1.000000000000000000 ) ) ;
#15401=ORIENTED_EDGE ( 'NONE', *, *, #46515, .F. ) ;
#15410=ORIENTED_EDGE ( 'NONE', *, *, #25409, .F. ) ;
#15411=ORIENTED_EDGE ( 'NONE', *, *, #51764, .F. ) ;
#15413=LINE ( 'NONE', #53944, #36100 ) ;
#15414=UNCERTAINTY_MEASURE_WITH_UNIT (LENGTH_MEASURE( 1.000000000000000082E-05 ), #53713, 'distance_accuracy_value', 'NONE');
#15422=ORIENTED_EDGE ( 'NONE', *, *, #64991, .F. ) ;
#15429=STYLED_ITEM ( 'NONE', ( #64157 ), #19898 ) ;
#15431=ORIENTED_EDGE ( 'NONE', *, *, #53991, .F. ) ;
#15434=DIRECTION ( 'NONE',  ( 1.000000000000000000, -0.000000000000000000, 0.000000000000000000 ) ) ;
#15455=CARTESIAN_POINT ( 'NONE',  ( 47.00000000000000000, 0.7500000000000000000, -4.943429983321300014 ) ) ;
#15467=CYLINDRICAL_SURFACE ( 'NONE', #54310, 24.99999999998789946 ) ;
#15472=CARTESIAN_POINT ( 'NONE',  ( 49.00000000000000000, -0.2000000000089119934, 8.909539772616881237E-12 ) ) ;
#15478=ORIENTED_EDGE ( 'NONE', *, *, #35522, .T. ) ;
#15481=ORIENTED_EDGE ( 'NONE', *, *, #16645, .F. ) ;
#15490=VERTEX_POINT ( 'NONE', #57602 ) ;
#15520=ORIENTED_EDGE ( 'NONE', *, *, #43110, .F. ) ;
#15539=CARTESIAN_POINT ( 'NONE',  ( 46.39999999999999858, 21.00000000000000000, 0.7500000000000000000 ) ) ;
#15542=CARTESIAN_POINT ( 'NONE',  ( 41.09999999999999432, -14.06939075806901940, -20.80000000000000426 ) ) ;
#15546=AXIS2_PLACEMENT_3D ( 'NONE', #26145, #47700, #57608 ) ;
#15553=FACE_OUTER_BOUND ( 'NONE', #50002, .T. ) ;
#15568=ORIENTED_EDGE ( 'NONE', *, *, #19802, .T. ) ;
#15572=VECTOR ( 'NONE', #37055, 1000.000000000000000 ) ;
#15573=CARTESIAN_POINT ( 'NONE',  ( 21.90000000000000213, 20.60000000000000142, 13.86939075806899702 ) ) ;
#15583=CARTESIAN_POINT ( 'NONE',  ( 14.89999999999999680, -0.2000000000089119934, 8.909539772616881237E-12 ) ) ;
#15586=CARTESIAN_POINT ( 'NONE',  ( 40.90000000000000568, 0.000000000000000000, 3.447897592003593022E-15 ) ) ;
#15597=EDGE_CURVE ( 'NONE', #22670, #32725, #5273, .T. ) ;
#15611=ORIENTED_EDGE ( 'NONE', *, *, #44869, .F. ) ;
#15612=DIRECTION ( 'NONE',  ( -1.000000000000000000, 0.000000000000000000, 0.000000000000000000 ) ) ;
#15618=CARTESIAN_POINT ( 'NONE',  ( 46.39999999999999858, 21.00000000000000000, 2.750000000000000444 ) ) ;
#15629=ORIENTED_EDGE ( 'NONE', *, *, #41885, .F. ) ;
#15630=CARTESIAN_POINT ( 'NONE',  ( 24.90000000000000213, -0.2000000000089119934, -8.913009219568841313E-12 ) ) ;
#15631=DIRECTION ( 'NONE',  ( 1.000000000000000000, -0.000000000000000000, 0.000000000000000000 ) ) ;
#15636=EDGE_CURVE ( 'NONE', #34243, #18370, #26480, .T. ) ;
#15649=ORIENTED_EDGE ( 'NONE', *, *, #4465, .F. ) ;
#15657=PLANE ( 'NONE',  #41090 ) ;
#15664=PLANE ( 'NONE',  #7237 ) ;
#15666=AXIS2_PLACEMENT_3D ( 'NONE', #55949, #66219, #17778 ) ;
#15679=VERTEX_POINT ( 'NONE', #21182 ) ;
#15683=DIRECTION ( 'NONE',  ( 1.000000000000000000, -0.000000000000000000, 0.000000000000000000 ) ) ;
#15691=ORIENTED_EDGE ( 'NONE', *, *, #57755, .F. ) ;
#15695=PLANE ( 'NONE',  #719 ) ;
#15697=DIRECTION ( 'NONE',  ( 1.000000000000000000, 0.000000000000000000, 0.000000000000000000 ) ) ;
#15711=AXIS2_PLACEMENT_3D ( 'NONE', #55775, #2721, #62112 ) ;
#15725=DIRECTION ( 'NONE',  ( 0.000000000000000000, 0.000000000000000000, 1.000000000000000000 ) ) ;
#15730=LINE ( 'NONE', #58159, #40780 ) ;
#15755=CARTESIAN_POINT ( 'NONE',  ( 22.90000000000000213, 20.60000000000000142, -13.86939075806900057 ) ) ;
#15763=CARTESIAN_POINT ( 'NONE',  ( 35.89999999999999858, -21.00000000000001421, -13.86939075806900945 ) ) ;
#15777=CARTESIAN_POINT ( 'NONE',  ( 39.00000000000000000, 6.123233995736766282E-16, -5.000000000000000000 ) ) ;
#15792=CARTESIAN_POINT ( 'NONE',  ( 12.90000000000000213, -0.2000000000089119934, -8.913009219568841313E-12 ) ) ;
#15793=ORIENTED_EDGE ( 'NONE', *, *, #3218, .F. ) ;
#15817=CYLINDRICAL_SURFACE ( 'NONE', #13657, 2.458500000000000796 ) ;
#15830=ORIENTED_EDGE ( 'NONE', *, *, #41450, .F. ) ;
#15843=CIRCLE ( 'NONE', #55361, 3.500000000000000000 ) ;
#15848=AXIS2_PLACEMENT_3D ( 'NONE', #15111, #57532, #37376 ) ;
#15851=EDGE_CURVE ( 'NONE', #49922, #11420, #69709, .T. ) ;
#15858=CARTESIAN_POINT ( 'NONE',  ( 55.00000000000000000, -21.00000000000000000, -16.96999999999999886 ) ) ;
#15872=DIRECTION ( 'NONE',  ( 0.000000000000000000, 1.000000000000000000, -0.000000000000000000 ) ) ;
#15890=AXIS2_PLACEMENT_3D ( 'NONE', #30802, #9585, #25148 ) ;
#15896=ORIENTED_EDGE ( 'NONE', *, *, #67493, .F. ) ;
#15909=AXIS2_PLACEMENT_3D ( 'NONE', #21723, #33373, #27031 ) ;
#15911=FACE_OUTER_BOUND ( 'NONE', #32318, .T. ) ;
#15913=CARTESIAN_POINT ( 'NONE',  ( 28.90000000000000213, 20.60000000000000142, -13.86939075806900057 ) ) ;
#15932=LINE ( 'NONE', #365, #46979 ) ;
#15933=ORIENTED_EDGE ( 'NONE', *, *, #20903, .F. ) ;
#15942=VECTOR ( 'NONE', #28357, 1000.000000000000000 ) ;
#15957=DIRECTION ( 'NONE',  ( 0.000000000000000000, 1.000000000000000000, -0.000000000000000000 ) ) ;
#15974=CARTESIAN_POINT ( 'NONE',  ( 10.00000000000000000, 21.00000000000000000, 18.00000000000000355 ) ) ;
#15983=CARTESIAN_POINT ( 'NONE',  ( 8.900000000000005684, 14.08845687959340154, 20.99999999999999645 ) ) ;
#16000=EDGE_CURVE ( 'NONE', #22473, #14048, #32732, .T. ) ;
#16001=CARTESIAN_POINT ( 'NONE',  ( 10.90000000000000036, -21.00000000000000000, 13.86939075806900057 ) ) ;
#16004=EDGE_LOOP ( 'NONE', ( #40994, #39769, #55904, #30480 ) ) ;
#16007=VERTEX_POINT ( 'NONE', #53283 ) ;
#16009=AXIS2_PLACEMENT_3D ( 'NONE', #29349, #66492, #18047 ) ;
#16012=CLOSED_SHELL ( 'NONE', ( #40494, #55754, #48275, #41647, #54638, #20062 ) ) ;
#16024=DIRECTION ( 'NONE',  ( 1.000000000000000000, 0.000000000000000000, 0.000000000000000000 ) ) ;
#16029=EDGE_CURVE ( 'NONE', #24345, #45256, #26855, .T. ) ;
#16032=ADVANCED_FACE ( 'NONE', ( #22134 ), #5873, .F. ) ;
#16054=ORIENTED_EDGE ( 'NONE', *, *, #12175, .T. ) ;
#16055=B_SPLINE_CURVE_WITH_KNOTS ( 'NONE', 3,
 ( #24901, #7223, #29150, #40461 ),
 .UNSPECIFIED., .F., .F.,
 ( 4, 4 ),
 ( -0.001424424334280369533, 0.0007144698416513659174 ),
 .UNSPECIFIED. ) ;
#16056=LINE ( 'NONE', #58843, #27995 ) ;
#16073=EDGE_CURVE ( 'NONE', #45421, #58100, #25692, .T. ) ;
#16088=VECTOR ( 'NONE', #68566, 1000.000000000000114 ) ;
#16103=DIRECTION ( 'NONE',  ( -1.000000000000000000, 0.000000000000000000, 0.000000000000000000 ) ) ;
#16107=VECTOR ( 'NONE', #41552, 1000.000000000000000 ) ;
#16125=VECTOR ( 'NONE', #58855, 1000.000000000000000 ) ;
#16159=AXIS2_PLACEMENT_3D ( 'NONE', #63550, #58596, #27106 ) ;
#16161=ORIENTED_EDGE ( 'NONE', *, *, #63689, .F. ) ;
#16171=VECTOR ( 'NONE', #60787, 1000.000000000000000 ) ;
#16172=VERTEX_POINT ( 'NONE', #41079 ) ;
#16186=DIRECTION ( 'NONE',  ( -1.000000000000000000, 0.000000000000000000, 0.000000000000000000 ) ) ;
#16195=CARTESIAN_POINT ( 'NONE',  ( 38.90000000000000568, 0.000000000000000000, 0.000000000000000000 ) ) ;
#16207=AXIS2_PLACEMENT_3D ( 'NONE', #54197, #60171, #11723 ) ;
#16215=( NAMED_UNIT ( * ) SI_UNIT ( $, .STERADIAN. ) SOLID_ANGLE_UNIT ( ) );
#16218=CARTESIAN_POINT ( 'NONE',  ( 25.90000000000000213, 13.66939075806899240, -20.79999999999999361 ) ) ;
#16222=CARTESIAN_POINT ( 'NONE',  ( 8.900000000000002132, -18.00000000000000355, -21.00000000000000000 ) ) ;
#16227=DIRECTION ( 'NONE',  ( -1.000000000000000000, 0.000000000000000000, 0.000000000000000000 ) ) ;
#16230=DIRECTION ( 'NONE',  ( -1.000000000000000000, 0.000000000000000000, 0.000000000000000000 ) ) ;
#16232=EDGE_CURVE ( 'NONE', #63246, #38926, #44029, .T. ) ;
#16236=EDGE_CURVE ( 'NONE', #4872, #2943, #50992, .T. ) ;
#16243=EDGE_CURVE ( 'NONE', #24345, #62375, #36852, .T. ) ;
#16249=CARTESIAN_POINT ( 'NONE',  ( 39.90000000000000568, 0.000000000000000000, 3.500000000000000000 ) ) ;
#16261=DIRECTION ( 'NONE',  ( -1.000000000000000000, 0.000000000000000000, 0.000000000000000000 ) ) ;
#16275=EDGE_LOOP ( 'NONE', ( #58537, #15215, #40426, #35425 ) ) ;
#16283=CIRCLE ( 'NONE', #55794, 24.99999999998784972 ) ;
#16285=ORIENTED_EDGE ( 'NONE', *, *, #35241, .F. ) ;
#16287=EDGE_LOOP ( 'NONE', ( #43026, #62205, #19694, #37467 ) ) ;
#16291=VECTOR ( 'NONE', #3886, 1000.000000000000000 ) ;
#16294=CARTESIAN_POINT ( 'NONE',  ( 8.900000000000002132, -18.00000000000000355, -21.00000000000000000 ) ) ;
#16304=VECTOR ( 'NONE', #11721, 1000.000000000000000 ) ;
#16315=CYLINDRICAL_SURFACE ( 'NONE', #62825, 24.99999999998784972 ) ;
#16318=DIRECTION ( 'NONE',  ( 0.000000000000000000, -1.000000000000000000, 0.000000000000000000 ) ) ;
#16347=EDGE_LOOP ( 'NONE', ( #53156, #49609 ) ) ;
#16369=EDGE_CURVE ( 'NONE', #14861, #44485, #65899, .T. ) ;
#16372=EDGE_CURVE ( 'NONE', #51717, #23171, #3774, .T. ) ;
#16386=VERTEX_POINT ( 'NONE', #400 ) ;
#16394=EDGE_CURVE ( 'NONE', #10593, #7152, #65448, .T. ) ;
#16400=SURFACE_SIDE_STYLE ('',( #27014 ) ) ;
#16416=CARTESIAN_POINT ( 'NONE',  ( 32.89999999999999858, -0.1999999999911795112, 8.826273045769999343E-12 ) ) ;
#16426=AXIS2_PLACEMENT_3D ( 'NONE', #52491, #29860, #41526 ) ;
#16444=DIRECTION ( 'NONE',  ( 0.000000000000000000, 0.000000000000000000, -1.000000000000000000 ) ) ;
#16445=VERTEX_POINT ( 'NONE', #27613 ) ;
#16463=AXIS2_PLACEMENT_3D ( 'NONE', #26464, #52646, #59330 ) ;
#16476=CIRCLE ( 'NONE', #55985, 24.99999999998789946 ) ;
#16477=CARTESIAN_POINT ( 'NONE',  ( 0.5000000000000000000, 18.00000000000000355, 21.00000000000000000 ) ) ;
#16493=CARTESIAN_POINT ( 'NONE',  ( 31.89999999999999858, -14.06939075806900874, 20.80000000000001137 ) ) ;
#16495=AXIS2_PLACEMENT_3D ( 'NONE', #28480, #61003, #12563 ) ;
#16504=CIRCLE ( 'NONE', #68441, 0.5000000000000000000 ) ;
#16518=ORIENTED_EDGE ( 'NONE', *, *, #17384, .F. ) ;
#16528=CYLINDRICAL_SURFACE ( 'NONE', #65479, 25.39999999999999858 ) ;
#16529=DIRECTION ( 'NONE',  ( 0.000000000000000000, -1.000000000000000000, 0.000000000000000000 ) ) ;
#16538=CARTESIAN_POINT ( 'NONE',  ( 41.09999999999999432, -21.00000000000000000, 13.86939075806900057 ) ) ;
#16541=( GEOMETRIC_REPRESENTATION_CONTEXT ( 3 ) GLOBAL_UNCERTAINTY_ASSIGNED_CONTEXT ( ( #30968 ) ) GLOBAL_UNIT_ASSIGNED_CONTEXT ( ( #9341, #58837, #63083 ) ) REPRESENTATION_CONTEXT ( 'NONE', 'WORKASPACE' ) );
#16543=ADVANCED_FACE ( 'NONE', ( #30042 ), #61154, .T. ) ;
#16544=DIRECTION ( 'NONE',  ( -1.000000000000000000, 0.000000000000000000, 0.000000000000000000 ) ) ;
#16564=AXIS2_PLACEMENT_3D ( 'NONE', #38643, #17408, #60544 ) ;
#16580=DIRECTION ( 'NONE',  ( 0.000000000000000000, 0.000000000000000000, 1.000000000000000000 ) ) ;
#16584=CARTESIAN_POINT ( 'NONE',  ( 49.00000000000000000, -21.00000000000000000, 13.86939075806900057 ) ) ;
#16596=VERTEX_POINT ( 'NONE', #34279 ) ;
#16600=EDGE_CURVE ( 'NONE', #60100, #60377, #53517, .T. ) ;
#16602=EDGE_CURVE ( 'NONE', #15679, #35535, #23003, .T. ) ;
#16609=VERTEX_POINT ( 'NONE', #67169 ) ;
#16616=CARTESIAN_POINT ( 'NONE',  ( 26.90000000000000213, -14.06939075806900163, -20.80000000000000426 ) ) ;
#16620=ORIENTED_EDGE ( 'NONE', *, *, #37530, .T. ) ;
#16624=DIRECTION ( 'NONE',  ( -1.000000000000000000, 0.000000000000000000, 0.000000000000000000 ) ) ;
#16630=ORIENTED_EDGE ( 'NONE', *, *, #53658, .T. ) ;
#16645=EDGE_CURVE ( 'NONE', #46863, #51495, #56563, .T. ) ;
#16650=ORIENTED_EDGE ( 'NONE', *, *, #7023, .T. ) ;
#16682=AXIS2_PLACEMENT_3D ( 'NONE', #11497, #21082, #16825 ) ;
#16686=ORIENTED_EDGE ( 'NONE', *, *, #35755, .F. ) ;
#16687=FACE_OUTER_BOUND ( 'NONE', #49250, .T. ) ;
#16698=CARTESIAN_POINT ( 'NONE',  ( 41.09999999999999432, 13.66939075806899950, -20.80000000000000426 ) ) ;
#16709=EDGE_CURVE ( 'NONE', #7460, #1302, #64327, .T. ) ;
#16739=DIRECTION ( 'NONE',  ( -1.000000000000000000, 0.000000000000000000, 0.000000000000000000 ) ) ;
#16746=ORIENTED_EDGE ( 'NONE', *, *, #21042, .F. ) ;
#16754=LINE ( 'NONE', #33008, #35858 ) ;
#16759=DIRECTION ( 'NONE',  ( 1.000000000000000000, -0.000000000000000000, 0.000000000000000000 ) ) ;
#16767=EDGE_CURVE ( 'NONE', #7560, #37330, #37113, .T. ) ;
#16791=VERTEX_POINT ( 'NONE', #63273 ) ;
#16798=EDGE_CURVE ( 'NONE', #8221, #64619, #5003, .T. ) ;
#16803=UNCERTAINTY_MEASURE_WITH_UNIT (LENGTH_MEASURE( 1.000000000000000082E-05 ), #34449, 'distance_accuracy_value', 'NONE');
#16821=LINE ( 'NONE', #38051, #26856 ) ;
#16825=DIRECTION ( 'NONE',  ( 0.000000000000000000, 0.000000000000000000, -1.000000000000000000 ) ) ;
#16834=CARTESIAN_POINT ( 'NONE',  ( 39.90000000000000568, -14.06939075806900874, 20.80000000000001137 ) ) ;
#16836=ORIENTED_EDGE ( 'NONE', *, *, #60550, .T. ) ;
#16839=DIRECTION ( 'NONE',  ( 0.000000000000000000, 0.000000000000000000, -1.000000000000000000 ) ) ;
#16845=VERTEX_POINT ( 'NONE', #16222 ) ;
#16852=ADVANCED_FACE ( 'NONE', ( #22235 ), #27528, .T. ) ;
#16867=LINE ( 'NONE', #65649, #35883 ) ;
#16871=CARTESIAN_POINT ( 'NONE',  ( 41.09999999999999432, -0.2000000000000000111, 0.000000000000000000 ) ) ;
#16889=EDGE_LOOP ( 'NONE', ( #53109, #15055, #29342, #67810, #68772, #47785, #27332, #43367 ) ) ;
#16894=AXIS2_PLACEMENT_3D ( 'NONE', #48334, #63903, #63556 ) ;
#16897=CARTESIAN_POINT ( 'NONE',  ( 16.89999999999999858, -0.2000000000089119934, -8.913009219568841313E-12 ) ) ;
#16899=LINE ( 'NONE', #48383, #22964 ) ;
#16904=LINE ( 'NONE', #46540, #26282 ) ;
#16909=ORIENTED_EDGE ( 'NONE', *, *, #59209, .F. ) ;
#16910=CARTESIAN_POINT ( 'NONE',  ( 11.90000000000000036, 20.60000000000000142, -13.86939075806900057 ) ) ;
#16919=DIRECTION ( 'NONE',  ( -1.000000000000000000, 0.000000000000000000, 0.000000000000000000 ) ) ;
#16920=VERTEX_POINT ( 'NONE', #44812 ) ;
#16926=DIRECTION ( 'NONE',  ( -1.000000000000000000, 0.000000000000000000, 0.000000000000000000 ) ) ;
#16946=CARTESIAN_POINT ( 'NONE',  ( 49.00000000000000000, -0.2000000000089119934, -8.913009219568841313E-12 ) ) ;
#16978=DIRECTION ( 'NONE',  ( 0.000000000000000000, 0.000000000000000000, -1.000000000000000000 ) ) ;
#16994=VECTOR ( 'NONE', #21605, 1000.000000000000000 ) ;
#17000=ORIENTED_EDGE ( 'NONE', *, *, #43585, .F. ) ;
#17010=FACE_BOUND ( 'NONE', #2829, .T. ) ;
#17014=ADVANCED_FACE ( 'NONE', ( #18996 ), #1678, .T. ) ;
#17020=DIRECTION ( 'NONE',  ( 0.000000000000000000, 0.000000000000000000, -1.000000000000000000 ) ) ;
#17033=CARTESIAN_POINT ( 'NONE',  ( 39.90000000000000568, -21.00000000000001421, -13.86939075806900945 ) ) ;
#17050=VERTEX_POINT ( 'NONE', #51168 ) ;
#17053=DIRECTION ( 'NONE',  ( -0.000000000000000000, -1.000000000000000000, 0.000000000000000000 ) ) ;
#17059=CARTESIAN_POINT ( 'NONE',  ( 32.89999999999999858, -0.1999999999911430404, -8.864436962241481021E-12 ) ) ;
#17061=ORIENTED_EDGE ( 'NONE', *, *, #36832, .F. ) ;
#17073=PLANE ( 'NONE',  #16564 ) ;
#17075=DIRECTION ( 'NONE',  ( 0.000000000000000000, 1.000000000000000000, 0.000000000000000000 ) ) ;
#17078=ORIENTED_EDGE ( 'NONE', *, *, #39085, .F. ) ;
#17083=CARTESIAN_POINT ( 'NONE',  ( 19.90000000000000213, 0.000000000000000000, 1.292961597001347137E-15 ) ) ;
#17090=( GEOMETRIC_REPRESENTATION_CONTEXT ( 3 ) GLOBAL_UNCERTAINTY_ASSIGNED_CONTEXT ( ( #22455 ) ) GLOBAL_UNIT_ASSIGNED_CONTEXT ( ( #1482, #7127, #18085 ) ) REPRESENTATION_CONTEXT ( 'NONE', 'WORKASPACE' ) );
#17097=ORIENTED_EDGE ( 'NONE', *, *, #39820, .T. ) ;
#17103=ORIENTED_EDGE ( 'NONE', *, *, #64960, .F. ) ;
#17136=ORIENTED_EDGE ( 'NONE', *, *, #42730, .T. ) ;
#17145=VERTEX_POINT ( 'NONE', #41615 ) ;
#17147=AXIS2_PLACEMENT_3D ( 'NONE', #47637, #21121, #64260 ) ;
#17148=CLOSED_SHELL ( 'NONE', ( #60638, #53205, #51983, #51181, #24773, #19438, #7199, #5948, #13627, #54003, #65363, #46058 ) ) ;
#17152=DIRECTION ( 'NONE',  ( 0.000000000000000000, -1.000000000000000000, 0.000000000000000000 ) ) ;
#17159=CARTESIAN_POINT ( 'NONE',  ( 46.39999999999999858, 33.00000000000000000, 0.7500000000000000000 ) ) ;
#17162=PLANE ( 'NONE',  #25252 ) ;
#17176=CIRCLE ( 'NONE', #68012, 5.000000000000000000 ) ;
#17193=ORIENTED_EDGE ( 'NONE', *, *, #60108, .F. ) ;
#17198=CARTESIAN_POINT ( 'NONE',  ( 11.90000000000000036, -0.1999999999911430404, -8.864436962241481021E-12 ) ) ;
#17199=ADVANCED_FACE ( 'NONE', ( #55032 ), #53985, .F. ) ;
#17207=DIRECTION ( 'NONE',  ( 1.000000000000000000, -0.000000000000000000, 0.000000000000000000 ) ) ;
#17211=EDGE_LOOP ( 'NONE', ( #67264, #65171, #46583, #40182 ) ) ;
#17219=AXIS2_PLACEMENT_3D ( 'NONE', #46133, #50040, #67700 ) ;
#17223=AXIS2_PLACEMENT_3D ( 'NONE', #60285, #56379, #13595 ) ;
#17226=CYLINDRICAL_SURFACE ( 'NONE', #48296, 24.99999999998784972 ) ;
#17228=VERTEX_POINT ( 'NONE', #16493 ) ;
#17229=ORIENTED_EDGE ( 'NONE', *, *, #5137, .T. ) ;
#17233=DIRECTION ( 'NONE',  ( -1.000000000000000000, 0.000000000000000000, 0.000000000000000000 ) ) ;
#17245=VECTOR ( 'NONE', #14339, 1000.000000000000000 ) ;
#17247=EDGE_CURVE ( 'NONE', #39291, #33489, #36632, .T. ) ;
#17260=CARTESIAN_POINT ( 'NONE',  ( 49.00000000000000000, -14.06939075806900163, -20.80000000000000426 ) ) ;
#17270=ORIENTED_EDGE ( 'NONE', *, *, #13085, .F. ) ;
#17274=DIRECTION ( 'NONE',  ( 1.000000000000000000, -0.000000000000000000, 0.000000000000000000 ) ) ;
#17277=VECTOR ( 'NONE', #12077, 1000.000000000000000 ) ;
#17282=EDGE_CURVE ( 'NONE', #33288, #44820, #69881, .T. ) ;
#17286=ORIENTED_EDGE ( 'NONE', *, *, #6514, .T. ) ;
#17291=DIRECTION ( 'NONE',  ( 1.000000000000000000, 0.000000000000000000, 0.000000000000000000 ) ) ;
#17299=CIRCLE ( 'NONE', #362, 25.39999999999999858 ) ;
#17308=AXIS2_PLACEMENT_3D ( 'NONE', #21782, #59617, #11161 ) ;
#17315=ORIENTED_EDGE ( 'NONE', *, *, #22534, .F. ) ;
#17316=DIRECTION ( 'NONE',  ( 0.000000000000000000, -0.8188976377952759123, 0.5739395950910837207 ) ) ;
#17350=ORIENTED_EDGE ( 'NONE', *, *, #16602, .F. ) ;
#17359=FACE_OUTER_BOUND ( 'NONE', #54612, .T. ) ;
#17371=SURFACE_STYLE_FILL_AREA ( #33970 ) ;
#17376=ORIENTED_EDGE ( 'NONE', *, *, #58776, .F. ) ;
#17384=EDGE_CURVE ( 'NONE', #59658, #6660, #39985, .T. ) ;
#17393=ORIENTED_EDGE ( 'NONE', *, *, #62750, .F. ) ;
#17398=CARTESIAN_POINT ( 'NONE',  ( 41.09999999999999432, -14.06939075806901940, -20.80000000000000426 ) ) ;
#17408=DIRECTION ( 'NONE',  ( 0.000000000000000000, 0.000000000000000000, -1.000000000000000000 ) ) ;
#17409=FACE_BOUND ( 'NONE', #4700, .T. ) ;
#17418=DIRECTION ( 'NONE',  ( 0.000000000000000000, 0.000000000000000000, -1.000000000000000000 ) ) ;
#17429=EDGE_LOOP ( 'NONE', ( #64795, #51645 ) ) ;
#17456=CARTESIAN_POINT ( 'NONE',  ( 49.00000000000000000, -21.00000000000000000, 13.86939075806900057 ) ) ;
#17470=EDGE_LOOP ( 'NONE', ( #22877, #53654, #10680, #62884 ) ) ;
#17475=VERTEX_POINT ( 'NONE', #63811 ) ;
#17478=CARTESIAN_POINT ( 'NONE',  ( 55.00000000000000000, 21.00000000000000000, 16.96999999999999886 ) ) ;
#17487=LINE ( 'NONE', #53000, #68980 ) ;
#17496=CARTESIAN_POINT ( 'NONE',  ( 38.90000000000000568, 13.66939075806899240, 20.79999999999999361 ) ) ;
#17502=VECTOR ( 'NONE', #1720, 1000.000000000000000 ) ;
#17507=VECTOR ( 'NONE', #51033, 1000.000000000000114 ) ;
#17508=DIRECTION ( 'NONE',  ( 0.000000000000000000, -0.7071067811865475727, -0.7071067811865475727 ) ) ;
#17519=DIRECTION ( 'NONE',  ( 0.000000000000000000, 0.7071067811865475727, 0.7071067811865475727 ) ) ;
#17531=CARTESIAN_POINT ( 'NONE',  ( 27.90000000000000213, 20.60000000000000142, -13.86939075806900057 ) ) ;
#17536=DIRECTION ( 'NONE',  ( 0.000000000000000000, 0.000000000000000000, -1.000000000000000000 ) ) ;
#17545=VECTOR ( 'NONE', #6612, 1000.000000000000000 ) ;
#17564=VERTEX_POINT ( 'NONE', #52502 ) ;
#17581=CARTESIAN_POINT ( 'NONE',  ( 49.00000000000000000, 13.66939075806899950, 20.80000000000000426 ) ) ;
#17585=CARTESIAN_POINT ( 'NONE',  ( 35.89999999999999858, 20.60000000000000142, -13.86939075806900057 ) ) ;
#17590=DIRECTION ( 'NONE',  ( 1.000000000000000000, -0.000000000000000000, 0.000000000000000000 ) ) ;
#17591=EDGE_CURVE ( 'NONE', #19691, #33306, #43483, .T. ) ;
#17593=VECTOR ( 'NONE', #25233, 1000.000000000000000 ) ;
#17597=DIRECTION ( 'NONE',  ( 1.000000000000000000, -0.000000000000000000, 0.000000000000000000 ) ) ;
#17598=AXIS2_PLACEMENT_3D ( 'NONE', #65972, #44395, #17536 ) ;
#17623=EDGE_LOOP ( 'NONE', ( #64345, #44022, #50954, #5759 ) ) ;
#17628=DIRECTION ( 'NONE',  ( 0.000000000000000000, 1.000000000000000000, -0.000000000000000000 ) ) ;
#17637=CARTESIAN_POINT ( 'NONE',  ( 47.00000000000000000, -0.7500000000000000000, -4.943429983321300014 ) ) ;
#17640=ORIENTED_EDGE ( 'NONE', *, *, #4732, .T. ) ;
#17646=VECTOR ( 'NONE', #66, 1000.000000000000000 ) ;
#17662=CARTESIAN_POINT ( 'NONE',  ( 22.90000000000000213, -21.00000000000000000, 13.86939075806900057 ) ) ;
#17673=CARTESIAN_POINT ( 'NONE',  ( 49.00000000000000000, 0.000000000000000000, 0.000000000000000000 ) ) ;
#17684=FILL_AREA_STYLE_COLOUR ( '', #34456 ) ;
#17688=CARTESIAN_POINT ( 'NONE',  ( 7.899999999999999467, -21.00000000000000000, -14.57806571531351914 ) ) ;
#17692=ORIENTED_EDGE ( 'NONE', *, *, #68349, .F. ) ;
#17693=CARTESIAN_POINT ( 'NONE',  ( 41.09999999999999432, 13.66939075806899950, -20.80000000000000426 ) ) ;
#17702=CARTESIAN_POINT ( 'NONE',  ( 17.89999999999999858, 13.66939075806899240, -20.79999999999999361 ) ) ;
#17709=ORIENTED_EDGE ( 'NONE', *, *, #5439, .T. ) ;
#17720=EDGE_LOOP ( 'NONE', ( #2725, #54906, #48114, #36626 ) ) ;
#17726=ADVANCED_FACE ( 'NONE', ( #39011 ), #61250, .F. ) ;
#17741=CIRCLE ( 'NONE', #10986, 5.000000000000000000 ) ;
#17757=VERTEX_POINT ( 'NONE', #45001 ) ;
#17758=VERTEX_POINT ( 'NONE', #28066 ) ;
#17775=FACE_OUTER_BOUND ( 'NONE', #16275, .T. ) ;
#17776=CARTESIAN_POINT ( 'NONE',  ( 40.90000000000000568, 13.66939075806899950, 20.80000000000000426 ) ) ;
#17778=DIRECTION ( 'NONE',  ( 0.000000000000000000, 0.000000000000000000, -1.000000000000000000 ) ) ;
#17784=ORIENTED_EDGE ( 'NONE', *, *, #53930, .T. ) ;
#17788=PLANE ( 'NONE',  #52816 ) ;
#17794=VECTOR ( 'NONE', #8350, 1000.000000000000000 ) ;
#17820=ADVANCED_FACE ( 'NONE', ( #7166 ), #66576, .F. ) ;
#17835=DIRECTION ( 'NONE',  ( 0.000000000000000000, 0.000000000000000000, -1.000000000000000000 ) ) ;
#17838=DIRECTION ( 'NONE',  ( 1.000000000000000000, -0.000000000000000000, 0.000000000000000000 ) ) ;
#17841=DIRECTION ( 'NONE',  ( -1.000000000000000000, 0.000000000000000000, -0.000000000000000000 ) ) ;
#17849=EDGE_CURVE ( 'NONE', #68247, #4520, #37849, .T. ) ;
#17859=ADVANCED_FACE ( 'NONE', ( #51720 ), #52790, .F. ) ;
#17863=SURFACE_SIDE_STYLE ('',( #18202 ) ) ;
#17865=AXIS2_PLACEMENT_3D ( 'NONE', #32317, #37626, #10736 ) ;
#17874=LINE ( 'NONE', #59630, #57624 ) ;
#17883=ORIENTED_EDGE ( 'NONE', *, *, #69547, .F. ) ;
#17888=ORIENTED_EDGE ( 'NONE', *, *, #12007, .F. ) ;
#17899=DIRECTION ( 'NONE',  ( 0.000000000000000000, 0.000000000000000000, 1.000000000000000000 ) ) ;
#17900=CIRCLE ( 'NONE', #49557, 2.458500000000000796 ) ;
#17908=AXIS2_PLACEMENT_3D ( 'NONE', #37278, #69800, #21357 ) ;
#17909=DIRECTION ( 'NONE',  ( -1.000000000000000000, 0.000000000000000000, 0.000000000000000000 ) ) ;
#17919=ORIENTED_EDGE ( 'NONE', *, *, #50701, .T. ) ;
#17928=AXIS2_PLACEMENT_3D ( 'NONE', #30955, #42255, #15397 ) ;
#17944=LINE ( 'NONE', #12627, #57191 ) ;
#17946=VECTOR ( 'NONE', #34167, 1000.000000000000000 ) ;
#17950=PLANE ( 'NONE',  #56458 ) ;
#17967=DIRECTION ( 'NONE',  ( 0.000000000000000000, 0.000000000000000000, -1.000000000000000000 ) ) ;
#17973=FACE_OUTER_BOUND ( 'NONE', #11227, .T. ) ;
#17980=VERTEX_POINT ( 'NONE', #6324 ) ;
#17981=VECTOR ( 'NONE', #27968, 1000.000000000000000 ) ;
#17986=ADVANCED_FACE ( 'NONE', ( #48768 ), #329, .F. ) ;
#18005=ORIENTED_EDGE ( 'NONE', *, *, #55227, .F. ) ;
#18020=CARTESIAN_POINT ( 'NONE',  ( 49.00000000000000000, -21.00000000000000000, 13.86939075806900057 ) ) ;
#18023=EDGE_CURVE ( 'NONE', #56320, #27398, #54764, .T. ) ;
#18027=EDGE_LOOP ( 'NONE', ( #43758, #28251, #39680, #956 ) ) ;
#18028=DIRECTION ( 'NONE',  ( 1.000000000000000000, -0.000000000000000000, 0.000000000000000000 ) ) ;
#18029=LINE ( 'NONE', #29333, #50410 ) ;
#18040=EDGE_CURVE ( 'NONE', #8437, #68001, #21888, .T. ) ;
#18047=DIRECTION ( 'NONE',  ( 0.000000000000000000, 0.000000000000000000, -1.000000000000000000 ) ) ;
#18071=DIRECTION ( 'NONE',  ( 0.000000000000000000, 0.000000000000000000, 1.000000000000000000 ) ) ;
#18085=( NAMED_UNIT ( * ) SI_UNIT ( $, .STERADIAN. ) SOLID_ANGLE_UNIT ( ) );
#18099=ORIENTED_EDGE ( 'NONE', *, *, #18323, .F. ) ;
#18101=ADVANCED_FACE ( 'NONE', ( #22924 ), #54426, .T. ) ;
#18109=VECTOR ( 'NONE', #45663, 1000.000000000000000 ) ;
#18111=LINE ( 'NONE', #6808, #59714 ) ;
#18152=DIRECTION ( 'NONE',  ( 1.000000000000000000, -0.000000000000000000, 0.000000000000000000 ) ) ;
#18161=EDGE_LOOP ( 'NONE', ( #36473, #55317 ) ) ;
#18164=EDGE_LOOP ( 'NONE', ( #35112, #11779, #31225, #43629 ) ) ;
#18169=DIRECTION ( 'NONE',  ( 1.000000000000000000, -0.000000000000000000, 0.000000000000000000 ) ) ;
#18177=ORIENTED_EDGE ( 'NONE', *, *, #51394, .F. ) ;
#18181=VECTOR ( 'NONE', #58121, 1000.000000000000000 ) ;
#18186=COLOUR_RGB ( '', 0.08235294, 0.09019608, 0.10196078) ;
#18190=CARTESIAN_POINT ( 'NONE',  ( 25.57999999999999829, 0.000000000000000000, 0.000000000000000000 ) ) ;
#18195=EDGE_CURVE ( 'NONE', #7564, #4698, #8034, .T. ) ;
#18199=CARTESIAN_POINT ( 'NONE',  ( 41.09999999999999432, 20.60000000000000142, -13.86939075806900057 ) ) ;
#18202=SURFACE_STYLE_FILL_AREA ( #33772 ) ;
#18206=DIRECTION ( 'NONE',  ( 1.000000000000000000, -0.000000000000000000, 0.000000000000000000 ) ) ;
#18227=FACE_OUTER_BOUND ( 'NONE', #19835, .T. ) ;
#18236=MECHANICAL_DESIGN_GEOMETRIC_PRESENTATION_REPRESENTATION('',(#43086),#52124);
#18237=VERTEX_POINT ( 'NONE', #45880 ) ;
#18295=CARTESIAN_POINT ( 'NONE',  ( 8.900000000000002132, -18.00000000000000355, -21.00000000000000000 ) ) ;
#18307=EDGE_LOOP ( 'NONE', ( #54616, #30140, #52190, #12859, #15401, #48293, #10945, #38774, #42829, #64038, #36908, #11465, #43215, #60042, #26581, #26890 ) ) ;
#18311=CARTESIAN_POINT ( 'NONE',  ( 39.90000000000000568, 21.00000000000000355, 13.98999642601812354 ) ) ;
#18312=ORIENTED_EDGE ( 'NONE', *, *, #11665, .T. ) ;
#18313=EDGE_CURVE ( 'NONE', #44242, #67236, #46572, .T. ) ;
#18314=DIRECTION ( 'NONE',  ( 0.6785983445458448893, 0.2810846377148217834, -0.6785983445458485530 ) ) ;
#18323=EDGE_CURVE ( 'NONE', #60266, #16172, #9458, .T. ) ;
#18327=ORIENTED_EDGE ( 'NONE', *, *, #10469, .T. ) ;
#18338=DIRECTION ( 'NONE',  ( 1.000000000000000000, -0.000000000000000000, 0.000000000000000000 ) ) ;
#18341=CARTESIAN_POINT ( 'NONE',  ( 34.89999999999999858, -14.06939075806902117, -20.80000000000000426 ) ) ;
#18351=VECTOR ( 'NONE', #43079, 1000.000000000000000 ) ;
#18366=ORIENTED_EDGE ( 'NONE', *, *, #43131, .F. ) ;
#18370=VERTEX_POINT ( 'NONE', #69200 ) ;
#18374=SURFACE_STYLE_USAGE ( .BOTH. , #39263 ) ;
#18380=ORIENTED_EDGE ( 'NONE', *, *, #8236, .T. ) ;
#18385=DIRECTION ( 'NONE',  ( 0.000000000000000000, 0.000000000000000000, -1.000000000000000000 ) ) ;
#18403=ORIENTED_EDGE ( 'NONE', *, *, #29577, .F. ) ;
#18404=ORIENTED_EDGE ( 'NONE', *, *, #1657, .T. ) ;
#18407=COLOUR_RGB ( '', 0.40784314, 0.44705882, 0.49803922) ;
#18426=CIRCLE ( 'NONE', #57980, 25.39999999999999858 ) ;
#18443=VECTOR ( 'NONE', #63363, 1000.000000000000000 ) ;
#18450=STYLED_ITEM ( 'NONE', ( #50740 ), #66174 ) ;
#18451=CARTESIAN_POINT ( 'NONE',  ( 25.90000000000000213, 0.000000000000000000, 0.000000000000000000 ) ) ;
#18454=VERTEX_POINT ( 'NONE', #59640 ) ;
#18460=FILL_AREA_STYLE ('',( #63276 ) ) ;
#18480=CARTESIAN_POINT ( 'NONE',  ( 49.00000000000000000, -0.1999999999911795112, 8.826273045769999343E-12 ) ) ;
#18505=VECTOR ( 'NONE', #54253, 1000.000000000000000 ) ;
#18508=EDGE_LOOP ( 'NONE', ( #9380, #40857 ) ) ;
#18512=AXIS2_PLACEMENT_3D ( 'NONE', #15583, #37483, #32173 ) ;
#18514=CARTESIAN_POINT ( 'NONE',  ( 30.90000000000000213, -14.06939075806902117, -20.80000000000000426 ) ) ;
#18517=LINE ( 'NONE', #34420, #40211 ) ;
#18534=ADVANCED_FACE ( 'NONE', ( #22508 ), #38756, .T. ) ;
#18541=EDGE_CURVE ( 'NONE', #58826, #21251, #69599, .T. ) ;
#18544=VECTOR ( 'NONE', #49789, 1000.000000000000000 ) ;
#18545=VERTEX_POINT ( 'NONE', #34128 ) ;
#18564=PLANE ( 'NONE',  #58237 ) ;
#18577=DIRECTION ( 'NONE',  ( -1.000000000000000000, 0.000000000000000000, 0.000000000000000000 ) ) ;
#18580=DIRECTION ( 'NONE',  ( 0.000000000000000000, 0.000000000000000000, -1.000000000000000000 ) ) ;
#18583=CARTESIAN_POINT ( 'NONE',  ( 49.00000000000000000, -0.1999999999911795112, 8.826273045769999343E-12 ) ) ;
#18595=DIRECTION ( 'NONE',  ( 0.000000000000000000, 1.000000000000000000, 0.000000000000000000 ) ) ;
#18597=CARTESIAN_POINT ( 'NONE',  ( 46.39999999999999858, 21.00000000000000000, -1.750000000000000222 ) ) ;
#18608=DIRECTION ( 'NONE',  ( 0.000000000000000000, 1.000000000000000000, 0.000000000000000000 ) ) ;
#18612=DIRECTION ( 'NONE',  ( 0.000000000000000000, 0.000000000000000000, 1.000000000000000000 ) ) ;
#18621=FACE_OUTER_BOUND ( 'NONE', #36093, .T. ) ;
#18631=ADVANCED_FACE ( 'NONE', ( #29533 ), #6917, .F. ) ;
#18649=ORIENTED_EDGE ( 'NONE', *, *, #61874, .F. ) ;
#18653=AXIS2_PLACEMENT_3D ( 'NONE', #60417, #33557, #7016 ) ;
#18664=EDGE_CURVE ( 'NONE', #17757, #30300, #48146, .T. ) ;
#18667=( GEOMETRIC_REPRESENTATION_CONTEXT ( 3 ) GLOBAL_UNCERTAINTY_ASSIGNED_CONTEXT ( ( #536 ) ) GLOBAL_UNIT_ASSIGNED_CONTEXT ( ( #15361, #37281, #4755 ) ) REPRESENTATION_CONTEXT ( 'NONE', 'WORKASPACE' ) );
#18677=EDGE_LOOP ( 'NONE', ( #67107, #51038, #34551, #51906 ) ) ;
#18690=ORIENTED_EDGE ( 'NONE', *, *, #40272, .F. ) ;
#18694=VERTEX_POINT ( 'NONE', #19281 ) ;
#18704=SURFACE_STYLE_USAGE ( .BOTH. , #28276 ) ;
#18712=CARTESIAN_POINT ( 'NONE',  ( 7.900000000000000355, 18.00000000000000355, -21.00000000000000000 ) ) ;
#18719=CYLINDRICAL_SURFACE ( 'NONE', #49651, 24.99999999998784972 ) ;
#18724=AXIS2_PLACEMENT_3D ( 'NONE', #9182, #52320, #56653 ) ;
#18736=( NAMED_UNIT ( * ) SI_UNIT ( $, .STERADIAN. ) SOLID_ANGLE_UNIT ( ) );
#18744=ORIENTED_EDGE ( 'NONE', *, *, #66823, .F. ) ;
#18747=SURFACE_SIDE_STYLE ('',( #40666 ) ) ;
#18762=CYLINDRICAL_SURFACE ( 'NONE', #409, 24.99999999998784972 ) ;
#18770=DIRECTION ( 'NONE',  ( -0.7071067811865475727, 0.000000000000000000, -0.7071067811865475727 ) ) ;
#18774=AXIS2_PLACEMENT_3D ( 'NONE', #36273, #26028, #47582 ) ;
#18777=AXIS2_PLACEMENT_3D ( 'NONE', #39397, #45044, #35133 ) ;
#18778=CARTESIAN_POINT ( 'NONE',  ( 47.00000000000000000, 0.7500000000000000000, 3.418698582794335028 ) ) ;
#18783=DIRECTION ( 'NONE',  ( -1.000000000000000000, 0.000000000000000000, 0.000000000000000000 ) ) ;
#18787=CARTESIAN_POINT ( 'NONE',  ( 55.00000000000000000, 21.00000000000000000, -16.96999999999999886 ) ) ;
#18788=ORIENTED_EDGE ( 'NONE', *, *, #43183, .T. ) ;
#18795=DIRECTION ( 'NONE',  ( 0.000000000000000000, 0.000000000000000000, -1.000000000000000000 ) ) ;
#18802=VECTOR ( 'NONE', #59071, 1000.000000000000000 ) ;
#18818=ORIENTED_EDGE ( 'NONE', *, *, #51938, .T. ) ;
#18822=VECTOR ( 'NONE', #6023, 1000.000000000000000 ) ;
#18834=DIRECTION ( 'NONE',  ( 0.000000000000000000, 0.000000000000000000, 1.000000000000000000 ) ) ;
#18847=AXIS2_PLACEMENT_3D ( 'NONE', #18020, #34978, #45950 ) ;
#18867=EDGE_CURVE ( 'NONE', #8437, #35406, #5123, .T. ) ;
#18876=PRODUCT_DEFINITION ( 'UNKNOWN', '', #1908, #19027 ) ;
#18888=CARTESIAN_POINT ( 'NONE',  ( 36.90000000000000568, 13.66939075806899240, -20.79999999999999361 ) ) ;
#18910=LINE ( 'NONE', #51434, #9887 ) ;
#18917=CARTESIAN_POINT ( 'NONE',  ( 37.90000000000000568, 20.60000000000000142, -13.86939075806900057 ) ) ;
#18922=DIRECTION ( 'NONE',  ( 0.000000000000000000, 0.000000000000000000, 1.000000000000000000 ) ) ;
#18925=FACE_OUTER_BOUND ( 'NONE', #24329, .T. ) ;
#18926=CARTESIAN_POINT ( 'NONE',  ( 12.90000000000000213, -0.1999999999911430404, -8.864436962241481021E-12 ) ) ;
#18931=CARTESIAN_POINT ( 'NONE',  ( 29.89999999999999858, 0.000000000000000000, 0.000000000000000000 ) ) ;
#18936=EDGE_CURVE ( 'NONE', #40026, #10730, #42942, .T. ) ;
#18938=CARTESIAN_POINT ( 'NONE',  ( 38.90000000000000568, -21.00000000000000000, 13.86939075806900057 ) ) ;
#18942=CYLINDRICAL_SURFACE ( 'NONE', #60560, 2.458500000000000796 ) ;
#18943=ORIENTED_EDGE ( 'NONE', *, *, #7618, .F. ) ;
#18947=FACE_OUTER_BOUND ( 'NONE', #19424, .T. ) ;
#18948=DIRECTION ( 'NONE',  ( 0.000000000000000000, 0.000000000000000000, 1.000000000000000000 ) ) ;
#18954=DIRECTION ( 'NONE',  ( -1.000000000000000000, 0.000000000000000000, 0.000000000000000000 ) ) ;
#18956=ORIENTED_EDGE ( 'NONE', *, *, #6122, .F. ) ;
#18962=ADVANCED_FACE ( 'NONE', ( #66243 ), #45706, .F. ) ;
#18965=PLANE ( 'NONE',  #39670 ) ;
#18967=ORIENTED_EDGE ( 'NONE', *, *, #39286, .F. ) ;
#18974=FACE_OUTER_BOUND ( 'NONE', #62317, .T. ) ;
#18977=ORIENTED_EDGE ( 'NONE', *, *, #13541, .F. ) ;
#18979=LINE ( 'NONE', #3078, #44790 ) ;
#18980=CYLINDRICAL_SURFACE ( 'NONE', #10477, 25.39999999999999858 ) ;
#18996=FACE_OUTER_BOUND ( 'NONE', #41795, .T. ) ;
#19001=CYLINDRICAL_SURFACE ( 'NONE', #52540, 24.99999999998794920 ) ;
#19018=ADVANCED_FACE ( 'NONE', ( #6832 ), #23459, .T. ) ;
#19027=PRODUCT_DEFINITION_CONTEXT ( 'detailed design', #9255, 'design' ) ;
#19034=DIRECTION ( 'NONE',  ( -1.000000000000000000, 0.000000000000000000, 0.000000000000000000 ) ) ;
#19037=ORIENTED_EDGE ( 'NONE', *, *, #47050, .T. ) ;
#19042=EDGE_LOOP ( 'NONE', ( #4878, #10901, #29927, #50408, #12287, #15410, #29089, #25849 ) ) ;
#19045=PLANE ( 'NONE',  #68924 ) ;
#19049=LINE ( 'NONE', #52278, #4098 ) ;
#19053=CARTESIAN_POINT ( 'NONE',  ( 8.900000000000005684, -21.00000000000000355, 14.57806571531352269 ) ) ;
#19061=DIRECTION ( 'NONE',  ( 0.000000000000000000, -1.000000000000000000, 0.000000000000000000 ) ) ;
#19077=VERTEX_POINT ( 'NONE', #3993 ) ;
#19081=VECTOR ( 'NONE', #50195, 1000.000000000000000 ) ;
#19089=CARTESIAN_POINT ( 'NONE',  ( 49.00000000000000000, 20.60000000000000142, -13.86939075806900057 ) ) ;
#19094=DIRECTION ( 'NONE',  ( 0.000000000000000000, 0.000000000000000000, -1.000000000000000000 ) ) ;
#19106=VERTEX_POINT ( 'NONE', #30156 ) ;
#19112=DIRECTION ( 'NONE',  ( 0.000000000000000000, 0.000000000000000000, -1.000000000000000000 ) ) ;
#19115=DIRECTION ( 'NONE',  ( -1.000000000000000000, 0.000000000000000000, 0.000000000000000000 ) ) ;
#19143=EDGE_LOOP ( 'NONE', ( #55731, #63420, #1396, #62329 ) ) ;
#19150=CARTESIAN_POINT ( 'NONE',  ( 33.89999999999999858, -14.06939075806902117, -20.80000000000000426 ) ) ;
#19156=ADVANCED_BREP_SHAPE_REPRESENTATION ( '', ( #66174, #44181, #66857, #43035, #19195, #65828, #19540, #21524, #43959, #42462, #43380, #42921, #19898, #44638, #20709, #43848, #43151, #67216, #42807, #67800, #42691, #67577, #44406, #66294, #20943, #43268, #44878, #45918 ), #55023 ) ;
#19159=EDGE_CURVE ( 'NONE', #19378, #22473, #3014, .T. ) ;
#19161=FACE_OUTER_BOUND ( 'NONE', #13617, .T. ) ;
#19169=ORIENTED_EDGE ( 'NONE', *, *, #66090, .F. ) ;
#19182=AXIS2_PLACEMENT_3D ( 'NONE', #36925, #15697, #58495 ) ;
#19192=CARTESIAN_POINT ( 'NONE',  ( 19.90000000000000213, -21.00000000000001421, -13.86939075806900945 ) ) ;
#19195=MANIFOLD_SOLID_BREP ( 'LPattern1[5]', #12582 ) ;
#19198=FILL_AREA_STYLE ('',( #13543 ) ) ;
#19201=ORIENTED_EDGE ( 'NONE', *, *, #36521, .T. ) ;
#19224=ORIENTED_EDGE ( 'NONE', *, *, #15122, .T. ) ;
#19225=DIRECTION ( 'NONE',  ( 1.000000000000000000, -0.000000000000000000, 0.000000000000000000 ) ) ;
#19232=CARTESIAN_POINT ( 'NONE',  ( 49.00000000000000000, -21.00000000000000000, 13.86939075806900057 ) ) ;
#19237=AXIS2_PLACEMENT_3D ( 'NONE', #69838, #28091, #16444 ) ;
#19241=ORIENTED_EDGE ( 'NONE', *, *, #69634, .F. ) ;
#19246=ORIENTED_EDGE ( 'NONE', *, *, #35295, .T. ) ;
#19258=ORIENTED_EDGE ( 'NONE', *, *, #33987, .T. ) ;
#19261=EDGE_CURVE ( 'NONE', #46721, #65971, #13842, .T. ) ;
#19265=ORIENTED_EDGE ( 'NONE', *, *, #16709, .F. ) ;
#19272=( NAMED_UNIT ( * ) PLANE_ANGLE_UNIT ( ) SI_UNIT ( $, .RADIAN. ) );
#19276=DIRECTION ( 'NONE',  ( 1.000000000000000000, -0.000000000000000000, 0.000000000000000000 ) ) ;
#19281=CARTESIAN_POINT ( 'NONE',  ( 40.90000000000000568, 20.60000000000000142, 13.86939075806900057 ) ) ;
#19289=DIRECTION ( 'NONE',  ( 1.000000000000000000, -0.000000000000000000, 0.000000000000000000 ) ) ;
#19291=DIRECTION ( 'NONE',  ( 0.000000000000000000, 0.000000000000000000, 1.000000000000000000 ) ) ;
#19295=CYLINDRICAL_SURFACE ( 'NONE', #54236, 24.99999999998784972 ) ;
#19306=AXIS2_PLACEMENT_3D ( 'NONE', #16584, #58676, #31467 ) ;
#19312=CYLINDRICAL_SURFACE ( 'NONE', #34660, 24.99999999998789946 ) ;
#19313=EDGE_CURVE ( 'NONE', #14048, #5488, #62872, .T. ) ;
#19319=DIRECTION ( 'NONE',  ( 0.000000000000000000, 0.000000000000000000, -1.000000000000000000 ) ) ;
#19322=LINE ( 'NONE', #8723, #24185 ) ;
#19323=CARTESIAN_POINT ( 'NONE',  ( 46.39999999999999858, 33.00000000000000000, -2.250000000000000444 ) ) ;
#19327=EDGE_CURVE ( 'NONE', #51399, #33655, #9841, .T. ) ;
#19336=DIRECTION ( 'NONE',  ( 0.000000000000000000, 0.000000000000000000, 1.000000000000000000 ) ) ;
#19337=ORIENTED_EDGE ( 'NONE', *, *, #6841, .T. ) ;
#19344=SURFACE_STYLE_FILL_AREA ( #25013 ) ;
#19351=AXIS2_PLACEMENT_3D ( 'NONE', #43496, #37176, #42465 ) ;
#19361=CARTESIAN_POINT ( 'NONE',  ( 41.09999999999999432, -0.2000000000000000111, 0.000000000000000000 ) ) ;
#19368=DIRECTION ( 'NONE',  ( -1.000000000000000000, 0.000000000000000000, 0.000000000000000000 ) ) ;
#19373=VECTOR ( 'NONE', #62291, 1000.000000000000000 ) ;
#19378=VERTEX_POINT ( 'NONE', #65677 ) ;
#19388=VERTEX_POINT ( 'NONE', #33498 ) ;
#19394=DIRECTION ( 'NONE',  ( 0.000000000000000000, 0.000000000000000000, 1.000000000000000000 ) ) ;
#19395=CARTESIAN_POINT ( 'NONE',  ( 8.900000000000005684, -21.00000000000000000, -14.57806571531351914 ) ) ;
#19396=ADVANCED_FACE ( 'NONE', ( #18974 ), #46533, .T. ) ;
#19399=ORIENTED_EDGE ( 'NONE', *, *, #65792, .T. ) ;
#19401=DIRECTION ( 'NONE',  ( 1.000000000000000000, -0.000000000000000000, 0.000000000000000000 ) ) ;
#19403=CARTESIAN_POINT ( 'NONE',  ( 41.09999999999999432, -14.06939075806901940, -20.80000000000000426 ) ) ;
#19414=ADVANCED_FACE ( 'NONE', ( #67758 ), #61386, .F. ) ;
#19415=AXIS2_PLACEMENT_3D ( 'NONE', #18931, #19276, #45087 ) ;
#19416=CARTESIAN_POINT ( 'NONE',  ( 41.09999999999999432, -14.06939075806901940, -20.80000000000000426 ) ) ;
#19418=ORIENTED_EDGE ( 'NONE', *, *, #12218, .F. ) ;
#19424=EDGE_LOOP ( 'NONE', ( #18690, #63538, #59304, #11682 ) ) ;
#19431=DIRECTION ( 'NONE',  ( -1.000000000000000000, 0.000000000000000000, 0.000000000000000000 ) ) ;
#19438=ADVANCED_FACE ( 'NONE', ( #45479 ), #13663, .F. ) ;
#19444=ORIENTED_EDGE ( 'NONE', *, *, #6335, .T. ) ;
#19456=CYLINDRICAL_SURFACE ( 'NONE', #9553, 3.500000000000000000 ) ;
#19457=DIRECTION ( 'NONE',  ( 0.000000000000000000, 0.000000000000000000, 1.000000000000000000 ) ) ;
#19493=FACE_OUTER_BOUND ( 'NONE', #45813, .T. ) ;
#19495=CARTESIAN_POINT ( 'NONE',  ( 25.90000000000000213, -21.00000000000000000, 13.86939075806900057 ) ) ;
#19496=LINE ( 'NONE', #15618, #48217 ) ;
#19498=DIRECTION ( 'NONE',  ( 0.000000000000000000, 0.000000000000000000, -1.000000000000000000 ) ) ;
#19516=EDGE_CURVE ( 'NONE', #44316, #40017, #19857, .T. ) ;
#19518=AXIS2_PLACEMENT_3D ( 'NONE', #53839, #21304, #69384 ) ;
#19526=CARTESIAN_POINT ( 'NONE',  ( 10.00000000000000000, -18.00000000000000355, -21.00000000000000000 ) ) ;
#19530=DIRECTION ( 'NONE',  ( 0.000000000000000000, -1.000000000000000000, 0.000000000000000000 ) ) ;
#19536=DIRECTION ( 'NONE',  ( 0.000000000000000000, -1.000000000000000000, 0.000000000000000000 ) ) ;
#19540=MANIFOLD_SOLID_BREP ( 'LPattern1[7]', #27317 ) ;
#19555=VERTEX_POINT ( 'NONE', #30635 ) ;
#19558=CARTESIAN_POINT ( 'NONE',  ( 8.900000000000005684, -0.2000000000000000111, 0.000000000000000000 ) ) ;
#19585=DIRECTION ( 'NONE',  ( 0.000000000000000000, -1.000000000000000000, 0.000000000000000000 ) ) ;
#19588=VECTOR ( 'NONE', #61388, 1000.000000000000114 ) ;
#19605=EDGE_CURVE ( 'NONE', #13851, #35406, #59940, .T. ) ;
#19611=FACE_OUTER_BOUND ( 'NONE', #9871, .T. ) ;
#19619=DIRECTION ( 'NONE',  ( 0.000000000000000000, 0.000000000000000000, 1.000000000000000000 ) ) ;
#19624=CARTESIAN_POINT ( 'NONE',  ( 49.00000000000000000, 13.66939075806899950, 20.80000000000000426 ) ) ;
#19625=VECTOR ( 'NONE', #56031, 1000.000000000000000 ) ;
#19630=DIRECTION ( 'NONE',  ( 1.000000000000000000, -0.000000000000000000, 0.000000000000000000 ) ) ;
#19639=VERTEX_POINT ( 'NONE', #17496 ) ;
#19644=UNCERTAINTY_MEASURE_WITH_UNIT (LENGTH_MEASURE( 1.000000000000000082E-05 ), #53350, 'distance_accuracy_value', 'NONE');
#19655=FACE_OUTER_BOUND ( 'NONE', #13363, .T. ) ;
#19660=DIRECTION ( 'NONE',  ( -1.000000000000000000, 0.000000000000000000, 0.000000000000000000 ) ) ;
#19665=LINE ( 'NONE', #51151, #68064 ) ;
#19678=FACE_OUTER_BOUND ( 'NONE', #21376, .T. ) ;
#19691=VERTEX_POINT ( 'NONE', #213 ) ;
#19694=ORIENTED_EDGE ( 'NONE', *, *, #34944, .T. ) ;
#19695=AXIS2_PLACEMENT_3D ( 'NONE', #68606, #64010, #53739 ) ;
#19701=CARTESIAN_POINT ( 'NONE',  ( 39.90000000000000568, -0.1999999999911795112, 8.826273045769999343E-12 ) ) ;
#19704=CARTESIAN_POINT ( 'NONE',  ( 30.90000000000000213, 20.60000000000000142, 13.86939075806900057 ) ) ;
#19711=DIRECTION ( 'NONE',  ( 0.000000000000000000, 0.000000000000000000, 1.000000000000000000 ) ) ;
#19712=ORIENTED_EDGE ( 'NONE', *, *, #66355, .T. ) ;
#19713=CARTESIAN_POINT ( 'NONE',  ( 9.900000000000000355, -18.00000000000000355, -21.00000000000000000 ) ) ;
#19746=CARTESIAN_POINT ( 'NONE',  ( 40.90000000000000568, 0.000000000000000000, 0.000000000000000000 ) ) ;
#19759=CYLINDRICAL_SURFACE ( 'NONE', #52621, 2.458500000000000796 ) ;
#19762=CIRCLE ( 'NONE', #551, 24.99999999998789946 ) ;
#19763=VECTOR ( 'NONE', #26109, 1000.000000000000000 ) ;
#19777=DIRECTION ( 'NONE',  ( 0.000000000000000000, 0.000000000000000000, 1.000000000000000000 ) ) ;
#19781=ORIENTED_EDGE ( 'NONE', *, *, #8154, .T. ) ;
#19782=LINE ( 'NONE', #41354, #13413 ) ;
#19802=EDGE_CURVE ( 'NONE', #69031, #63520, #16055, .T. ) ;
#19816=EDGE_CURVE ( 'NONE', #58955, #13881, #55680, .T. ) ;
#19818=VECTOR ( 'NONE', #9522, 1000.000000000000000 ) ;
#19829=ORIENTED_EDGE ( 'NONE', *, *, #43002, .F. ) ;
#19832=VECTOR ( 'NONE', #17909, 1000.000000000000000 ) ;
#19835=EDGE_LOOP ( 'NONE', ( #37667, #25575, #59364, #62595 ) ) ;
#19843=ORIENTED_EDGE ( 'NONE', *, *, #27585, .T. ) ;
#19844=DIRECTION ( 'NONE',  ( 1.000000000000000000, -0.000000000000000000, 0.000000000000000000 ) ) ;
#19848=CARTESIAN_POINT ( 'NONE',  ( 46.39999999999999858, 33.00000000000000000, 0.2500000000000000000 ) ) ;
#19849=LINE ( 'NONE', #14547, #5728 ) ;
#19851=EDGE_LOOP ( 'NONE', ( #65853, #14332, #30500, #1917 ) ) ;
#19857=CIRCLE ( 'NONE', #56000, 24.99999999998794920 ) ;
#19859=AXIS2_PLACEMENT_3D ( 'NONE', #11869, #29884, #7256 ) ;
#19881=VECTOR ( 'NONE', #66848, 1000.000000000000114 ) ;
#19891=DIRECTION ( 'NONE',  ( 1.000000000000000000, -0.000000000000000000, 0.000000000000000000 ) ) ;
#19893=ORIENTED_EDGE ( 'NONE', *, *, #33769, .F. ) ;
#19898=MANIFOLD_SOLID_BREP ( 'LPattern1[13]', #64559 ) ;
#19918=CARTESIAN_POINT ( 'NONE',  ( 40.90000000000000568, 6.429395695523604153E-16, -5.250000000000000000 ) ) ;
#19930=VECTOR ( 'NONE', #59101, 1000.000000000000000 ) ;
#19940=DIRECTION ( 'NONE',  ( 0.000000000000000000, 0.7071067811865474617, 0.7071067811865474617 ) ) ;
#19943=VERTEX_POINT ( 'NONE', #31283 ) ;
#19953=( NAMED_UNIT ( * ) PLANE_ANGLE_UNIT ( ) SI_UNIT ( $, .RADIAN. ) );
#19958=FACE_OUTER_BOUND ( 'NONE', #34748, .T. ) ;
#19969=ADVANCED_FACE ( 'NONE', ( #6129 ), #37620, .F. ) ;
#19971=DIRECTION ( 'NONE',  ( 0.000000000000000000, 0.000000000000000000, 1.000000000000000000 ) ) ;
#19973=VECTOR ( 'NONE', #68197, 1000.000000000000000 ) ;
#19986=CARTESIAN_POINT ( 'NONE',  ( 10.90000000000000036, 13.66939075806899240, 20.79999999999999361 ) ) ;
#20021=ADVANCED_FACE ( 'NONE', ( #11761 ), #49602, .F. ) ;
#20023=VECTOR ( 'NONE', #45213, 1000.000000000000000 ) ;
#20032=DIRECTION ( 'NONE',  ( -0.000000000000000000, -1.000000000000000000, 0.000000000000000000 ) ) ;
#20034=AXIS2_PLACEMENT_3D ( 'NONE', #52345, #35349, #62957 ) ;
#20039=CARTESIAN_POINT ( 'NONE',  ( 9.899999999999998579, -0.2000000000000000111, 0.000000000000000000 ) ) ;
#20046=DIRECTION ( 'NONE',  ( 0.000000000000000000, -1.000000000000000000, 0.000000000000000000 ) ) ;
#20047=CARTESIAN_POINT ( 'NONE',  ( 0.5000000000000000000, -18.00000000000000355, 21.00000000000000000 ) ) ;
#20052=ORIENTED_EDGE ( 'NONE', *, *, #26825, .F. ) ;
#20054=CARTESIAN_POINT ( 'NONE',  ( 23.90000000000000213, -14.06939075806900874, 20.80000000000001137 ) ) ;
#20062=ADVANCED_FACE ( 'NONE', ( #54928 ), #27356, .T. ) ;
#20063=CARTESIAN_POINT ( 'NONE',  ( 39.00000000000000000, 4.286263797015736595E-16, -3.500000000000000000 ) ) ;
#20067=CARTESIAN_POINT ( 'NONE',  ( 41.09999999999999432, -14.06939075806901940, -20.80000000000000426 ) ) ;
#20079=DIRECTION ( 'NONE',  ( 0.000000000000000000, 0.000000000000000000, 1.000000000000000000 ) ) ;
#20082=VECTOR ( 'NONE', #6035, 1000.000000000000000 ) ;
#20088=CARTESIAN_POINT ( 'NONE',  ( 41.09999999999999432, -21.00000000000000000, -13.86939075806900057 ) ) ;
#20089=ORIENTED_EDGE ( 'NONE', *, *, #9965, .T. ) ;
#20092=ORIENTED_EDGE ( 'NONE', *, *, #55289, .F. ) ;
#20095=FACE_OUTER_BOUND ( 'NONE', #62651, .T. ) ;
#20110=DIRECTION ( 'NONE',  ( 0.000000000000000000, 0.000000000000000000, -1.000000000000000000 ) ) ;
#20123=DIRECTION ( 'NONE',  ( 0.000000000000000000, 0.000000000000000000, -1.000000000000000000 ) ) ;
#20125=DIRECTION ( 'NONE',  ( -1.000000000000000000, 0.000000000000000000, 0.000000000000000000 ) ) ;
#20139=CARTESIAN_POINT ( 'NONE',  ( 24.90000000000000213, -14.06939075806900163, -20.80000000000000426 ) ) ;
#20145=DIRECTION ( 'NONE',  ( -1.000000000000000000, 0.000000000000000000, 0.000000000000000000 ) ) ;
#20147=ADVANCED_FACE ( 'NONE', ( #19161 ), #55946, .F. ) ;
#20154=CARTESIAN_POINT ( 'NONE',  ( 39.90000000000000568, -14.48845687959340012, 21.00000000000000000 ) ) ;
#20155=ADVANCED_FACE ( 'NONE', ( #17775 ), #34017, .T. ) ;
#20173=ORIENTED_EDGE ( 'NONE', *, *, #5480, .F. ) ;
#20174=LINE ( 'NONE', #64031, #69186 ) ;
#20196=VERTEX_POINT ( 'NONE', #1501 ) ;
#20206=DIRECTION ( 'NONE',  ( 0.000000000000000000, 1.000000000000000000, -0.000000000000000000 ) ) ;
#20209=CARTESIAN_POINT ( 'NONE',  ( 39.00000000000000000, 16.96999999999999886, -21.00000000000000000 ) ) ;
#20227=ORIENTED_EDGE ( 'NONE', *, *, #14647, .F. ) ;
#20241=EDGE_CURVE ( 'NONE', #7082, #46721, #4661, .T. ) ;
#20267=VERTEX_POINT ( 'NONE', #9615 ) ;
#20268=EDGE_CURVE ( 'NONE', #5139, #45732, #8653, .T. ) ;
#20273=AXIS2_PLACEMENT_3D ( 'NONE', #61706, #35528, #19619 ) ;
#20275=VECTOR ( 'NONE', #57292, 1000.000000000000000 ) ;
#20276=EDGE_CURVE ( 'NONE', #26452, #52164, #3606, .T. ) ;
#20286=DIRECTION ( 'NONE',  ( -1.000000000000000000, 0.000000000000000000, 0.000000000000000000 ) ) ;
#20295=SURFACE_SIDE_STYLE ('',( #37273 ) ) ;
#20296=EDGE_LOOP ( 'NONE', ( #640, #51487, #24565, #20092 ) ) ;
#20306=FILL_AREA_STYLE_COLOUR ( '', #13288 ) ;
#20329=EDGE_CURVE ( 'NONE', #49395, #7815, #9833, .T. ) ;
#20335=VECTOR ( 'NONE', #15872, 1000.000000000000000 ) ;
#20357=UNCERTAINTY_MEASURE_WITH_UNIT (LENGTH_MEASURE( 1.000000000000000082E-05 ), #63624, 'distance_accuracy_value', 'NONE');
#20358=LINE ( 'NONE', #9049, #46919 ) ;
#20366=EDGE_CURVE ( 'NONE', #4872, #49395, #53800, .T. ) ;
#20369=FACE_OUTER_BOUND ( 'NONE', #34003, .T. ) ;
#20371=PLANE ( 'NONE',  #51884 ) ;
#20376=DIRECTION ( 'NONE',  ( 0.000000000000000000, 0.000000000000000000, -1.000000000000000000 ) ) ;
#20377=SURFACE_SIDE_STYLE ('',( #31700 ) ) ;
#20384=AXIS2_PLACEMENT_3D ( 'NONE', #56056, #40123, #67005 ) ;
#20390=FILL_AREA_STYLE ('',( #62108 ) ) ;
#20391=DIRECTION ( 'NONE',  ( 0.000000000000000000, 0.000000000000000000, -1.000000000000000000 ) ) ;
#20393=CARTESIAN_POINT ( 'NONE',  ( 0.5000000000000000000, 21.00000000000000000, -18.00000000000000355 ) ) ;
#20395=LINE ( 'NONE', #15455, #32406 ) ;
#20405=EDGE_CURVE ( 'NONE', #45925, #40436, #52747, .T. ) ;
#20419=ORIENTED_EDGE ( 'NONE', *, *, #18313, .F. ) ;
#20422=VERTEX_POINT ( 'NONE', #5711 ) ;
#20436=VECTOR ( 'NONE', #54955, 1000.000000000000000 ) ;
#20441=CARTESIAN_POINT ( 'NONE',  ( 41.09999999999999432, -21.00000000000000000, 13.86939075806900057 ) ) ;
#20444=EDGE_CURVE ( 'NONE', #26978, #17145, #43518, .T. ) ;
#20445=DIRECTION ( 'NONE',  ( 1.000000000000000000, -0.000000000000000000, 0.000000000000000000 ) ) ;
#20453=ORIENTED_EDGE ( 'NONE', *, *, #21036, .F. ) ;
#20470=CARTESIAN_POINT ( 'NONE',  ( 21.90000000000000213, -0.000000000000000000, -20.80000000000000426 ) ) ;
#20483=CARTESIAN_POINT ( 'NONE',  ( 0.5000000000000000000, 21.00000000000000000, 18.00000000000000355 ) ) ;
#20488=AXIS2_PLACEMENT_3D ( 'NONE', #56761, #52169, #57815 ) ;
#20495=ORIENTED_EDGE ( 'NONE', *, *, #16369, .F. ) ;
#20507=EDGE_LOOP ( 'NONE', ( #62245, #159, #46869, #58806 ) ) ;
#20512=CARTESIAN_POINT ( 'NONE',  ( 46.39999999999999858, 21.00000000000000000, 2.250000000000000444 ) ) ;
#20518=CARTESIAN_POINT ( 'NONE',  ( 20.90000000000000213, -0.1999999999911795112, 8.826273045769999343E-12 ) ) ;
#20523=CARTESIAN_POINT ( 'NONE',  ( 25.57999999999999829, 6.429395695523604153E-16, -5.250000000000000000 ) ) ;
#20527=ORIENTED_EDGE ( 'NONE', *, *, #45339, .T. ) ;
#20533=EDGE_LOOP ( 'NONE', ( #65549, #24042, #38762, #42650 ) ) ;
#20534=CARTESIAN_POINT ( 'NONE',  ( 39.00000000000000000, -16.96999999999999886, -21.00000000000000000 ) ) ;
#20559=EDGE_CURVE ( 'NONE', #35542, #49922, #2809, .T. ) ;
#20567=CARTESIAN_POINT ( 'NONE',  ( 41.09999999999999432, 13.66939075806899950, -20.80000000000000426 ) ) ;
#20578=ORIENTED_EDGE ( 'NONE', *, *, #42258, .T. ) ;
#20579=CARTESIAN_POINT ( 'NONE',  ( 35.89999999999999858, 0.000000000000000000, 3.016910393003143647E-15 ) ) ;
#20590=VERTEX_POINT ( 'NONE', #13424 ) ;
#20596=ADVANCED_FACE ( 'NONE', ( #40292 ), #23340, .F. ) ;
#20603=FACE_OUTER_BOUND ( 'NONE', #26456, .T. ) ;
#20617=AXIS2_PLACEMENT_3D ( 'NONE', #17159, #27777, #12874 ) ;
#20626=ORIENTED_EDGE ( 'NONE', *, *, #60935, .T. ) ;
#20632=LINE ( 'NONE', #9333, #30073 ) ;
#20633=FACE_OUTER_BOUND ( 'NONE', #4623, .T. ) ;
#20634=ADVANCED_FACE ( 'NONE', ( #68922 ), #3873, .T. ) ;
#20642=CARTESIAN_POINT ( 'NONE',  ( 18.89999999999999858, -21.00000000000000000, 13.86939075806900057 ) ) ;
#20647=ORIENTED_EDGE ( 'NONE', *, *, #10665, .F. ) ;
#20651=ORIENTED_EDGE ( 'NONE', *, *, #29465, .F. ) ;
#20653=EDGE_CURVE ( 'NONE', #34278, #53158, #17741, .T. ) ;
#20660=CARTESIAN_POINT ( 'NONE',  ( 41.09999999999999432, 13.66939075806899950, 20.80000000000000426 ) ) ;
#20673=DIRECTION ( 'NONE',  ( 0.000000000000000000, -1.000000000000000000, 0.000000000000000000 ) ) ;
#20687=ORIENTED_EDGE ( 'NONE', *, *, #27202, .T. ) ;
#20688=EDGE_CURVE ( 'NONE', #17050, #36357, #3522, .T. ) ;
#20690=EDGE_CURVE ( 'NONE', #5139, #42288, #62547, .T. ) ;
#20694=VECTOR ( 'NONE', #28818, 1000.000000000000000 ) ;
#20707=DIRECTION ( 'NONE',  ( 0.000000000000000000, 0.000000000000000000, -1.000000000000000000 ) ) ;
#20709=MANIFOLD_SOLID_BREP ( 'LPattern1[15]', #56617 ) ;
#20710=EDGE_CURVE ( 'NONE', #31270, #68694, #5280, .T. ) ;
#20711=DIRECTION ( 'NONE',  ( 0.000000000000000000, 0.000000000000000000, 1.000000000000000000 ) ) ;
#20722=VERTEX_POINT ( 'NONE', #32824 ) ;
#20725=CARTESIAN_POINT ( 'NONE',  ( 39.00000000000000000, -16.96999999999999886, 21.00000000000000000 ) ) ;
#20726=LINE ( 'NONE', #58213, #44327 ) ;
#20732=DIRECTION ( 'NONE',  ( 1.000000000000000000, -0.000000000000000000, 0.000000000000000000 ) ) ;
#20756=DIRECTION ( 'NONE',  ( -1.000000000000000000, 0.000000000000000000, 0.000000000000000000 ) ) ;
#20764=DIRECTION ( 'NONE',  ( 1.000000000000000000, -0.000000000000000000, 0.000000000000000000 ) ) ;
#20773=ORIENTED_EDGE ( 'NONE', *, *, #6442, .F. ) ;
#20777=DIRECTION ( 'NONE',  ( 0.000000000000000000, 0.000000000000000000, 1.000000000000000000 ) ) ;
#20783=EDGE_LOOP ( 'NONE', ( #28915, #33917, #40637, #22002 ) ) ;
#20785=LINE ( 'NONE', #31053, #1477 ) ;
#20789=AXIS2_PLACEMENT_3D ( 'NONE', #45024, #12834, #34398 ) ;
#20793=VECTOR ( 'NONE', #7167, 1000.000000000000000 ) ;
#20804=SURFACE_SIDE_STYLE ('',( #59335 ) ) ;
#20806=DIRECTION ( 'NONE',  ( 0.000000000000000000, -1.000000000000000000, 0.000000000000000000 ) ) ;
#20808=DIRECTION ( 'NONE',  ( -1.000000000000000000, 0.000000000000000000, 0.000000000000000000 ) ) ;
#20830=CARTESIAN_POINT ( 'NONE',  ( 14.89999999999999680, -21.00000000000001421, -13.86939075806900945 ) ) ;
#20834=DIRECTION ( 'NONE',  ( -1.000000000000000000, 0.000000000000000000, 0.000000000000000000 ) ) ;
#20835=PLANE ( 'NONE',  #40665 ) ;
#20839=VECTOR ( 'NONE', #1137, 1000.000000000000000 ) ;
#20842=DIRECTION ( 'NONE',  ( 0.000000000000000000, 1.000000000000000000, 0.000000000000000000 ) ) ;
#20850=EDGE_CURVE ( 'NONE', #19388, #37742, #18910, .T. ) ;
#20855=ADVANCED_FACE ( 'NONE', ( #13598 ), #34447, .F. ) ;
#20860=ORIENTED_EDGE ( 'NONE', *, *, #57890, .T. ) ;
#20878=AXIS2_PLACEMENT_3D ( 'NONE', #59728, #1705, #48775 ) ;
#20883=VERTEX_POINT ( 'NONE', #41524 ) ;
#20886=DIRECTION ( 'NONE',  ( -1.000000000000000000, 0.000000000000000000, 0.000000000000000000 ) ) ;
#20895=CARTESIAN_POINT ( 'NONE',  ( 11.90000000000000036, -0.000000000000000000, -20.80000000000000426 ) ) ;
#20896=ORIENTED_EDGE ( 'NONE', *, *, #46306, .F. ) ;
#20897=EDGE_CURVE ( 'NONE', #56261, #12819, #39232, .T. ) ;
#20899=AXIS2_PLACEMENT_3D ( 'NONE', #56155, #55464, #23612 ) ;
#20903=EDGE_CURVE ( 'NONE', #30511, #12117, #16056, .T. ) ;
#20906=LINE ( 'NONE', #9964, #5571 ) ;
#20914=DIRECTION ( 'NONE',  ( 1.000000000000000000, -0.000000000000000000, 0.000000000000000000 ) ) ;
#20918=EDGE_LOOP ( 'NONE', ( #35512, #10364, #28239, #33361 ) ) ;
#20922=VERTEX_POINT ( 'NONE', #52857 ) ;
#20930=CARTESIAN_POINT ( 'NONE',  ( 41.09999999999999432, 20.60000000000000142, -13.86939075806900057 ) ) ;
#20932=EDGE_LOOP ( 'NONE', ( #65346, #23880, #12639, #5985 ) ) ;
#20943=MANIFOLD_SOLID_BREP ( 'LPattern1[26]', #25029 ) ;
#20958=VECTOR ( 'NONE', #3003, 1000.000000000000000 ) ;
#20974=PLANE ( 'NONE',  #31358 ) ;
#20978=ORIENTED_EDGE ( 'NONE', *, *, #56988, .F. ) ;
#20993=AXIS2_PLACEMENT_3D ( 'NONE', #41399, #3930, #24793 ) ;
#21003=DIRECTION ( 'NONE',  ( 0.6785983445458467767, -0.2810846377148228381, -0.6785983445458462215 ) ) ;
#21007=CARTESIAN_POINT ( 'NONE',  ( 27.90000000000000213, 0.000000000000000000, 0.000000000000000000 ) ) ;
#21008=CARTESIAN_POINT ( 'NONE',  ( 41.09999999999999432, -21.00000000000000000, 13.86939075806900057 ) ) ;
#21016=CARTESIAN_POINT ( 'NONE',  ( 39.00000000000000000, 21.00000000000000000, 16.96999999999999886 ) ) ;
#21018=CARTESIAN_POINT ( 'NONE',  ( 10.00000000000000000, 21.00000000000000000, -18.00000000000000355 ) ) ;
#21020=CARTESIAN_POINT ( 'NONE',  ( 39.00000000000000000, -14.48845687959340012, 21.00000000000000000 ) ) ;
#21024=EDGE_CURVE ( 'NONE', #12238, #16445, #69802, .T. ) ;
#21031=DIRECTION ( 'NONE',  ( -1.000000000000000000, 0.000000000000000000, 0.000000000000000000 ) ) ;
#21036=EDGE_CURVE ( 'NONE', #48516, #9337, #16754, .T. ) ;
#21042=EDGE_CURVE ( 'NONE', #40439, #42288, #24608, .T. ) ;
#21043=DIRECTION ( 'NONE',  ( 0.000000000000000000, 0.000000000000000000, -1.000000000000000000 ) ) ;
#21053=AXIS2_PLACEMENT_3D ( 'NONE', #27228, #44494, #38852 ) ;
#21065=CARTESIAN_POINT ( 'NONE',  ( 13.90000000000000213, -14.06939075806902117, -20.80000000000000426 ) ) ;
#21068=VERTEX_POINT ( 'NONE', #53897 ) ;
#21074=VECTOR ( 'NONE', #5373, 1000.000000000000000 ) ;
#21082=DIRECTION ( 'NONE',  ( 1.000000000000000000, -0.000000000000000000, 0.000000000000000000 ) ) ;
#21116=DIRECTION ( 'NONE',  ( -1.000000000000000000, 0.000000000000000000, 0.000000000000000000 ) ) ;
#21121=DIRECTION ( 'NONE',  ( 1.000000000000000000, -0.000000000000000000, -0.000000000000000000 ) ) ;
#21122=ORIENTED_EDGE ( 'NONE', *, *, #68021, .F. ) ;
#21124=EDGE_LOOP ( 'NONE', ( #60700, #61597, #50873, #55944 ) ) ;
#21125=ORIENTED_EDGE ( 'NONE', *, *, #29506, .F. ) ;
#21129=CARTESIAN_POINT ( 'NONE',  ( 49.00000000000000000, -0.2000000000089119934, 8.909539772616881237E-12 ) ) ;
#21144=ORIENTED_EDGE ( 'NONE', *, *, #9526, .T. ) ;
#21167=ADVANCED_FACE ( 'NONE', ( #29773 ), #41083, .T. ) ;
#21168=AXIS2_PLACEMENT_3D ( 'NONE', #63259, #15174, #31449 ) ;
#21172=ORIENTED_EDGE ( 'NONE', *, *, #56039, .F. ) ;
#21180=DIRECTION ( 'NONE',  ( 0.000000000000000000, 0.000000000000000000, 1.000000000000000000 ) ) ;
#21182=CARTESIAN_POINT ( 'NONE',  ( 8.900000000000005684, -14.48845687959340012, 21.00000000000000000 ) ) ;
#21234=CARTESIAN_POINT ( 'NONE',  ( 40.90000000000000568, 16.96999999999999886, 21.00000000000000000 ) ) ;
#21250=CARTESIAN_POINT ( 'NONE',  ( 16.89999999999999858, 20.60000000000000142, 13.86939075806900057 ) ) ;
#21251=VERTEX_POINT ( 'NONE', #23777 ) ;
#21256=DIRECTION ( 'NONE',  ( -1.000000000000000000, 0.000000000000000000, 0.000000000000000000 ) ) ;
#21259=ORIENTED_EDGE ( 'NONE', *, *, #25428, .T. ) ;
#21263=VECTOR ( 'NONE', #30956, 1000.000000000000000 ) ;
#21271=EDGE_CURVE ( 'NONE', #8645, #57546, #26235, .T. ) ;
#21280=VERTEX_POINT ( 'NONE', #9625 ) ;
#21284=PLANE ( 'NONE',  #59457 ) ;
#21292=CYLINDRICAL_SURFACE ( 'NONE', #21912, 24.99999999998794920 ) ;
#21304=DIRECTION ( 'NONE',  ( 1.000000000000000000, -0.000000000000000000, 0.000000000000000000 ) ) ;
#21305=EDGE_CURVE ( 'NONE', #67015, #29909, #32549, .T. ) ;
#21307=DIRECTION ( 'NONE',  ( 0.000000000000000000, 0.000000000000000000, 1.000000000000000000 ) ) ;
#21314=EDGE_LOOP ( 'NONE', ( #7799, #48746, #22140, #58534 ) ) ;
#21316=CARTESIAN_POINT ( 'NONE',  ( 9.900000000000000355, 0.000000000000000000, 2.154935995002245639E-16 ) ) ;
#21321=VERTEX_POINT ( 'NONE', #37202 ) ;
#21332=DIRECTION ( 'NONE',  ( -1.000000000000000000, 0.000000000000000000, 0.000000000000000000 ) ) ;
#21334=VERTEX_POINT ( 'NONE', #14567 ) ;
#21344=PLANE ( 'NONE',  #33854 ) ;
#21346=ADVANCED_FACE ( 'NONE', ( #28303 ), #1430, .F. ) ;
#21357=DIRECTION ( 'NONE',  ( 0.000000000000000000, 0.000000000000000000, -1.000000000000000000 ) ) ;
#21361=AXIS2_PLACEMENT_3D ( 'NONE', #14743, #52942, #69532 ) ;
#21364=CARTESIAN_POINT ( 'NONE',  ( 41.09999999999999432, -21.00000000000000000, -13.86939075806900057 ) ) ;
#21371=DIRECTION ( 'NONE',  ( 1.000000000000000000, -0.000000000000000000, 0.000000000000000000 ) ) ;
#21376=EDGE_LOOP ( 'NONE', ( #66055, #56133, #44987, #42100 ) ) ;
#21381=EDGE_CURVE ( 'NONE', #63246, #14509, #59103, .T. ) ;
#21395=PLANE ( 'NONE',  #40420 ) ;
#21417=CARTESIAN_POINT ( 'NONE',  ( 39.90000000000000568, 6.429395695523604153E-16, -5.250000000000000000 ) ) ;
#21419=FILL_AREA_STYLE_COLOUR ( '', #49252 ) ;
#21420=FACE_OUTER_BOUND ( 'NONE', #9089, .T. ) ;
#21422=AXIS2_PLACEMENT_3D ( 'NONE', #35374, #35738, #18071 ) ;
#21441=DIRECTION ( 'NONE',  ( 0.000000000000000000, 0.000000000000000000, -1.000000000000000000 ) ) ;
#21446=CARTESIAN_POINT ( 'NONE',  ( 29.89999999999999858, -21.00000000000000000, 13.86939075806900057 ) ) ;
#21456=FACE_OUTER_BOUND ( 'NONE', #64459, .T. ) ;
#21460=AXIS2_PLACEMENT_3D ( 'NONE', #37959, #59525, #475 ) ;
#21461=VECTOR ( 'NONE', #8692, 1000.000000000000000 ) ;
#21468=DIRECTION ( 'NONE',  ( 0.000000000000000000, 0.000000000000000000, 1.000000000000000000 ) ) ;
#21478=DIRECTION ( 'NONE',  ( 0.000000000000000000, 0.000000000000000000, 1.000000000000000000 ) ) ;
#21492=ORIENTED_EDGE ( 'NONE', *, *, #28082, .F. ) ;
#21493=ORIENTED_EDGE ( 'NONE', *, *, #65910, .T. ) ;
#21507=EDGE_LOOP ( 'NONE', ( #53506, #3387, #24620, #22622, #66611, #33940, #1569, #32831 ) ) ;
#21524=MANIFOLD_SOLID_BREP ( 'LPattern1[8]', #49854 ) ;
#21526=PLANE ( 'NONE',  #64220 ) ;
#21530=CARTESIAN_POINT ( 'NONE',  ( 46.39999999999999858, 21.00000000000000000, 0.7500000000000000000 ) ) ;
#21540=AXIS2_PLACEMENT_3D ( 'NONE', #47203, #10071, #68767 ) ;
#21541=ORIENTED_EDGE ( 'NONE', *, *, #23563, .T. ) ;
#21542=VERTEX_POINT ( 'NONE', #46305 ) ;
#21546=VECTOR ( 'NONE', #27964, 1000.000000000000000 ) ;
#21557=VECTOR ( 'NONE', #53226, 1000.000000000000000 ) ;
#21566=AXIS2_PLACEMENT_3D ( 'NONE', #10907, #63260, #64310 ) ;
#21580=EDGE_CURVE ( 'NONE', #32122, #33533, #58338, .T. ) ;
#21582=EDGE_CURVE ( 'NONE', #29427, #18454, #14847, .T. ) ;
#21596=VECTOR ( 'NONE', #54216, 1000.000000000000114 ) ;
#21601=EDGE_LOOP ( 'NONE', ( #56414, #16054, #60096, #205, #14088, #51529, #44637, #68444 ) ) ;
#21605=DIRECTION ( 'NONE',  ( 0.000000000000000000, 0.000000000000000000, 1.000000000000000000 ) ) ;
#21613=EDGE_CURVE ( 'NONE', #36374, #37725, #30403, .T. ) ;
#21620=LINE ( 'NONE', #48841, #60389 ) ;
#21622=DIRECTION ( 'NONE',  ( 0.000000000000000000, 0.8346456692913390985, -0.5507872608668546999 ) ) ;
#21623=VECTOR ( 'NONE', #25423, 1000.000000000000000 ) ;
#21624=PLANE ( 'NONE',  #45360 ) ;
#21630=LINE ( 'NONE', #32590, #17646 ) ;
#21638=CARTESIAN_POINT ( 'NONE',  ( 25.57999999999999829, 0.000000000000000000, 2.458500000000000796 ) ) ;
#21641=VERTEX_POINT ( 'NONE', #48416 ) ;
#21642=AXIS2_PLACEMENT_3D ( 'NONE', #44971, #1839, #28709 ) ;
#21656=VERTEX_POINT ( 'NONE', #5969 ) ;
#21666=DIRECTION ( 'NONE',  ( 0.000000000000000000, 0.000000000000000000, 1.000000000000000000 ) ) ;
#21689=LINE ( 'NONE', #22722, #47578 ) ;
#21696=CARTESIAN_POINT ( 'NONE',  ( 9.900000000000000355, 18.00000000000000355, 21.00000000000000000 ) ) ;
#21703=LINE ( 'NONE', #48926, #9199 ) ;
#21704=PLANE ( 'NONE',  #17865 ) ;
#21717=DIRECTION ( 'NONE',  ( 0.000000000000000000, 0.000000000000000000, -1.000000000000000000 ) ) ;
#21723=CARTESIAN_POINT ( 'NONE',  ( 8.900000000000005684, -0.2000000000089119934, -8.913009219568841313E-12 ) ) ;
#21725=ADVANCED_FACE ( 'NONE', ( #64667 ), #26497, .T. ) ;
#21730=EDGE_CURVE ( 'NONE', #21280, #65046, #59368, .T. ) ;
#21733=EDGE_CURVE ( 'NONE', #1307, #58955, #29806, .T. ) ;
#21734=CIRCLE ( 'NONE', #61216, 24.99999999998789946 ) ;
#21739=EDGE_CURVE ( 'NONE', #60151, #30310, #43798, .T. ) ;
#21777=EDGE_CURVE ( 'NONE', #20922, #21542, #51173, .T. ) ;
#21779=CARTESIAN_POINT ( 'NONE',  ( 46.39999999999999858, 21.00000000000000000, -0.2500000000000000000 ) ) ;
#21782=CARTESIAN_POINT ( 'NONE',  ( 32.89999999999999858, -0.2000000000089119934, 8.909539772616881237E-12 ) ) ;
#21793=CARTESIAN_POINT ( 'NONE',  ( 23.90000000000000213, -21.00000000000001421, -13.86939075806900945 ) ) ;
#21804=DIRECTION ( 'NONE',  ( 0.000000000000000000, 0.7071067811865474617, -0.7071067811865474617 ) ) ;
#21806=EDGE_LOOP ( 'NONE', ( #64972, #66343 ) ) ;
#21820=DIRECTION ( 'NONE',  ( 1.000000000000000000, -0.000000000000000000, 0.000000000000000000 ) ) ;
#21829=ORIENTED_EDGE ( 'NONE', *, *, #57887, .T. ) ;
#21831=CARTESIAN_POINT ( 'NONE',  ( 8.900000000000005684, 14.08845687959340331, -21.00000000000000000 ) ) ;
#21838=VERTEX_POINT ( 'NONE', #55108 ) ;
#21853=CARTESIAN_POINT ( 'NONE',  ( 0.000000000000000000, 20.50000000000002487, 17.79289321881347163 ) ) ;
#21859=EDGE_CURVE ( 'NONE', #4446, #1910, #51306, .T. ) ;
#21862=DIRECTION ( 'NONE',  ( 0.000000000000000000, 0.000000000000000000, -1.000000000000000000 ) ) ;
#21880=CARTESIAN_POINT ( 'NONE',  ( 49.00000000000000000, -0.2000000000089119934, 8.909539772616881237E-12 ) ) ;
#21882=DIRECTION ( 'NONE',  ( -1.000000000000000000, 0.000000000000000000, 0.000000000000000000 ) ) ;
#21884=ORIENTED_EDGE ( 'NONE', *, *, #51754, .F. ) ;
#21887=ORIENTED_EDGE ( 'NONE', *, *, #42492, .T. ) ;
#21888=LINE ( 'NONE', #36870, #34477 ) ;
#21891=DIRECTION ( 'NONE',  ( -1.000000000000000000, 0.000000000000000000, 0.000000000000000000 ) ) ;
#21893=CARTESIAN_POINT ( 'NONE',  ( 40.90000000000000568, 0.000000000000000000, 3.447897592003593022E-15 ) ) ;
#21895=EDGE_LOOP ( 'NONE', ( #26932, #42095, #53999, #3113 ) ) ;
#21897=ORIENTED_EDGE ( 'NONE', *, *, #43067, .F. ) ;
#21905=ADVANCED_FACE ( 'NONE', ( #40212 ), #13347, .F. ) ;
#21912=AXIS2_PLACEMENT_3D ( 'NONE', #47118, #25194, #47802 ) ;
#21913=AXIS2_PLACEMENT_3D ( 'NONE', #47518, #30210, #52480 ) ;
#21917=ORIENTED_EDGE ( 'NONE', *, *, #47464, .T. ) ;
#21921=CIRCLE ( 'NONE', #5962, 24.99999999998789946 ) ;
#21927=CARTESIAN_POINT ( 'NONE',  ( 31.89999999999999858, -21.00000000000000000, 13.86939075806900057 ) ) ;
#21939=FACE_OUTER_BOUND ( 'NONE', #64257, .T. ) ;
#21962=CARTESIAN_POINT ( 'NONE',  ( 16.90000000000000213, 0.000000000000000000, 8.619743980008982554E-16 ) ) ;
#21975=AXIS2_PLACEMENT_3D ( 'NONE', #15586, #3915, #26183 ) ;
#21977=PLANE ( 'NONE',  #53959 ) ;
#21982=DIRECTION ( 'NONE',  ( 0.000000000000000000, 0.000000000000000000, -1.000000000000000000 ) ) ;
#22002=ORIENTED_EDGE ( 'NONE', *, *, #50911, .F. ) ;
#22003=VERTEX_POINT ( 'NONE', #68850 ) ;
#22009=VECTOR ( 'NONE', #54107, 1000.000000000000000 ) ;
#22027=DIRECTION ( 'NONE',  ( 0.000000000000000000, -1.000000000000000000, 0.000000000000000000 ) ) ;
#22035=CARTESIAN_POINT ( 'NONE',  ( 26.90000000000000213, -21.00000000000000000, 13.86939075806900057 ) ) ;
#22038=CARTESIAN_POINT ( 'NONE',  ( 41.09999999999999432, -0.1999999999911795112, 8.826273045769999343E-12 ) ) ;
#22070=EDGE_CURVE ( 'NONE', #26452, #9904, #37718, .T. ) ;
#22078=ADVANCED_FACE ( 'NONE', ( #4845, #64249 ), #10147, .T. ) ;
#22080=CARTESIAN_POINT ( 'NONE',  ( 37.90000000000000568, -21.00000000000000000, 13.86939075806900057 ) ) ;
#22083=ORIENTED_EDGE ( 'NONE', *, *, #20329, .T. ) ;
#22087=ORIENTED_EDGE ( 'NONE', *, *, #40503, .F. ) ;
#22094=EDGE_LOOP ( 'NONE', ( #47148, #18380, #51574, #49565 ) ) ;
#22105=DIRECTION ( 'NONE',  ( -0.7071067811865474617, -0.7071067811865474617, 0.000000000000000000 ) ) ;
#22106=ORIENTED_EDGE ( 'NONE', *, *, #42387, .F. ) ;
#22126=CARTESIAN_POINT ( 'NONE',  ( 25.90000000000000213, -21.00000000000001421, -13.86939075806900945 ) ) ;
#22128=LINE ( 'NONE', #560, #38690 ) ;
#22130=EDGE_CURVE ( 'NONE', #37742, #39718, #67152, .T. ) ;
#22134=FACE_OUTER_BOUND ( 'NONE', #43059, .T. ) ;
#22140=ORIENTED_EDGE ( 'NONE', *, *, #11103, .T. ) ;
#22142=VECTOR ( 'NONE', #44357, 1000.000000000000000 ) ;
#22145=PLANE ( 'NONE',  #2530 ) ;
#22156=VECTOR ( 'NONE', #53881, 1000.000000000000000 ) ;
#22159=EDGE_LOOP ( 'NONE', ( #8755, #33402, #63586, #19712 ) ) ;
#22163=VECTOR ( 'NONE', #5447, 1000.000000000000000 ) ;
#22168=AXIS2_PLACEMENT_3D ( 'NONE', #58898, #30621, #20707 ) ;
#22176=LINE ( 'NONE', #43739, #24579 ) ;
#22182=DIRECTION ( 'NONE',  ( -1.000000000000000000, 0.000000000000000000, 0.000000000000000000 ) ) ;
#22189=CARTESIAN_POINT ( 'NONE',  ( 8.900000000000002132, -18.00000000000000355, 21.00000000000000000 ) ) ;
#22195=AXIS2_PLACEMENT_3D ( 'NONE', #48573, #28041, #17418 ) ;
#22214=AXIS2_PLACEMENT_3D ( 'NONE', #44409, #45457, #17899 ) ;
#22235=FACE_OUTER_BOUND ( 'NONE', #48635, .T. ) ;
#22237=ORIENTED_EDGE ( 'NONE', *, *, #6047, .F. ) ;
#22242=DIRECTION ( 'NONE',  ( 1.000000000000000000, 0.000000000000000000, 0.000000000000000000 ) ) ;
#22244=ORIENTED_EDGE ( 'NONE', *, *, #37164, .T. ) ;
#22246=DIRECTION ( 'NONE',  ( 0.000000000000000000, 0.000000000000000000, 1.000000000000000000 ) ) ;
#22248=ORIENTED_EDGE ( 'NONE', *, *, #5858, .F. ) ;
#22254=FACE_OUTER_BOUND ( 'NONE', #49563, .T. ) ;
#22261=VECTOR ( 'NONE', #37338, 1000.000000000000000 ) ;
#22270=ADVANCED_FACE ( 'NONE', ( #10037 ), #14632, .T. ) ;
#22285=ORIENTED_EDGE ( 'NONE', *, *, #50921, .F. ) ;
#22292=CARTESIAN_POINT ( 'NONE',  ( 29.89999999999999858, 0.000000000000000000, 2.370429594502469981E-15 ) ) ;
#22298=ORIENTED_EDGE ( 'NONE', *, *, #30666, .T. ) ;
#22304=DIRECTION ( 'NONE',  ( 0.000000000000000000, 0.000000000000000000, -1.000000000000000000 ) ) ;
#22307=AXIS2_PLACEMENT_3D ( 'NONE', #52925, #58571, #4819 ) ;
#22324=EDGE_CURVE ( 'NONE', #23509, #51833, #11078, .T. ) ;
#22328=ORIENTED_EDGE ( 'NONE', *, *, #49695, .T. ) ;
#22341=ORIENTED_EDGE ( 'NONE', *, *, #63499, .F. ) ;
#22342=DIRECTION ( 'NONE',  ( 0.000000000000000000, -1.000000000000000000, 0.000000000000000000 ) ) ;
#22355=FILL_AREA_STYLE_COLOUR ( '', #41274 ) ;
#22366=CARTESIAN_POINT ( 'NONE',  ( 9.899999999999998579, -0.2000000000089119934, 8.909539772616881237E-12 ) ) ;
#22373=LINE ( 'NONE', #31935, #52599 ) ;
#22385=ORIENTED_EDGE ( 'NONE', *, *, #54891, .F. ) ;
#22393=EDGE_LOOP ( 'NONE', ( #50015, #42939, #64686, #1461 ) ) ;
#22395=CYLINDRICAL_SURFACE ( 'NONE', #67183, 24.99999999998789946 ) ;
#22398=DIRECTION ( 'NONE',  ( 1.000000000000000000, 0.000000000000000000, 0.000000000000000000 ) ) ;
#22413=LINE ( 'NONE', #21364, #3875 ) ;
#22414=VERTEX_POINT ( 'NONE', #59163 ) ;
#22420=EDGE_CURVE ( 'NONE', #65971, #41893, #31952, .T. ) ;
#22434=ORIENTED_EDGE ( 'NONE', *, *, #45448, .F. ) ;
#22443=ORIENTED_EDGE ( 'NONE', *, *, #3839, .T. ) ;
#22451=VERTEX_POINT ( 'NONE', #23055 ) ;
#22455=UNCERTAINTY_MEASURE_WITH_UNIT (LENGTH_MEASURE( 1.000000000000000082E-05 ), #1482, 'distance_accuracy_value', 'NONE');
#22461=LINE ( 'NONE', #49665, #5877 ) ;
#22464=ORIENTED_EDGE ( 'NONE', *, *, #8236, .F. ) ;
#22469=EDGE_CURVE ( 'NONE', #25374, #58001, #28706, .T. ) ;
#22473=VERTEX_POINT ( 'NONE', #1489 ) ;
#22474=LINE ( 'NONE', #54300, #29194 ) ;
#22504=EDGE_LOOP ( 'NONE', ( #43828, #66240, #47307, #1990 ) ) ;
#22508=FACE_OUTER_BOUND ( 'NONE', #38659, .T. ) ;
#22526=EDGE_CURVE ( 'NONE', #14272, #40017, #56630, .T. ) ;
#22528=AXIS2_PLACEMENT_3D ( 'NONE', #1243, #60630, #49676 ) ;
#22534=EDGE_CURVE ( 'NONE', #30734, #47809, #13489, .T. ) ;
#22550=CARTESIAN_POINT ( 'NONE',  ( 38.90000000000000568, 20.60000000000000142, -13.86939075806900057 ) ) ;
#22551=ORIENTED_EDGE ( 'NONE', *, *, #50121, .F. ) ;
#22555=FACE_OUTER_BOUND ( 'NONE', #49061, .T. ) ;
#22559=LINE ( 'NONE', #54052, #18351 ) ;
#22569=EDGE_CURVE ( 'NONE', #27390, #26801, #18029, .T. ) ;
#22574=DIRECTION ( 'NONE',  ( 0.000000000000000000, 0.000000000000000000, -1.000000000000000000 ) ) ;
#22597=EDGE_CURVE ( 'NONE', #66031, #36357, #33946, .T. ) ;
#22602=ORIENTED_EDGE ( 'NONE', *, *, #17247, .F. ) ;
#22613=AXIS2_PLACEMENT_3D ( 'NONE', #12632, #33183, #11602 ) ;
#22619=CARTESIAN_POINT ( 'NONE',  ( 22.90000000000000213, -0.2000000000089119934, 8.909539772616881237E-12 ) ) ;
#22622=ORIENTED_EDGE ( 'NONE', *, *, #68959, .T. ) ;
#22623=VECTOR ( 'NONE', #46112, 1000.000000000000000 ) ;
#22628=CARTESIAN_POINT ( 'NONE',  ( 49.00000000000000000, -0.1999999999911430404, -8.864436962241481021E-12 ) ) ;
#22631=DIRECTION ( 'NONE',  ( 1.000000000000000000, -0.000000000000000000, 0.000000000000000000 ) ) ;
#22663=DIRECTION ( 'NONE',  ( 1.000000000000000000, -0.000000000000000000, 0.000000000000000000 ) ) ;
#22669=ORIENTED_EDGE ( 'NONE', *, *, #57556, .T. ) ;
#22670=VERTEX_POINT ( 'NONE', #61506 ) ;
#22688=ORIENTED_EDGE ( 'NONE', *, *, #21739, .T. ) ;
#22698=CARTESIAN_POINT ( 'NONE',  ( 33.89999999999999858, 0.000000000000000000, 0.000000000000000000 ) ) ;
#22705=DIRECTION ( 'NONE',  ( 1.000000000000000000, -0.000000000000000000, 0.000000000000000000 ) ) ;
#22712=CARTESIAN_POINT ( 'NONE',  ( 19.90000000000000213, 13.66939075806899240, -20.79999999999999361 ) ) ;
#22717=ORIENTED_EDGE ( 'NONE', *, *, #35755, .T. ) ;
#22718=ORIENTED_EDGE ( 'NONE', *, *, #35241, .T. ) ;
#22722=CARTESIAN_POINT ( 'NONE',  ( 41.09999999999999432, 13.66939075806899950, -20.80000000000000426 ) ) ;
#22730=CARTESIAN_POINT ( 'NONE',  ( 41.09999999999999432, -0.2000000000000000111, 0.000000000000000000 ) ) ;
#22731=AXIS2_PLACEMENT_3D ( 'NONE', #53598, #17838, #38039 ) ;
#22733=LINE ( 'NONE', #40015, #35161 ) ;
#22737=ORIENTED_EDGE ( 'NONE', *, *, #8882, .F. ) ;
#22751=DIRECTION ( 'NONE',  ( -0.000000000000000000, -0.7071067811865474617, 0.7071067811865474617 ) ) ;
#22752=VECTOR ( 'NONE', #59470, 1000.000000000000000 ) ;
#22775=CARTESIAN_POINT ( 'NONE',  ( 0.000000000000000000, 0.000000000000000000, 0.000000000000000000 ) ) ;
#22781=ORIENTED_EDGE ( 'NONE', *, *, #59779, .T. ) ;
#22791=CARTESIAN_POINT ( 'NONE',  ( 11.90000000000000036, 0.000000000000000000, 4.309871990004491277E-16 ) ) ;
#22801=AXIS2_PLACEMENT_3D ( 'NONE', #19624, #67018, #57110 ) ;
#22806=CONICAL_SURFACE ( 'NONE', #23911, 2.458500000000000796, 1.047019301333029784 ) ;
#22808=CARTESIAN_POINT ( 'NONE',  ( 41.09999999999999432, -0.2000000000000000111, 0.000000000000000000 ) ) ;
#22814=CARTESIAN_POINT ( 'NONE',  ( 46.39999999999999858, 21.00000000000000000, 0.2500000000000000000 ) ) ;
#22821=EDGE_CURVE ( 'NONE', #2624, #69031, #20395, .T. ) ;
#22825=CARTESIAN_POINT ( 'NONE',  ( 41.09999999999999432, -21.00000000000000000, -13.86939075806900057 ) ) ;
#22827=CARTESIAN_POINT ( 'NONE',  ( 25.57999999999999829, 0.000000000000000000, 0.000000000000000000 ) ) ;
#22829=CARTESIAN_POINT ( 'NONE',  ( 40.90000000000000568, -0.2000000000000000111, 0.000000000000000000 ) ) ;
#22838=CARTESIAN_POINT ( 'NONE',  ( 25.57999999999999829, 0.000000000000000000, 0.000000000000000000 ) ) ;
#22863=ADVANCED_FACE ( 'NONE', ( #61333 ), #44375, .T. ) ;
#22876=DIRECTION ( 'NONE',  ( -1.000000000000000000, 0.000000000000000000, 0.000000000000000000 ) ) ;
#22877=ORIENTED_EDGE ( 'NONE', *, *, #44270, .F. ) ;
#22878=ORIENTED_EDGE ( 'NONE', *, *, #56035, .T. ) ;
#22887=( LENGTH_UNIT ( ) NAMED_UNIT ( * ) SI_UNIT ( .MILLI., .METRE. ) );
#22892=CARTESIAN_POINT ( 'NONE',  ( 40.90000000000000568, -0.2000000000000000111, 0.000000000000000000 ) ) ;
#22897=VERTEX_POINT ( 'NONE', #16834 ) ;
#22899=CARTESIAN_POINT ( 'NONE',  ( 55.00000000000000000, 16.96999999999999886, 21.00000000000000000 ) ) ;
#22905=EDGE_CURVE ( 'NONE', #48285, #43972, #6224, .T. ) ;
#22908=STYLED_ITEM ( 'NONE', ( #35243 ), #65828 ) ;
#22920=LINE ( 'NONE', #27535, #36179 ) ;
#22924=FACE_OUTER_BOUND ( 'NONE', #10782, .T. ) ;
#22930=ORIENTED_EDGE ( 'NONE', *, *, #19313, .T. ) ;
#22941=LINE ( 'NONE', #39205, #69616 ) ;
#22945=CARTESIAN_POINT ( 'NONE',  ( 36.90000000000000568, 0.000000000000000000, 2.458500000000000796 ) ) ;
#22953=AXIS2_PLACEMENT_3D ( 'NONE', #7968, #45104, #50069 ) ;
#22959=CIRCLE ( 'NONE', #12798, 2.458500000000000796 ) ;
#22964=VECTOR ( 'NONE', #59337, 1000.000000000000000 ) ;
#22996=CARTESIAN_POINT ( 'NONE',  ( 41.09999999999999432, 13.66939075806899950, 20.80000000000000426 ) ) ;
#23002=FACE_OUTER_BOUND ( 'NONE', #9891, .T. ) ;
#23003=CIRCLE ( 'NONE', #62508, 25.39999999999999858 ) ;
#23004=VECTOR ( 'NONE', #69574, 1000.000000000000000 ) ;
#23013=CARTESIAN_POINT ( 'NONE',  ( 41.09999999999999432, 20.60000000000000142, 13.86939075806900057 ) ) ;
#23039=PLANE ( 'NONE',  #50111 ) ;
#23041=VECTOR ( 'NONE', #10234, 1000.000000000000000 ) ;
#23049=VECTOR ( 'NONE', #4787, 1000.000000000000000 ) ;
#23055=CARTESIAN_POINT ( 'NONE',  ( 22.90000000000000213, -21.00000000000001421, -13.86939075806900945 ) ) ;
#23067=EDGE_CURVE ( 'NONE', #20590, #50665, #29867, .T. ) ;
#23073=CARTESIAN_POINT ( 'NONE',  ( 0.5000000000000000000, -21.00000000000000000, -18.00000000000000355 ) ) ;
#23093=EDGE_LOOP ( 'NONE', ( #61809, #30164, #16836, #56436 ) ) ;
#23133=CIRCLE ( 'NONE', #38940, 24.99999999998789946 ) ;
#23134=DIRECTION ( 'NONE',  ( 0.000000000000000000, 0.000000000000000000, -1.000000000000000000 ) ) ;
#23140=ADVANCED_FACE ( 'NONE', ( #4068 ), #3069, .F. ) ;
#23148=VERTEX_POINT ( 'NONE', #36947 ) ;
#23151=VECTOR ( 'NONE', #54964, 1000.000000000000000 ) ;
#23167=DIRECTION ( 'NONE',  ( 0.000000000000000000, 0.000000000000000000, -1.000000000000000000 ) ) ;
#23169=DIRECTION ( 'NONE',  ( 0.000000000000000000, 1.000000000000000000, -0.000000000000000000 ) ) ;
#23171=VERTEX_POINT ( 'NONE', #15014 ) ;
#23174=EDGE_CURVE ( 'NONE', #34997, #52164, #69107, .T. ) ;
#23178=CARTESIAN_POINT ( 'NONE',  ( 25.90000000000000213, -0.000000000000000000, -20.80000000000000071 ) ) ;
#23190=VECTOR ( 'NONE', #28139, 1000.000000000000000 ) ;
#23191=DIRECTION ( 'NONE',  ( 0.000000000000000000, 0.000000000000000000, 1.000000000000000000 ) ) ;
#23192=ORIENTED_EDGE ( 'NONE', *, *, #2472, .F. ) ;
#23193=ORIENTED_EDGE ( 'NONE', *, *, #41431, .T. ) ;
#23195=CARTESIAN_POINT ( 'NONE',  ( 39.00000000000000000, -0.2000000000000000111, 0.000000000000000000 ) ) ;
#23227=( GEOMETRIC_REPRESENTATION_CONTEXT ( 3 ) GLOBAL_UNCERTAINTY_ASSIGNED_CONTEXT ( ( #69845 ) ) GLOBAL_UNIT_ASSIGNED_CONTEXT ( ( #9067, #63158, #57848 ) ) REPRESENTATION_CONTEXT ( 'NONE', 'WORKASPACE' ) );
#23228=LINE ( 'NONE', #34170, #12801 ) ;
#23244=VECTOR ( 'NONE', #41839, 1000.000000000000000 ) ;
#23261=CARTESIAN_POINT ( 'NONE',  ( 20.90000000000000213, 20.60000000000000142, -13.86939075806900057 ) ) ;
#23267=DIRECTION ( 'NONE',  ( 0.000000000000000000, 1.000000000000000000, -0.000000000000000000 ) ) ;
#23283=DIRECTION ( 'NONE',  ( 0.000000000000000000, 0.000000000000000000, -1.000000000000000000 ) ) ;
#23301=CARTESIAN_POINT ( 'NONE',  ( 10.00000000000000000, -21.00000000000000000, 18.00000000000000355 ) ) ;
#23302=DIRECTION ( 'NONE',  ( 0.000000000000000000, 0.000000000000000000, -1.000000000000000000 ) ) ;
#23315=PLANE ( 'NONE',  #38453 ) ;
#23320=ADVANCED_FACE ( 'NONE', ( #866 ), #17788, .T. ) ;
#23340=PLANE ( 'NONE',  #18847 ) ;
#23346=DIRECTION ( 'NONE',  ( 0.000000000000000000, 0.000000000000000000, 1.000000000000000000 ) ) ;
#23354=DIRECTION ( 'NONE',  ( 0.5001543609659999667, 0.000000000000000000, -0.8659362650950080953 ) ) ;
#23370=VERTEX_POINT ( 'NONE', #62656 ) ;
#23382=CARTESIAN_POINT ( 'NONE',  ( 46.39999999999999858, 33.00000000000000000, -0.2500000000000000000 ) ) ;
#23386=CARTESIAN_POINT ( 'NONE',  ( 25.90000000000000213, -14.06939075806902117, -20.80000000000000426 ) ) ;
#23396=CARTESIAN_POINT ( 'NONE',  ( 0.000000000000000000, -20.50000000000000000, 17.79289321881345032 ) ) ;
#23406=LINE ( 'NONE', #18787, #56012 ) ;
#23414=CARTESIAN_POINT ( 'NONE',  ( 39.90000000000000568, 14.08845687959340331, 21.00000000000000000 ) ) ;
#23421=DIRECTION ( 'NONE',  ( 1.000000000000000000, 0.000000000000000000, 0.000000000000000000 ) ) ;
#23427=AXIS2_PLACEMENT_3D ( 'NONE', #32485, #44444, #48390 ) ;
#23449=AXIS2_PLACEMENT_3D ( 'NONE', #16195, #1320, #6954 ) ;
#23451=CARTESIAN_POINT ( 'NONE',  ( 8.900000000000005684, -14.06939075806900874, 20.80000000000001137 ) ) ;
#23458=DIRECTION ( 'NONE',  ( 0.000000000000000000, 0.000000000000000000, -1.000000000000000000 ) ) ;
#23459=CYLINDRICAL_SURFACE ( 'NONE', #62814, 24.99999999998794920 ) ;
#23469=CARTESIAN_POINT ( 'NONE',  ( 47.00000000000000000, 0.7500000000000000000, 3.418698582794334584 ) ) ;
#23474=ORIENTED_EDGE ( 'NONE', *, *, #5221, .T. ) ;
#23475=EDGE_LOOP ( 'NONE', ( #15649, #15478, #8244, #10327 ) ) ;
#23477=CYLINDRICAL_SURFACE ( 'NONE', #32811, 24.99999999998794920 ) ;
#23486=EDGE_CURVE ( 'NONE', #68001, #13851, #34738, .T. ) ;
#23489=CARTESIAN_POINT ( 'NONE',  ( 46.39999999999999858, 21.00000000000000000, -2.250000000000000444 ) ) ;
#23493=VECTOR ( 'NONE', #69366, 1000.000000000000000 ) ;
#23495=ORIENTED_EDGE ( 'NONE', *, *, #41114, .T. ) ;
#23500=ORIENTED_EDGE ( 'NONE', *, *, #45403, .T. ) ;
#23506=FACE_OUTER_BOUND ( 'NONE', #59486, .T. ) ;
#23509=VERTEX_POINT ( 'NONE', #52788 ) ;
#23535=CARTESIAN_POINT ( 'NONE',  ( 9.899999999999998579, -0.1999999999911430404, -8.864436962241481021E-12 ) ) ;
#23539=CARTESIAN_POINT ( 'NONE',  ( 25.57999999999999829, 0.000000000000000000, 0.000000000000000000 ) ) ;
#23543=DIRECTION ( 'NONE',  ( -1.000000000000000000, 0.000000000000000000, 0.000000000000000000 ) ) ;
#23550=DIRECTION ( 'NONE',  ( 0.000000000000000000, 1.000000000000000000, 0.000000000000000000 ) ) ;
#23553=ORIENTED_EDGE ( 'NONE', *, *, #69952, .F. ) ;
#23555=ORIENTED_EDGE ( 'NONE', *, *, #4609, .F. ) ;
#23563=EDGE_CURVE ( 'NONE', #44820, #57287, #51676, .T. ) ;
#23567=ADVANCED_FACE ( 'NONE', ( #9988, #63374 ), #41796, .T. ) ;
#23568=FACE_OUTER_BOUND ( 'NONE', #12494, .T. ) ;
#23572=EDGE_CURVE ( 'NONE', #61504, #34324, #58435, .T. ) ;
#23578=CARTESIAN_POINT ( 'NONE',  ( 49.00000000000000000, -0.2000000000089119934, 8.909539772616881237E-12 ) ) ;
#23585=DIRECTION ( 'NONE',  ( 0.000000000000000000, 0.000000000000000000, -1.000000000000000000 ) ) ;
#23602=EDGE_LOOP ( 'NONE', ( #3280, #46266, #28348, #34303 ) ) ;
#23611=EDGE_CURVE ( 'NONE', #4446, #8645, #26245, .T. ) ;
#23612=DIRECTION ( 'NONE',  ( 1.000000000000000000, 0.000000000000000000, 0.000000000000000000 ) ) ;
#23614=LINE ( 'NONE', #50832, #49225 ) ;
#23620=CARTESIAN_POINT ( 'NONE',  ( 17.89999999999999858, -21.00000000000001421, -13.86939075806900945 ) ) ;
#23640=DIRECTION ( 'NONE',  ( -1.000000000000000000, 0.000000000000000000, 0.000000000000000000 ) ) ;
#23653=CARTESIAN_POINT ( 'NONE',  ( 32.89999999999999858, -0.2000000000089119934, -8.913009219568841313E-12 ) ) ;
#23659=ORIENTED_EDGE ( 'NONE', *, *, #22469, .F. ) ;
#23666=DIRECTION ( 'NONE',  ( 0.000000000000000000, 0.000000000000000000, -1.000000000000000000 ) ) ;
#23690=ADVANCED_FACE ( 'NONE', ( #49543, #38593 ), #21977, .F. ) ;
#23693=ORIENTED_EDGE ( 'NONE', *, *, #16236, .F. ) ;
#23721=DIRECTION ( 'NONE',  ( -1.000000000000000000, 0.000000000000000000, 0.000000000000000000 ) ) ;
#23725=EDGE_CURVE ( 'NONE', #56183, #64226, #39273, .T. ) ;
#23729=ADVANCED_FACE ( 'NONE', ( #16687 ), #38253, .F. ) ;
#23739=DIRECTION ( 'NONE',  ( 0.000000000000000000, 0.000000000000000000, 1.000000000000000000 ) ) ;
#23740=ORIENTED_EDGE ( 'NONE', *, *, #29111, .F. ) ;
#23753=ORIENTED_EDGE ( 'NONE', *, *, #65792, .F. ) ;
#23777=CARTESIAN_POINT ( 'NONE',  ( 9.899999999999998579, 20.60000000000000142, -13.86939075806900057 ) ) ;
#23782=VECTOR ( 'NONE', #47665, 1000.000000000000000 ) ;
#23783=CARTESIAN_POINT ( 'NONE',  ( 39.00000000000000000, -21.00000000000000000, 16.96999999999999886 ) ) ;
#23794=DIRECTION ( 'NONE',  ( 0.000000000000000000, 0.000000000000000000, -1.000000000000000000 ) ) ;
#23801=CARTESIAN_POINT ( 'NONE',  ( 39.00000000000000000, -16.96999999999999886, -21.00000000000000000 ) ) ;
#23805=CIRCLE ( 'NONE', #2351, 0.5000000000000000000 ) ;
#23813=ORIENTED_EDGE ( 'NONE', *, *, #17282, .T. ) ;
#23819=CARTESIAN_POINT ( 'NONE',  ( 28.90000000000000213, -14.06939075806900874, 20.80000000000001137 ) ) ;
#23858=CARTESIAN_POINT ( 'NONE',  ( 47.00000000000000000, 0.000000000000000000, 0.000000000000000000 ) ) ;
#23880=ORIENTED_EDGE ( 'NONE', *, *, #24319, .T. ) ;
#23884=PLANE ( 'NONE',  #20273 ) ;
#23890=PLANE ( 'NONE',  #45863 ) ;
#23893=CARTESIAN_POINT ( 'NONE',  ( 19.90000000000000213, -21.00000000000000000, 13.86939075806900057 ) ) ;
#23895=LINE ( 'NONE', #45806, #12791 ) ;
#23896=CYLINDRICAL_SURFACE ( 'NONE', #65508, 24.99999999998794920 ) ;
#23898=VECTOR ( 'NONE', #25419, 1000.000000000000000 ) ;
#23905=VECTOR ( 'NONE', #9282, 1000.000000000000000 ) ;
#23911=AXIS2_PLACEMENT_3D ( 'NONE', #29353, #65807, #60495 ) ;
#23919=AXIS2_PLACEMENT_3D ( 'NONE', #14209, #63360, #25884 ) ;
#23925=CARTESIAN_POINT ( 'NONE',  ( 39.00000000000000000, 21.00000000000000000, -16.96999999999999886 ) ) ;
#23933=AXIS2_PLACEMENT_3D ( 'NONE', #11552, #10880, #977 ) ;
#23942=CARTESIAN_POINT ( 'NONE',  ( 7.900000000000000355, 21.00000000000000000, -18.00000000000000355 ) ) ;
#23950=AXIS2_PLACEMENT_3D ( 'NONE', #15036, #64529, #53571 ) ;
#23951=FACE_OUTER_BOUND ( 'NONE', #32009, .T. ) ;
#23959=ORIENTED_EDGE ( 'NONE', *, *, #15851, .F. ) ;
#23960=ADVANCED_FACE ( 'NONE', ( #58349 ), #62941, .F. ) ;
#23981=ORIENTED_EDGE ( 'NONE', *, *, #31964, .T. ) ;
#23983=VERTEX_POINT ( 'NONE', #20154 ) ;
#24004=DIRECTION ( 'NONE',  ( -1.000000000000000000, 0.000000000000000000, 0.000000000000000000 ) ) ;
#24008=CARTESIAN_POINT ( 'NONE',  ( 16.89999999999999858, 13.66939075806899950, 20.80000000000000426 ) ) ;
#24010=VECTOR ( 'NONE', #58227, 1000.000000000000000 ) ;
#24018=CARTESIAN_POINT ( 'NONE',  ( 40.90000000000000568, 21.00000000000000000, 16.96999999999999886 ) ) ;
#24028=EDGE_LOOP ( 'NONE', ( #26116, #65613, #9300, #25827 ) ) ;
#24031=AXIS2_PLACEMENT_3D ( 'NONE', #158, #27373, #21717 ) ;
#24042=ORIENTED_EDGE ( 'NONE', *, *, #39684, .T. ) ;
#24052=ORIENTED_EDGE ( 'NONE', *, *, #14884, .F. ) ;
#24059=CARTESIAN_POINT ( 'NONE',  ( 39.00000000000000000, 21.00000000000000000, 16.96999999999999886 ) ) ;
#24062=DIRECTION ( 'NONE',  ( -1.000000000000000000, 0.000000000000000000, 0.000000000000000000 ) ) ;
#24063=ORIENTED_EDGE ( 'NONE', *, *, #13586, .F. ) ;
#24067=CARTESIAN_POINT ( 'NONE',  ( 49.00000000000000000, -0.1999999999911430404, -8.864436962241481021E-12 ) ) ;
#24081=DIRECTION ( 'NONE',  ( 0.000000000000000000, 0.000000000000000000, -1.000000000000000000 ) ) ;
#24082=LINE ( 'NONE', #23396, #43551 ) ;
#24104=EDGE_LOOP ( 'NONE', ( #46662, #43113, #59502, #54863, #22602, #60083, #69611, #47357 ) ) ;
#24107=EDGE_LOOP ( 'NONE', ( #9396, #10365, #33752, #19241, #25588, #14365, #44535, #26771 ) ) ;
#24114=EDGE_CURVE ( 'NONE', #26801, #36169, #1364, .T. ) ;
#24116=FACE_OUTER_BOUND ( 'NONE', #46108, .T. ) ;
#24118=DIRECTION ( 'NONE',  ( 1.000000000000000000, -0.000000000000000000, 0.000000000000000000 ) ) ;
#24121=VERTEX_POINT ( 'NONE', #59724 ) ;
#24128=CIRCLE ( 'NONE', #4969, 2.458500000000000796 ) ;
#24131=CARTESIAN_POINT ( 'NONE',  ( 7.900000000000000355, -21.00000000000000000, 14.57806571531351914 ) ) ;
#24135=ORIENTED_EDGE ( 'NONE', *, *, #31966, .T. ) ;
#24141=CARTESIAN_POINT ( 'NONE',  ( 49.00000000000000000, -14.06939075806900163, -20.80000000000000426 ) ) ;
#24142=CARTESIAN_POINT ( 'NONE',  ( 48.50000000000000000, 0.7500000000000000000, -3.418698582794335028 ) ) ;
#24162=CARTESIAN_POINT ( 'NONE',  ( 39.90000000000000568, -16.96999999999999886, 21.00000000000000000 ) ) ;
#24167=LINE ( 'NONE', #5422, #59115 ) ;
#24180=PLANE ( 'NONE',  #54867 ) ;
#24185=VECTOR ( 'NONE', #62811, 1000.000000000000000 ) ;
#24194=DIRECTION ( 'NONE',  ( -1.000000000000000000, 0.000000000000000000, 0.000000000000000000 ) ) ;
#24196=CARTESIAN_POINT ( 'NONE',  ( 12.90000000000000213, -21.00000000000000000, 13.86939075806900057 ) ) ;
#24214=AXIS2_PLACEMENT_3D ( 'NONE', #32060, #26760, #60304 ) ;
#24215=VECTOR ( 'NONE', #46693, 1000.000000000000000 ) ;
#24228=LINE ( 'NONE', #40120, #56007 ) ;
#24234=PLANE ( 'NONE',  #46514 ) ;
#24245=DIRECTION ( 'NONE',  ( 0.000000000000000000, 1.000000000000000000, 0.000000000000000000 ) ) ;
#24272=CARTESIAN_POINT ( 'NONE',  ( 39.00000000000000000, 14.08845687959340331, -21.00000000000000000 ) ) ;
#24281=CARTESIAN_POINT ( 'NONE',  ( 21.90000000000000213, -21.00000000000000000, 13.86939075806900057 ) ) ;
#24284=CIRCLE ( 'NONE', #68308, 2.458500000000000796 ) ;
#24288=CARTESIAN_POINT ( 'NONE',  ( 31.89999999999999858, 20.60000000000000142, 13.86939075806899702 ) ) ;
#24302=EDGE_LOOP ( 'NONE', ( #47554, #55744 ) ) ;
#24305=CARTESIAN_POINT ( 'NONE',  ( 9.899999999999998579, -0.2000000000000000111, 0.000000000000000000 ) ) ;
#24307=SURFACE_SIDE_STYLE ('',( #19344 ) ) ;
#24310=LINE ( 'NONE', #2393, #39895 ) ;
#24312=CIRCLE ( 'NONE', #63851, 5.000000000000000000 ) ;
#24313=VECTOR ( 'NONE', #65359, 1000.000000000000000 ) ;
#24314=AXIS2_PLACEMENT_3D ( 'NONE', #57221, #31052, #35276 ) ;
#24316=CARTESIAN_POINT ( 'NONE',  ( 35.89999999999999858, -0.000000000000000000, -20.80000000000000071 ) ) ;
#24319=EDGE_CURVE ( 'NONE', #29208, #48285, #2054, .T. ) ;
#24321=VECTOR ( 'NONE', #21478, 1000.000000000000000 ) ;
#24329=EDGE_LOOP ( 'NONE', ( #12773, #20578, #16650, #37757 ) ) ;
#24336=VECTOR ( 'NONE', #63001, 1000.000000000000000 ) ;
#24343=EDGE_LOOP ( 'NONE', ( #68359, #53502, #63396, #28279 ) ) ;
#24345=VERTEX_POINT ( 'NONE', #57889 ) ;
#24366=CARTESIAN_POINT ( 'NONE',  ( 46.39999999999999858, 21.00000000000000000, 2.250000000000000444 ) ) ;
#24370=FACE_OUTER_BOUND ( 'NONE', #40170, .T. ) ;
#24379=ORIENTED_EDGE ( 'NONE', *, *, #55040, .F. ) ;
#24386=DIRECTION ( 'NONE',  ( 1.000000000000000000, 0.000000000000000000, 0.000000000000000000 ) ) ;
#24398=ORIENTED_EDGE ( 'NONE', *, *, #47372, .T. ) ;
#24404=ADVANCED_FACE ( 'NONE', ( #8757 ), #10155, .T. ) ;
#24420=DIRECTION ( 'NONE',  ( -1.000000000000000000, 0.000000000000000000, 0.000000000000000000 ) ) ;
#24427=VECTOR ( 'NONE', #69752, 1000.000000000000000 ) ;
#24431=ORIENTED_EDGE ( 'NONE', *, *, #56547, .F. ) ;
#24456=ORIENTED_EDGE ( 'NONE', *, *, #60108, .T. ) ;
#24463=LINE ( 'NONE', #46715, #32380 ) ;
#24470=CARTESIAN_POINT ( 'NONE',  ( 30.90000000000000213, -0.2000000000089119934, 8.909539772616881237E-12 ) ) ;
#24473=ORIENTED_EDGE ( 'NONE', *, *, #1934, .T. ) ;
#24478=DIRECTION ( 'NONE',  ( 1.000000000000000000, 0.000000000000000000, 0.000000000000000000 ) ) ;
#24482=AXIS2_PLACEMENT_3D ( 'NONE', #65321, #38104, #43039 ) ;
#24506=FACE_OUTER_BOUND ( 'NONE', #24958, .T. ) ;
#24507=DIRECTION ( 'NONE',  ( 1.000000000000000000, -0.000000000000000000, 0.000000000000000000 ) ) ;
#24529=ORIENTED_EDGE ( 'NONE', *, *, #59604, .T. ) ;
#24540=CARTESIAN_POINT ( 'NONE',  ( 35.89999999999999858, -0.1999999999911430404, -8.864436962241481021E-12 ) ) ;
#24542=EDGE_LOOP ( 'NONE', ( #40297, #38524, #10619, #52676 ) ) ;
#24563=CARTESIAN_POINT ( 'NONE',  ( 40.90000000000000568, 13.66939075806899240, -20.79999999999999361 ) ) ;
#24565=ORIENTED_EDGE ( 'NONE', *, *, #9376, .F. ) ;
#24566=AXIS2_PLACEMENT_3D ( 'NONE', #24708, #19394, #9148 ) ;
#24567=VECTOR ( 'NONE', #33082, 1000.000000000000000 ) ;
#24579=VECTOR ( 'NONE', #12231, 1000.000000000000000 ) ;
#24580=CARTESIAN_POINT ( 'NONE',  ( 21.90000000000000213, -0.1999999999911430404, -8.864436962241481021E-12 ) ) ;
#24583=DIRECTION ( 'NONE',  ( 0.000000000000000000, 0.000000000000000000, 1.000000000000000000 ) ) ;
#24595=DIRECTION ( 'NONE',  ( 0.000000000000000000, 0.7071067811865474617, -0.7071067811865474617 ) ) ;
#24604=CARTESIAN_POINT ( 'NONE',  ( 35.89999999999999858, -0.1999999999911795112, 8.826273045769999343E-12 ) ) ;
#24606=FACE_OUTER_BOUND ( 'NONE', #67842, .T. ) ;
#24608=CIRCLE ( 'NONE', #67513, 24.99999999998794920 ) ;
#24611=VERTEX_POINT ( 'NONE', #69558 ) ;
#24618=ADVANCED_FACE ( 'NONE', ( #13886 ), #51729, .T. ) ;
#24620=ORIENTED_EDGE ( 'NONE', *, *, #52744, .T. ) ;
#24621=LINE ( 'NONE', #29907, #25979 ) ;
#24624=EDGE_CURVE ( 'NONE', #31019, #62485, #66926, .T. ) ;
#24647=VERTEX_POINT ( 'NONE', #29798 ) ;
#24684=CIRCLE ( 'NONE', #17908, 24.99999999998789946 ) ;
#24688=VERTEX_POINT ( 'NONE', #19192 ) ;
#24700=ORIENTED_EDGE ( 'NONE', *, *, #47324, .F. ) ;
#24703=ORIENTED_EDGE ( 'NONE', *, *, #68283, .T. ) ;
#24708=CARTESIAN_POINT ( 'NONE',  ( 49.00000000000000000, -14.06939075806900163, -20.80000000000000426 ) ) ;
#24709=CARTESIAN_POINT ( 'NONE',  ( 41.09999999999999432, 20.60000000000000142, 13.86939075806900057 ) ) ;
#24717=DIRECTION ( 'NONE',  ( 0.000000000000000000, 0.000000000000000000, -1.000000000000000000 ) ) ;
#24718=ADVANCED_FACE ( 'NONE', ( #14590 ), #67988, .T. ) ;
#24720=CARTESIAN_POINT ( 'NONE',  ( 25.57999999999999829, 3.010794155703768650E-16, -2.458500000000000796 ) ) ;
#24731=DIRECTION ( 'NONE',  ( 0.000000000000000000, 0.000000000000000000, 1.000000000000000000 ) ) ;
#24734=AXIS2_PLACEMENT_3D ( 'NONE', #43765, #60348, #54724 ) ;
#24766=CIRCLE ( 'NONE', #7835, 24.99999999998794920 ) ;
#24773=ADVANCED_FACE ( 'NONE', ( #42857 ), #58445, .T. ) ;
#24775=ORIENTED_EDGE ( 'NONE', *, *, #3185, .T. ) ;
#24779=CYLINDRICAL_SURFACE ( 'NONE', #55911, 24.99999999998789946 ) ;
#24786=LINE ( 'NONE', #8504, #1694 ) ;
#24789=EDGE_LOOP ( 'NONE', ( #1263, #5616, #58358, #18943 ) ) ;
#24791=AXIS2_PLACEMENT_3D ( 'NONE', #63215, #51562, #35630 ) ;
#24793=DIRECTION ( 'NONE',  ( 0.000000000000000000, 0.000000000000000000, -1.000000000000000000 ) ) ;
#24813=DIRECTION ( 'NONE',  ( 0.000000000000000000, -1.000000000000000000, 0.000000000000000000 ) ) ;
#24820=DIRECTION ( 'NONE',  ( 0.000000000000000000, 0.000000000000000000, -1.000000000000000000 ) ) ;
#24834=DIRECTION ( 'NONE',  ( 0.000000000000000000, 0.000000000000000000, -1.000000000000000000 ) ) ;
#24837=VERTEX_POINT ( 'NONE', #47811 ) ;
#24886=DIRECTION ( 'NONE',  ( 1.000000000000000000, -0.000000000000000000, 0.000000000000000000 ) ) ;
#24900=DIRECTION ( 'NONE',  ( 0.000000000000000000, 0.000000000000000000, -1.000000000000000000 ) ) ;
#24901=CARTESIAN_POINT ( 'NONE',  ( 50.00000000000000711, 0.7500000000000000000, -4.943429983321300902 ) ) ;
#24908=ORIENTED_EDGE ( 'NONE', *, *, #4827, .T. ) ;
#24918=CARTESIAN_POINT ( 'NONE',  ( 10.00000000000000000, -21.00000000000000000, -18.00000000000000355 ) ) ;
#24921=CARTESIAN_POINT ( 'NONE',  ( 36.90000000000000568, -14.06939075806902117, -20.80000000000000426 ) ) ;
#24926=VECTOR ( 'NONE', #7952, 1000.000000000000000 ) ;
#24936=ORIENTED_EDGE ( 'NONE', *, *, #31085, .F. ) ;
#24958=EDGE_LOOP ( 'NONE', ( #10445, #67973, #29603, #13214 ) ) ;
#24962=CARTESIAN_POINT ( 'NONE',  ( 19.90000000000000213, -14.06939075806902117, -20.80000000000000426 ) ) ;
#24964=CARTESIAN_POINT ( 'NONE',  ( 12.90000000000000213, 20.60000000000000142, 13.86939075806900057 ) ) ;
#24967=DIRECTION ( 'NONE',  ( 0.000000000000000000, 0.000000000000000000, -1.000000000000000000 ) ) ;
#24969=ORIENTED_EDGE ( 'NONE', *, *, #27444, .T. ) ;
#25013=FILL_AREA_STYLE ('',( #3446 ) ) ;
#25016=ORIENTED_EDGE ( 'NONE', *, *, #57389, .T. ) ;
#25028=AXIS2_PLACEMENT_3D ( 'NONE', #40321, #57542, #12050 ) ;
#25029=CLOSED_SHELL ( 'NONE', ( #56369, #61287, #17014, #23320, #40966, #19396 ) ) ;
#25033=DIRECTION ( 'NONE',  ( -1.000000000000000000, 0.000000000000000000, 0.000000000000000000 ) ) ;
#25078=LINE ( 'NONE', #69618, #64087 ) ;
#25082=EDGE_CURVE ( 'NONE', #31241, #7152, #35718, .T. ) ;
#25086=LINE ( 'NONE', #62200, #65463 ) ;
#25113=CIRCLE ( 'NONE', #34124, 25.39999999999999858 ) ;
#25115=EDGE_CURVE ( 'NONE', #34859, #54853, #5593, .T. ) ;
#25116=ORIENTED_EDGE ( 'NONE', *, *, #5930, .F. ) ;
#25117=ORIENTED_EDGE ( 'NONE', *, *, #16236, .T. ) ;
#25119=CARTESIAN_POINT ( 'NONE',  ( 36.90000000000000568, -14.06939075806900163, -20.80000000000000426 ) ) ;
#25121=LINE ( 'NONE', #30069, #69365 ) ;
#25124=VECTOR ( 'NONE', #18580, 1000.000000000000000 ) ;
#25148=DIRECTION ( 'NONE',  ( 0.000000000000000000, 0.7071067811865474617, 0.7071067811865474617 ) ) ;
#25150=EDGE_CURVE ( 'NONE', #17757, #16609, #7788, .T. ) ;
#25175=DIRECTION ( 'NONE',  ( -1.000000000000000000, 0.000000000000000000, 0.000000000000000000 ) ) ;
#25184=CIRCLE ( 'NONE', #19518, 24.99999999998789946 ) ;
#25194=DIRECTION ( 'NONE',  ( -1.000000000000000000, 0.000000000000000000, 0.000000000000000000 ) ) ;
#25211=FACE_OUTER_BOUND ( 'NONE', #3463, .T. ) ;
#25216=EDGE_LOOP ( 'NONE', ( #57827, #29712 ) ) ;
#25223=EDGE_LOOP ( 'NONE', ( #33044, #41876, #66320, #42139 ) ) ;
#25228=ORIENTED_EDGE ( 'NONE', *, *, #59604, .F. ) ;
#25230=EDGE_LOOP ( 'NONE', ( #57013, #35708 ) ) ;
#25233=DIRECTION ( 'NONE',  ( 0.000000000000000000, 0.000000000000000000, -1.000000000000000000 ) ) ;
#25240=CARTESIAN_POINT ( 'NONE',  ( 18.89999999999999858, -0.2000000000089119934, 8.909539772616881237E-12 ) ) ;
#25249=CARTESIAN_POINT ( 'NONE',  ( 46.39999999999999858, 33.00000000000000000, -0.7500000000000000000 ) ) ;
#25252=AXIS2_PLACEMENT_3D ( 'NONE', #65936, #17508, #66989 ) ;
#25253=EDGE_CURVE ( 'NONE', #69832, #29208, #4489, .T. ) ;
#25258=ADVANCED_FACE ( 'NONE', ( #15911 ), #3909, .T. ) ;
#25277=SURFACE_STYLE_FILL_AREA ( #57100 ) ;
#25299=VECTOR ( 'NONE', #26603, 1000.000000000000000 ) ;
#25320=DIRECTION ( 'NONE',  ( 0.000000000000000000, 0.000000000000000000, -1.000000000000000000 ) ) ;
#25323=COLOUR_RGB ( '', 0.72549020, 0.75294118, 0.79215686) ;
#25325=DIRECTION ( 'NONE',  ( 0.000000000000000000, 0.7071067811865474617, 0.7071067811865474617 ) ) ;
#25329=DIRECTION ( 'NONE',  ( 0.000000000000000000, 0.000000000000000000, -1.000000000000000000 ) ) ;
#25338=LINE ( 'NONE', #51863, #3716 ) ;
#25359=ORIENTED_EDGE ( 'NONE', *, *, #3889, .F. ) ;
#25374=VERTEX_POINT ( 'NONE', #16249 ) ;
#25377=EDGE_LOOP ( 'NONE', ( #41614, #7906, #11715, #34917, #33541, #15611, #56687, #30255 ) ) ;
#25381=FACE_OUTER_BOUND ( 'NONE', #42024, .T. ) ;
#25386=ORIENTED_EDGE ( 'NONE', *, *, #33124, .T. ) ;
#25393=DIRECTION ( 'NONE',  ( 1.000000000000000000, -0.000000000000000000, 0.000000000000000000 ) ) ;
#25404=EDGE_LOOP ( 'NONE', ( #4239, #48354, #18403, #29515 ) ) ;
#25406=ORIENTED_EDGE ( 'NONE', *, *, #46259, .T. ) ;
#25409=EDGE_CURVE ( 'NONE', #27271, #64422, #11619, .T. ) ;
#25412=LINE ( 'NONE', #68556, #1919 ) ;
#25416=CARTESIAN_POINT ( 'NONE',  ( 8.900000000000005684, 13.66939075806899240, 20.79999999999999361 ) ) ;
#25419=DIRECTION ( 'NONE',  ( 0.000000000000000000, 0.000000000000000000, 1.000000000000000000 ) ) ;
#25420=ORIENTED_EDGE ( 'NONE', *, *, #36832, .T. ) ;
#25421=DIRECTION ( 'NONE',  ( 1.000000000000000000, -0.000000000000000000, 0.000000000000000000 ) ) ;
#25423=DIRECTION ( 'NONE',  ( -1.000000000000000000, 0.000000000000000000, 0.000000000000000000 ) ) ;
#25428=EDGE_CURVE ( 'NONE', #15393, #27271, #59389, .T. ) ;
#25439=VECTOR ( 'NONE', #47391, 1000.000000000000000 ) ;
#25440=DIRECTION ( 'NONE',  ( -1.000000000000000000, 0.000000000000000000, 0.000000000000000000 ) ) ;
#25459=ORIENTED_EDGE ( 'NONE', *, *, #50260, .T. ) ;
#25465=ORIENTED_EDGE ( 'NONE', *, *, #49198, .T. ) ;
#25479=CARTESIAN_POINT ( 'NONE',  ( 41.09999999999999432, 20.60000000000000142, -13.86939075806900057 ) ) ;
#25481=ADVANCED_FACE ( 'NONE', ( #28931 ), #1713, .F. ) ;
#25486=AXIS2_PLACEMENT_3D ( 'NONE', #8024, #51883, #3098 ) ;
#25492=DIRECTION ( 'NONE',  ( 0.000000000000000000, 0.7071067811865474617, 0.7071067811865474617 ) ) ;
#25494=VERTEX_POINT ( 'NONE', #23620 ) ;
#25496=ADVANCED_FACE ( 'NONE', ( #34577 ), #56166, .T. ) ;
#25502=ORIENTED_EDGE ( 'NONE', *, *, #39297, .F. ) ;
#25508=DIRECTION ( 'NONE',  ( 1.000000000000000000, -0.000000000000000000, 0.000000000000000000 ) ) ;
#25517=ORIENTED_EDGE ( 'NONE', *, *, #20444, .T. ) ;
#25530=CARTESIAN_POINT ( 'NONE',  ( 40.90000000000000568, -21.00000000000000000, 16.96999999999999886 ) ) ;
#25537=FACE_OUTER_BOUND ( 'NONE', #8940, .T. ) ;
#25568=CARTESIAN_POINT ( 'NONE',  ( 10.90000000000000036, 13.66939075806899240, -20.79999999999999361 ) ) ;
#25575=ORIENTED_EDGE ( 'NONE', *, *, #38294, .T. ) ;
#25588=ORIENTED_EDGE ( 'NONE', *, *, #8572, .F. ) ;
#25598=ORIENTED_EDGE ( 'NONE', *, *, #26936, .T. ) ;
#25601=VECTOR ( 'NONE', #64986, 1000.000000000000000 ) ;
#25608=DIRECTION ( 'NONE',  ( 0.000000000000000000, -1.000000000000000000, 0.000000000000000000 ) ) ;
#25611=CARTESIAN_POINT ( 'NONE',  ( 39.00000000000000000, 16.96999999999999886, -21.00000000000000000 ) ) ;
#25614=ORIENTED_EDGE ( 'NONE', *, *, #43121, .F. ) ;
#25625=ORIENTED_EDGE ( 'NONE', *, *, #40132, .T. ) ;
#25626=CARTESIAN_POINT ( 'NONE',  ( 30.90000000000000213, -21.00000000000000000, 13.86939075806900057 ) ) ;
#25637=EDGE_LOOP ( 'NONE', ( #38258, #68471, #25459, #27054 ) ) ;
#25646=DIRECTION ( 'NONE',  ( 0.000000000000000000, 0.000000000000000000, -1.000000000000000000 ) ) ;
#25647=EDGE_LOOP ( 'NONE', ( #17919, #64132, #11838, #32130 ) ) ;
#25649=ADVANCED_FACE ( 'NONE', ( #9120 ), #63920, .T. ) ;
#25656=AXIS2_PLACEMENT_3D ( 'NONE', #19323, #62444, #68474 ) ;
#25685=CARTESIAN_POINT ( 'NONE',  ( 39.00000000000000000, 6.429395695523604153E-16, -5.250000000000000000 ) ) ;
#25688=EDGE_LOOP ( 'NONE', ( #7954, #22781, #18744, #65805 ) ) ;
#25692=CIRCLE ( 'NONE', #13245, 24.99999999998789946 ) ;
#25693=DIRECTION ( 'NONE',  ( 0.000000000000000000, 0.000000000000000000, 1.000000000000000000 ) ) ;
#25717=CARTESIAN_POINT ( 'NONE',  ( 39.00000000000000000, 16.96999999999999886, -21.00000000000000000 ) ) ;
#25722=LINE ( 'NONE', #42313, #34994 ) ;
#25735=DIRECTION ( 'NONE',  ( 0.000000000000000000, 0.000000000000000000, -1.000000000000000000 ) ) ;
#25744=ADVANCED_FACE ( 'NONE', ( #25381 ), #46941, .T. ) ;
#25753=LINE ( 'NONE', #3817, #37974 ) ;
#25758=ORIENTED_EDGE ( 'NONE', *, *, #33390, .F. ) ;
#25759=EDGE_CURVE ( 'NONE', #23983, #34243, #42891, .T. ) ;
#25764=ORIENTED_EDGE ( 'NONE', *, *, #11246, .F. ) ;
#25772=FACE_OUTER_BOUND ( 'NONE', #5150, .T. ) ;
#25775=LINE ( 'NONE', #8793, #41373 ) ;
#25797=CARTESIAN_POINT ( 'NONE',  ( 24.90000000000000213, -21.00000000000000000, 13.86939075806900057 ) ) ;
#25802=EDGE_CURVE ( 'NONE', #30511, #47484, #58958, .T. ) ;
#25808=LINE ( 'NONE', #20139, #28858 ) ;
#25816=ORIENTED_EDGE ( 'NONE', *, *, #54556, .F. ) ;
#25817=CARTESIAN_POINT ( 'NONE',  ( 8.900000000000002132, 18.00000000000000355, 21.00000000000000000 ) ) ;
#25818=ORIENTED_EDGE ( 'NONE', *, *, #69856, .F. ) ;
#25822=CARTESIAN_POINT ( 'NONE',  ( 55.00000000000000000, 16.96999999999999886, -21.00000000000000000 ) ) ;
#25827=ORIENTED_EDGE ( 'NONE', *, *, #65958, .F. ) ;
#25831=DIRECTION ( 'NONE',  ( 0.000000000000000000, 0.000000000000000000, 1.000000000000000000 ) ) ;
#25849=ORIENTED_EDGE ( 'NONE', *, *, #35645, .F. ) ;
#25852=CYLINDRICAL_SURFACE ( 'NONE', #43212, 2.458500000000000796 ) ;
#25857=DIRECTION ( 'NONE',  ( 0.000000000000000000, -1.000000000000000000, 0.000000000000000000 ) ) ;
#25870=CARTESIAN_POINT ( 'NONE',  ( 18.89999999999999858, 13.66939075806899950, 20.80000000000000426 ) ) ;
#25884=DIRECTION ( 'NONE',  ( 0.000000000000000000, 0.000000000000000000, -1.000000000000000000 ) ) ;
#25891=CARTESIAN_POINT ( 'NONE',  ( 10.00000000000000000, 18.00000000000000355, -21.00000000000000000 ) ) ;
#25898=ADVANCED_FACE ( 'NONE', ( #18947 ), #23896, .T. ) ;
#25904=DIRECTION ( 'NONE',  ( -1.000000000000000000, 0.000000000000000000, -0.000000000000000000 ) ) ;
#25912=VERTEX_POINT ( 'NONE', #61724 ) ;
#25936=ORIENTED_EDGE ( 'NONE', *, *, #13277, .F. ) ;
#25940=ORIENTED_EDGE ( 'NONE', *, *, #64230, .F. ) ;
#25943=ORIENTED_EDGE ( 'NONE', *, *, #7995, .F. ) ;
#25960=DIRECTION ( 'NONE',  ( 0.000000000000000000, -1.000000000000000000, 0.000000000000000000 ) ) ;
#25962=DIRECTION ( 'NONE',  ( 0.000000000000000000, 1.000000000000000000, 0.000000000000000000 ) ) ;
#25965=ADVANCED_FACE ( 'NONE', ( #24606 ), #28838, .T. ) ;
#25978=EDGE_LOOP ( 'NONE', ( #51042, #66559, #51308, #2835 ) ) ;
#25979=VECTOR ( 'NONE', #2685, 1000.000000000000000 ) ;
#25987=FACE_OUTER_BOUND ( 'NONE', #10438, .T. ) ;
#25988=FACE_OUTER_BOUND ( 'NONE', #50428, .T. ) ;
#25992=LINE ( 'NONE', #47550, #50903 ) ;
#25993=ORIENTED_EDGE ( 'NONE', *, *, #52163, .F. ) ;
#26002=ORIENTED_EDGE ( 'NONE', *, *, #54153, .T. ) ;
#26010=EDGE_CURVE ( 'NONE', #31468, #53653, #41202, .T. ) ;
#26020=ORIENTED_EDGE ( 'NONE', *, *, #40487, .T. ) ;
#26021=ORIENTED_EDGE ( 'NONE', *, *, #8792, .T. ) ;
#26028=DIRECTION ( 'NONE',  ( -1.000000000000000000, -0.000000000000000000, -0.000000000000000000 ) ) ;
#26030=AXIS2_PLACEMENT_3D ( 'NONE', #37592, #1728, #23302 ) ;
#26036=CIRCLE ( 'NONE', #2296, 24.99999999998789946 ) ;
#26052=LINE ( 'NONE', #43700, #53478 ) ;
#26054=ORIENTED_EDGE ( 'NONE', *, *, #6473, .F. ) ;
#26059=CARTESIAN_POINT ( 'NONE',  ( 46.39999999999999858, 21.00000000000000000, 2.250000000000000444 ) ) ;
#26087=VECTOR ( 'NONE', #24194, 1000.000000000000000 ) ;
#26088=ORIENTED_EDGE ( 'NONE', *, *, #66371, .F. ) ;
#26089=DIRECTION ( 'NONE',  ( -1.000000000000000000, 0.000000000000000000, 0.000000000000000000 ) ) ;
#26095=EDGE_CURVE ( 'NONE', #4872, #37027, #33737, .T. ) ;
#26098=ADVANCED_FACE ( 'NONE', ( #3731 ), #52529, .F. ) ;
#26105=VECTOR ( 'NONE', #23794, 1000.000000000000000 ) ;
#26109=DIRECTION ( 'NONE',  ( 0.000000000000000000, 0.000000000000000000, 1.000000000000000000 ) ) ;
#26114=LINE ( 'NONE', #63230, #23782 ) ;
#26116=ORIENTED_EDGE ( 'NONE', *, *, #16029, .F. ) ;
#26126=CARTESIAN_POINT ( 'NONE',  ( 41.09999999999999432, -21.00000000000000000, -13.86939075806900057 ) ) ;
#26129=ORIENTED_EDGE ( 'NONE', *, *, #47724, .F. ) ;
#26145=CARTESIAN_POINT ( 'NONE',  ( 47.00000000000000000, 0.7500000000000000000, -5.000000000000000000 ) ) ;
#26148=DIRECTION ( 'NONE',  ( 0.000000000000000000, 0.000000000000000000, -1.000000000000000000 ) ) ;
#26156=CLOSED_SHELL ( 'NONE', ( #69946, #42046, #3815, #63331, #19969, #25496 ) ) ;
#26157=CARTESIAN_POINT ( 'NONE',  ( 22.90000000000000213, -14.06939075806900874, 20.80000000000001137 ) ) ;
#26169=LINE ( 'NONE', #36781, #65999 ) ;
#26171=ORIENTED_EDGE ( 'NONE', *, *, #51785, .F. ) ;
#26183=DIRECTION ( 'NONE',  ( 0.000000000000000000, 0.000000000000000000, -1.000000000000000000 ) ) ;
#26194=FACE_OUTER_BOUND ( 'NONE', #67149, .T. ) ;
#26196=ORIENTED_EDGE ( 'NONE', *, *, #40160, .F. ) ;
#26197=VECTOR ( 'NONE', #3895, 1000.000000000000000 ) ;
#26206=ORIENTED_EDGE ( 'NONE', *, *, #46201, .T. ) ;
#26214=CARTESIAN_POINT ( 'NONE',  ( 18.89999999999999858, 13.66939075806899240, -20.79999999999999361 ) ) ;
#26215=DIRECTION ( 'NONE',  ( 0.000000000000000000, 0.000000000000000000, -1.000000000000000000 ) ) ;
#26219=CARTESIAN_POINT ( 'NONE',  ( 7.900000000000000355, 21.00000000000000000, -13.98999642601811999 ) ) ;
#26222=DIRECTION ( 'NONE',  ( 0.000000000000000000, 0.000000000000000000, -1.000000000000000000 ) ) ;
#26235=LINE ( 'NONE', #25891, #23493 ) ;
#26240=ORIENTED_EDGE ( 'NONE', *, *, #58609, .T. ) ;
#26245=LINE ( 'NONE', #46747, #48300 ) ;
#26258=EDGE_CURVE ( 'NONE', #22003, #29691, #29224, .T. ) ;
#26260=CIRCLE ( 'NONE', #69158, 5.250000000000000000 ) ;
#26264=ORIENTED_EDGE ( 'NONE', *, *, #8965, .T. ) ;
#26272=ORIENTED_EDGE ( 'NONE', *, *, #43802, .T. ) ;
#26279=VERTEX_POINT ( 'NONE', #33042 ) ;
#26282=VECTOR ( 'NONE', #14731, 1000.000000000000000 ) ;
#26287=FACE_OUTER_BOUND ( 'NONE', #6577, .T. ) ;
#26289=LINE ( 'NONE', #36541, #60568 ) ;
#26295=LINE ( 'NONE', #9690, #37443 ) ;
#26311=( LENGTH_UNIT ( ) NAMED_UNIT ( * ) SI_UNIT ( .MILLI., .METRE. ) );
#26314=FILL_AREA_STYLE ('',( #58845 ) ) ;
#26317=CARTESIAN_POINT ( 'NONE',  ( 40.90000000000000568, -0.1999999999911795112, 8.826273045769999343E-12 ) ) ;
#26335=CARTESIAN_POINT ( 'NONE',  ( 49.00000000000000000, 20.60000000000000142, -13.86939075806900057 ) ) ;
#26338=ORIENTED_EDGE ( 'NONE', *, *, #31964, .F. ) ;
#26342=ORIENTED_EDGE ( 'NONE', *, *, #6872, .F. ) ;
#26349=DIRECTION ( 'NONE',  ( 1.000000000000000000, 0.000000000000000000, 0.000000000000000000 ) ) ;
#26360=ORIENTED_EDGE ( 'NONE', *, *, #64233, .F. ) ;
#26369=LINE ( 'NONE', #37680, #2378 ) ;
#26377=EDGE_CURVE ( 'NONE', #1302, #30390, #52421, .T. ) ;
#26378=DIRECTION ( 'NONE',  ( 0.000000000000000000, 0.000000000000000000, -1.000000000000000000 ) ) ;
#26380=DIRECTION ( 'NONE',  ( -1.000000000000000000, 0.000000000000000000, 0.000000000000000000 ) ) ;
#26394=CARTESIAN_POINT ( 'NONE',  ( 11.90000000000000036, -0.1999999999911795112, 8.826273045769999343E-12 ) ) ;
#26402=FACE_OUTER_BOUND ( 'NONE', #24104, .T. ) ;
#26411=DIRECTION ( 'NONE',  ( 0.000000000000000000, -1.000000000000000000, 0.000000000000000000 ) ) ;
#26417=ORIENTED_EDGE ( 'NONE', *, *, #30336, .F. ) ;
#26420=ORIENTED_EDGE ( 'NONE', *, *, #33719, .T. ) ;
#26423=LINE ( 'NONE', #58253, #58949 ) ;
#26430=FACE_OUTER_BOUND ( 'NONE', #57549, .T. ) ;
#26432=CARTESIAN_POINT ( 'NONE',  ( 39.90000000000000568, -0.2000000000000000111, 0.000000000000000000 ) ) ;
#26452=VERTEX_POINT ( 'NONE', #32925 ) ;
#26456=EDGE_LOOP ( 'NONE', ( #48195, #56555, #7443, #14779 ) ) ;
#26461=CARTESIAN_POINT ( 'NONE',  ( 41.09999999999999432, -0.2000000000000000111, 0.000000000000000000 ) ) ;
#26464=CARTESIAN_POINT ( 'NONE',  ( 10.90000000000000036, -0.2000000000089119934, 8.909539772616881237E-12 ) ) ;
#26480=LINE ( 'NONE', #65007, #50448 ) ;
#26486=FACE_OUTER_BOUND ( 'NONE', #57847, .T. ) ;
#26492=PLANE ( 'NONE',  #19306 ) ;
#26496=CARTESIAN_POINT ( 'NONE',  ( 40.90000000000000568, -16.96999999999999886, -21.00000000000000000 ) ) ;
#26497=CYLINDRICAL_SURFACE ( 'NONE', #11781, 24.99999999998784972 ) ;
#26515=CARTESIAN_POINT ( 'NONE',  ( 3.552713678800500929E-15, -17.79289321881343255, 20.50000000000000355 ) ) ;
#26520=DIRECTION ( 'NONE',  ( 0.000000000000000000, -0.7071067811865474617, -0.7071067811865474617 ) ) ;
#26524=VERTEX_POINT ( 'NONE', #33274 ) ;
#26527=EDGE_CURVE ( 'NONE', #19106, #46180, #54843, .T. ) ;
#26532=ORIENTED_EDGE ( 'NONE', *, *, #35131, .F. ) ;
#26537=EDGE_CURVE ( 'NONE', #53797, #6660, #51486, .T. ) ;
#26547=LINE ( 'NONE', #48118, #32787 ) ;
#26558=AXIS2_PLACEMENT_3D ( 'NONE', #39881, #19034, #68168 ) ;
#26563=LINE ( 'NONE', #48136, #62171 ) ;
#26571=CONICAL_SURFACE ( 'NONE', #6270, 4.000000000000000000, 0.7853981633974476129 ) ;
#26581=ORIENTED_EDGE ( 'NONE', *, *, #51785, .T. ) ;
#26588=DIRECTION ( 'NONE',  ( 0.000000000000000000, 0.000000000000000000, -1.000000000000000000 ) ) ;
#26591=FACE_OUTER_BOUND ( 'NONE', #24542, .T. ) ;
#26599=VECTOR ( 'NONE', #44684, 1000.000000000000000 ) ;
#26603=DIRECTION ( 'NONE',  ( -1.000000000000000000, 0.000000000000000000, 0.000000000000000000 ) ) ;
#26605=DIRECTION ( 'NONE',  ( 0.000000000000000000, 1.000000000000000000, 0.000000000000000000 ) ) ;
#26613=ORIENTED_EDGE ( 'NONE', *, *, #64762, .T. ) ;
#26616=FACE_OUTER_BOUND ( 'NONE', #29593, .T. ) ;
#26642=ORIENTED_EDGE ( 'NONE', *, *, #56804, .T. ) ;
#26646=AXIS2_PLACEMENT_3D ( 'NONE', #62054, #2659, #41551 ) ;
#26648=DIRECTION ( 'NONE',  ( 1.000000000000000000, -0.000000000000000000, 0.000000000000000000 ) ) ;
#26663=( GEOMETRIC_REPRESENTATION_CONTEXT ( 3 ) GLOBAL_UNCERTAINTY_ASSIGNED_CONTEXT ( ( #62790 ) ) GLOBAL_UNIT_ASSIGNED_CONTEXT ( ( #54529, #12396, #55554 ) ) REPRESENTATION_CONTEXT ( 'NONE', 'WORKASPACE' ) );
#26676=EDGE_CURVE ( 'NONE', #30300, #23148, #34156, .T. ) ;
#26679=CARTESIAN_POINT ( 'NONE',  ( 20.90000000000000213, -0.2000000000089119934, -8.913009219568841313E-12 ) ) ;
#26680=PRESENTATION_STYLE_ASSIGNMENT (( #64178 ) ) ;
#26688=DIRECTION ( 'NONE',  ( 0.000000000000000000, 0.000000000000000000, -1.000000000000000000 ) ) ;
#26717=UNCERTAINTY_MEASURE_WITH_UNIT (LENGTH_MEASURE( 1.000000000000000082E-05 ), #40769, 'distance_accuracy_value', 'NONE');
#26725=DIRECTION ( 'NONE',  ( -1.000000000000000000, 0.000000000000000000, 0.000000000000000000 ) ) ;
#26737=DIRECTION ( 'NONE',  ( 0.6785983445458467767, 0.2810846377148228381, 0.6785983445458462215 ) ) ;
#26744=DIRECTION ( 'NONE',  ( 1.000000000000000000, -0.000000000000000000, 0.000000000000000000 ) ) ;
#26753=LINE ( 'NONE', #32411, #2563 ) ;
#26754=EDGE_CURVE ( 'NONE', #17980, #39718, #20358, .T. ) ;
#26760=DIRECTION ( 'NONE',  ( 0.000000000000000000, -1.000000000000000000, 0.000000000000000000 ) ) ;
#26763=CYLINDRICAL_SURFACE ( 'NONE', #50296, 24.99999999998784972 ) ;
#26768=CARTESIAN_POINT ( 'NONE',  ( 49.00000000000000000, -0.1999999999911430404, -8.864436962241481021E-12 ) ) ;
#26771=ORIENTED_EDGE ( 'NONE', *, *, #50260, .F. ) ;
#26794=EDGE_LOOP ( 'NONE', ( #35008, #31059, #6136, #30657 ) ) ;
#26796=DIRECTION ( 'NONE',  ( 0.000000000000000000, 0.000000000000000000, -1.000000000000000000 ) ) ;
#26801=VERTEX_POINT ( 'NONE', #24962 ) ;
#26807=DIRECTION ( 'NONE',  ( -1.000000000000000000, 0.000000000000000000, 0.000000000000000000 ) ) ;
#26817=VECTOR ( 'NONE', #216, 1000.000000000000114 ) ;
#26825=EDGE_CURVE ( 'NONE', #68679, #10522, #36989, .T. ) ;
#26833=DIRECTION ( 'NONE',  ( 0.000000000000000000, 0.000000000000000000, -1.000000000000000000 ) ) ;
#26838=DIRECTION ( 'NONE',  ( 0.000000000000000000, -1.000000000000000000, 0.000000000000000000 ) ) ;
#26855=CIRCLE ( 'NONE', #61805, 24.99999999998789946 ) ;
#26856=VECTOR ( 'NONE', #54304, 1000.000000000000000 ) ;
#26890=ORIENTED_EDGE ( 'NONE', *, *, #12767, .F. ) ;
#26894=ADVANCED_FACE ( 'NONE', ( #69846 ), #6543, .T. ) ;
#26895=CARTESIAN_POINT ( 'NONE',  ( 30.90000000000000213, 0.000000000000000000, 0.000000000000000000 ) ) ;
#26903=FACE_OUTER_BOUND ( 'NONE', #40985, .T. ) ;
#26918=CARTESIAN_POINT ( 'NONE',  ( 40.90000000000000568, 0.000000000000000000, 0.000000000000000000 ) ) ;
#26932=ORIENTED_EDGE ( 'NONE', *, *, #27784, .F. ) ;
#26936=EDGE_CURVE ( 'NONE', #30390, #69031, #24312, .T. ) ;
#26948=CARTESIAN_POINT ( 'NONE',  ( 21.90000000000000213, -21.00000000000001421, -13.86939075806900945 ) ) ;
#26954=ORIENTED_EDGE ( 'NONE', *, *, #32111, .F. ) ;
#26964=ORIENTED_EDGE ( 'NONE', *, *, #20559, .F. ) ;
#26977=ORIENTED_EDGE ( 'NONE', *, *, #30336, .T. ) ;
#26978=VERTEX_POINT ( 'NONE', #18514 ) ;
#26979=EDGE_CURVE ( 'NONE', #29633, #11032, #29829, .T. ) ;
#26985=ORIENTED_EDGE ( 'NONE', *, *, #7903, .T. ) ;
#26990=CARTESIAN_POINT ( 'NONE',  ( 39.90000000000000568, 0.000000000000000000, 5.250000000000000000 ) ) ;
#27014=SURFACE_STYLE_FILL_AREA ( #26314 ) ;
#27017=EDGE_CURVE ( 'NONE', #10522, #27734, #35126, .T. ) ;
#27020=DIRECTION ( 'NONE',  ( -1.000000000000000000, 0.000000000000000000, 0.000000000000000000 ) ) ;
#27027=DIRECTION ( 'NONE',  ( -1.000000000000000000, 0.000000000000000000, 0.000000000000000000 ) ) ;
#27031=DIRECTION ( 'NONE',  ( 0.000000000000000000, 0.000000000000000000, -1.000000000000000000 ) ) ;
#27040=FACE_OUTER_BOUND ( 'NONE', #42121, .T. ) ;
#27046=CIRCLE ( 'NONE', #8960, 2.285366197183106074 ) ;
#27054=ORIENTED_EDGE ( 'NONE', *, *, #62265, .F. ) ;
#27068=ADVANCED_FACE ( 'NONE', ( #7207 ), #24180, .T. ) ;
#27100=LINE ( 'NONE', #31723, #29393 ) ;
#27106=DIRECTION ( 'NONE',  ( 0.000000000000000000, -0.2142857142857146346, -0.9767710236555243730 ) ) ;
#27126=ORIENTED_EDGE ( 'NONE', *, *, #40132, .F. ) ;
#27139=EDGE_CURVE ( 'NONE', #61504, #64531, #57122, .T. ) ;
#27151=AXIS2_PLACEMENT_3D ( 'NONE', #26394, #20732, #63878 ) ;
#27157=EDGE_CURVE ( 'NONE', #10558, #61792, #68729, .T. ) ;
#27177=LINE ( 'NONE', #48737, #44352 ) ;
#27189=CARTESIAN_POINT ( 'NONE',  ( 40.90000000000000568, 0.000000000000000000, 3.447897592003593022E-15 ) ) ;
#27202=EDGE_CURVE ( 'NONE', #7815, #13405, #8958, .T. ) ;
#27228=CARTESIAN_POINT ( 'NONE',  ( 15.89999999999999680, -0.1999999999911795112, 8.826273045769999343E-12 ) ) ;
#27234=LINE ( 'NONE', #43475, #7083 ) ;
#27238=CARTESIAN_POINT ( 'NONE',  ( 39.00000000000000000, -16.96999999999999886, -21.00000000000000000 ) ) ;
#27240=ORIENTED_EDGE ( 'NONE', *, *, #42919, .F. ) ;
#27245=LINE ( 'NONE', #33229, #14285 ) ;
#27247=LINE ( 'NONE', #367, #37632 ) ;
#27249=ADVANCED_FACE ( 'NONE', ( #820 ), #5769, .F. ) ;
#27257=ORIENTED_EDGE ( 'NONE', *, *, #20444, .F. ) ;
#27267=EDGE_CURVE ( 'NONE', #50321, #69402, #10373, .T. ) ;
#27271=VERTEX_POINT ( 'NONE', #59506 ) ;
#27281=AXIS2_PLACEMENT_3D ( 'NONE', #2546, #28724, #6805 ) ;
#27288=DIRECTION ( 'NONE',  ( 0.000000000000000000, 0.000000000000000000, -1.000000000000000000 ) ) ;
#27317=CLOSED_SHELL ( 'NONE', ( #63890, #20155, #15045, #54069, #61868, #9197, #67186, #5025, #20596, #68628 ) ) ;
#27319=LINE ( 'NONE', #42526, #63758 ) ;
#27332=ORIENTED_EDGE ( 'NONE', *, *, #47050, .F. ) ;
#27342=CARTESIAN_POINT ( 'NONE',  ( 19.90000000000000213, -0.1999999999911795112, 8.826273045769999343E-12 ) ) ;
#27344=EDGE_LOOP ( 'NONE', ( #26002, #51727, #63148, #39474 ) ) ;
#27356=PLANE ( 'NONE',  #22195 ) ;
#27358=AXIS2_PLACEMENT_3D ( 'NONE', #7967, #24245, #51112 ) ;
#27363=AXIS2_PLACEMENT_3D ( 'NONE', #16946, #60068, #11616 ) ;
#27370=VERTEX_POINT ( 'NONE', #45645 ) ;
#27373=DIRECTION ( 'NONE',  ( 1.000000000000000000, -0.000000000000000000, 0.000000000000000000 ) ) ;
#27376=CARTESIAN_POINT ( 'NONE',  ( 12.90000000000000213, 13.66939075806899240, 20.79999999999999361 ) ) ;
#27381=DIRECTION ( 'NONE',  ( 1.000000000000000000, -0.000000000000000000, 0.000000000000000000 ) ) ;
#27382=EDGE_LOOP ( 'NONE', ( #40343, #43127, #34930, #13927 ) ) ;
#27390=VERTEX_POINT ( 'NONE', #22712 ) ;
#27398=VERTEX_POINT ( 'NONE', #66868 ) ;
#27419=DIRECTION ( 'NONE',  ( -1.000000000000000000, 0.000000000000000000, 0.000000000000000000 ) ) ;
#27423=CYLINDRICAL_SURFACE ( 'NONE', #45609, 24.99999999998794920 ) ;
#27424=AXIS2_PLACEMENT_3D ( 'NONE', #7817, #50618, #2519 ) ;
#27442=EDGE_CURVE ( 'NONE', #68810, #8098, #23406, .T. ) ;
#27444=EDGE_CURVE ( 'NONE', #10558, #46985, #55657, .T. ) ;
#27452=DIRECTION ( 'NONE',  ( 0.000000000000000000, 0.000000000000000000, -1.000000000000000000 ) ) ;
#27453=LINE ( 'NONE', #23178, #67017 ) ;
#27462=CARTESIAN_POINT ( 'NONE',  ( 40.90000000000000568, 16.96999999999999886, -21.00000000000000000 ) ) ;
#27465=MECHANICAL_DESIGN_GEOMETRIC_PRESENTATION_REPRESENTATION('',(#7153),#6024);
#27471=DIRECTION ( 'NONE',  ( 1.000000000000000000, 0.000000000000000000, 0.000000000000000000 ) ) ;
#27476=PLANE ( 'NONE',  #24482 ) ;
#27485=ORIENTED_EDGE ( 'NONE', *, *, #58156, .F. ) ;
#27504=DIRECTION ( 'NONE',  ( 0.000000000000000000, 0.000000000000000000, -1.000000000000000000 ) ) ;
#27507=ORIENTED_EDGE ( 'NONE', *, *, #16798, .F. ) ;
#27510=( GEOMETRIC_REPRESENTATION_CONTEXT ( 3 ) GLOBAL_UNCERTAINTY_ASSIGNED_CONTEXT ( ( #36617 ) ) GLOBAL_UNIT_ASSIGNED_CONTEXT ( ( #51449, #19272, #40483 ) ) REPRESENTATION_CONTEXT ( 'NONE', 'WORKASPACE' ) );
#27524=FACE_OUTER_BOUND ( 'NONE', #10871, .T. ) ;
#27528=CYLINDRICAL_SURFACE ( 'NONE', #6108, 0.5000000000000000000 ) ;
#27533=DIRECTION ( 'NONE',  ( 0.000000000000000000, 0.000000000000000000, -1.000000000000000000 ) ) ;
#27535=CARTESIAN_POINT ( 'NONE',  ( 41.09999999999999432, -14.06939075806900163, 20.80000000000000426 ) ) ;
#27539=DIRECTION ( 'NONE',  ( 0.000000000000000000, 1.000000000000000000, 0.000000000000000000 ) ) ;
#27547=ORIENTED_EDGE ( 'NONE', *, *, #19327, .T. ) ;
#27556=CARTESIAN_POINT ( 'NONE',  ( 49.00000000000000000, 20.60000000000000142, -13.86939075806900057 ) ) ;
#27561=CARTESIAN_POINT ( 'NONE',  ( 37.90000000000000568, 20.60000000000000142, 13.86939075806899702 ) ) ;
#27573=EDGE_CURVE ( 'NONE', #50027, #67161, #26036, .T. ) ;
#27575=ORIENTED_EDGE ( 'NONE', *, *, #6484, .T. ) ;
#27581=CYLINDRICAL_SURFACE ( 'NONE', #10908, 24.99999999998789946 ) ;
#27585=EDGE_CURVE ( 'NONE', #57888, #40026, #60981, .T. ) ;
#27600=ORIENTED_EDGE ( 'NONE', *, *, #44528, .T. ) ;
#27610=MECHANICAL_DESIGN_GEOMETRIC_PRESENTATION_REPRESENTATION('',(#5057),#61447);
#27612=ORIENTED_EDGE ( 'NONE', *, *, #41288, .F. ) ;
#27613=CARTESIAN_POINT ( 'NONE',  ( 30.90000000000000213, -21.00000000000001421, -13.86939075806900945 ) ) ;
#27616=ADVANCED_FACE ( 'NONE', ( #3585 ), #68639, .F. ) ;
#27617=DIRECTION ( 'NONE',  ( 0.000000000000000000, 0.000000000000000000, 1.000000000000000000 ) ) ;
#27643=VECTOR ( 'NONE', #56580, 1000.000000000000000 ) ;
#27646=LINE ( 'NONE', #49227, #7215 ) ;
#27650=ORIENTED_EDGE ( 'NONE', *, *, #43928, .F. ) ;
#27652=VERTEX_POINT ( 'NONE', #5345 ) ;
#27654=EDGE_CURVE ( 'NONE', #36357, #2916, #26547, .T. ) ;
#27657=DIRECTION ( 'NONE',  ( 0.000000000000000000, 0.000000000000000000, -1.000000000000000000 ) ) ;
#27668=VERTEX_POINT ( 'NONE', #21250 ) ;
#27683=DIRECTION ( 'NONE',  ( 0.000000000000000000, 1.000000000000000000, 0.000000000000000000 ) ) ;
#27692=EDGE_CURVE ( 'NONE', #29909, #41212, #58389, .T. ) ;
#27714=VERTEX_POINT ( 'NONE', #33 ) ;
#27734=VERTEX_POINT ( 'NONE', #5683 ) ;
#27735=EDGE_CURVE ( 'NONE', #49662, #62779, #372, .T. ) ;
#27737=CARTESIAN_POINT ( 'NONE',  ( 7.899999999999999467, 21.00000000000000000, 13.98999642601811999 ) ) ;
#27746=ORIENTED_EDGE ( 'NONE', *, *, #30090, .F. ) ;
#27750=LINE ( 'NONE', #50693, #44050 ) ;
#27755=ADVANCED_FACE ( 'NONE', ( #61472, #50181 ), #23315, .T. ) ;
#27760=CYLINDRICAL_SURFACE ( 'NONE', #48256, 24.99999999998789946 ) ;
#27764=AXIS2_PLACEMENT_3D ( 'NONE', #38763, #49036, #69902 ) ;
#27769=ORIENTED_EDGE ( 'NONE', *, *, #53122, .F. ) ;
#27771=VECTOR ( 'NONE', #2554, 1000.000000000000114 ) ;
#27777=DIRECTION ( 'NONE',  ( 0.000000000000000000, -1.000000000000000000, 0.000000000000000000 ) ) ;
#27784=EDGE_CURVE ( 'NONE', #61917, #43744, #62143, .T. ) ;
#27797=DIRECTION ( 'NONE',  ( 1.000000000000000000, -0.000000000000000000, 0.000000000000000000 ) ) ;
#27812=VECTOR ( 'NONE', #19940, 1000.000000000000114 ) ;
#27824=DIRECTION ( 'NONE',  ( 0.000000000000000000, 0.000000000000000000, -1.000000000000000000 ) ) ;
#27856=CARTESIAN_POINT ( 'NONE',  ( 41.09999999999999432, -14.06939075806901940, -20.80000000000000426 ) ) ;
#27860=CIRCLE ( 'NONE', #38072, 24.99999999998784972 ) ;
#27861=CIRCLE ( 'NONE', #68495, 24.99999999998784972 ) ;
#27866=FACE_OUTER_BOUND ( 'NONE', #45328, .T. ) ;
#27884=DIRECTION ( 'NONE',  ( 1.000000000000000000, 0.000000000000000000, 0.000000000000000000 ) ) ;
#27887=EDGE_CURVE ( 'NONE', #27714, #5641, #49792, .T. ) ;
#27893=VECTOR ( 'NONE', #30472, 1000.000000000000000 ) ;
#27923=AXIS2_PLACEMENT_3D ( 'NONE', #69259, #3861, #20123 ) ;
#27932=FACE_OUTER_BOUND ( 'NONE', #5896, .T. ) ;
#27940=DIRECTION ( 'NONE',  ( -1.000000000000000000, 0.000000000000000000, 0.000000000000000000 ) ) ;
#27945=LINE ( 'NONE', #49513, #1925 ) ;
#27949=CIRCLE ( 'NONE', #34692, 24.99999999998784972 ) ;
#27954=ORIENTED_EDGE ( 'NONE', *, *, #21739, .F. ) ;
#27958=ORIENTED_EDGE ( 'NONE', *, *, #64960, .T. ) ;
#27959=CARTESIAN_POINT ( 'NONE',  ( 48.50000000000000000, 0.7500000000000000000, 3.418698582794335028 ) ) ;
#27964=DIRECTION ( 'NONE',  ( -1.000000000000000000, 0.000000000000000000, 0.000000000000000000 ) ) ;
#27967=PLANE ( 'NONE',  #66210 ) ;
#27968=DIRECTION ( 'NONE',  ( 0.000000000000000000, 0.000000000000000000, -1.000000000000000000 ) ) ;
#27973=DIRECTION ( 'NONE',  ( 0.000000000000000000, -0.5625376724249369076, 0.8267716535433071723 ) ) ;
#27974=ORIENTED_EDGE ( 'NONE', *, *, #57435, .T. ) ;
#27983=LINE ( 'NONE', #23013, #43402 ) ;
#27995=VECTOR ( 'NONE', #21003, 1000.000000000000000 ) ;
#28041=DIRECTION ( 'NONE',  ( 1.000000000000000000, -0.000000000000000000, 0.000000000000000000 ) ) ;
#28043=DIRECTION ( 'NONE',  ( 0.000000000000000000, 0.000000000000000000, -1.000000000000000000 ) ) ;
#28066=CARTESIAN_POINT ( 'NONE',  ( 28.90000000000000213, 13.66939075806899240, 20.79999999999999361 ) ) ;
#28074=CIRCLE ( 'NONE', #50667, 0.5540281690140901327 ) ;
#28081=ORIENTED_EDGE ( 'NONE', *, *, #46969, .F. ) ;
#28082=EDGE_CURVE ( 'NONE', #2943, #11562, #17487, .T. ) ;
#28085=CARTESIAN_POINT ( 'NONE',  ( 8.900000000000005684, -21.00000000000000000, -13.86939075806900057 ) ) ;
#28091=DIRECTION ( 'NONE',  ( 1.000000000000000000, -0.000000000000000000, 0.000000000000000000 ) ) ;
#28129=( NAMED_UNIT ( * ) SI_UNIT ( $, .STERADIAN. ) SOLID_ANGLE_UNIT ( ) );
#28139=DIRECTION ( 'NONE',  ( -1.000000000000000000, 0.000000000000000000, 0.000000000000000000 ) ) ;
#28149=ORIENTED_EDGE ( 'NONE', *, *, #65958, .T. ) ;
#28150=CIRCLE ( 'NONE', #67675, 24.99999999998794920 ) ;
#28157=CARTESIAN_POINT ( 'NONE',  ( 25.57999999999999829, 0.000000000000000000, 2.458500000000000796 ) ) ;
#28174=ORIENTED_EDGE ( 'NONE', *, *, #66967, .T. ) ;
#28175=EDGE_CURVE ( 'NONE', #68454, #31689, #2620, .T. ) ;
#28176=FACE_OUTER_BOUND ( 'NONE', #9026, .T. ) ;
#28177=CARTESIAN_POINT ( 'NONE',  ( 10.00000000000000000, 18.00000000000000355, 21.00000000000000000 ) ) ;
#28190=AXIS2_PLACEMENT_3D ( 'NONE', #15472, #5207, #30673 ) ;
#28194=CARTESIAN_POINT ( 'NONE',  ( 40.90000000000000568, -14.48845687959340012, -21.00000000000000000 ) ) ;
#28203=AXIS2_PLACEMENT_3D ( 'NONE', #26317, #41168, #65119 ) ;
#28222=FACE_OUTER_BOUND ( 'NONE', #82, .T. ) ;
#28228=ORIENTED_EDGE ( 'NONE', *, *, #16602, .T. ) ;
#28239=ORIENTED_EDGE ( 'NONE', *, *, #2901, .T. ) ;
#28251=ORIENTED_EDGE ( 'NONE', *, *, #61148, .T. ) ;
#28260=ORIENTED_EDGE ( 'NONE', *, *, #69723, .F. ) ;
#28265=CARTESIAN_POINT ( 'NONE',  ( 46.39999999999999858, 21.00000000000000000, -2.250000000000000444 ) ) ;
#28274=CIRCLE ( 'NONE', #63269, 25.39999999999999858 ) ;
#28276=SURFACE_SIDE_STYLE ('',( #39567 ) ) ;
#28279=ORIENTED_EDGE ( 'NONE', *, *, #1934, .F. ) ;
#28282=CARTESIAN_POINT ( 'NONE',  ( 39.00000000000000000, 21.00000000000000000, -13.98999642601811999 ) ) ;
#28286=ORIENTED_EDGE ( 'NONE', *, *, #33255, .F. ) ;
#28303=FACE_OUTER_BOUND ( 'NONE', #1739, .T. ) ;
#28324=CIRCLE ( 'NONE', #14812, 24.99999999998794920 ) ;
#28333=EDGE_CURVE ( 'NONE', #33655, #51399, #58895, .T. ) ;
#28342=VECTOR ( 'NONE', #36853, 1000.000000000000000 ) ;
#28348=ORIENTED_EDGE ( 'NONE', *, *, #25082, .T. ) ;
#28352=EDGE_CURVE ( 'NONE', #47619, #51803, #57767, .T. ) ;
#28354=EDGE_CURVE ( 'NONE', #25494, #14048, #68738, .T. ) ;
#28356=EDGE_CURVE ( 'NONE', #5469, #16596, #26295, .T. ) ;
#28357=DIRECTION ( 'NONE',  ( -1.000000000000000000, 0.000000000000000000, 0.000000000000000000 ) ) ;
#28365=DIRECTION ( 'NONE',  ( 0.000000000000000000, -1.000000000000000000, 0.000000000000000000 ) ) ;
#28366=LINE ( 'NONE', #66201, #22163 ) ;
#28384=STYLED_ITEM ( 'NONE', ( #1746 ), #42807 ) ;
#28397=CARTESIAN_POINT ( 'NONE',  ( 41.09999999999999432, -21.00000000000000000, -13.86939075806900057 ) ) ;
#28398=EDGE_LOOP ( 'NONE', ( #21493, #26264, #10112, #47914, #36918, #30773, #27126, #48002 ) ) ;
#28401=DIRECTION ( 'NONE',  ( -1.000000000000000000, 0.000000000000000000, 0.000000000000000000 ) ) ;
#28410=ORIENTED_EDGE ( 'NONE', *, *, #27157, .T. ) ;
#28436=FACE_OUTER_BOUND ( 'NONE', #24028, .T. ) ;
#28437=CARTESIAN_POINT ( 'NONE',  ( 39.90000000000000568, -21.00000000000000000, 13.86939075806900057 ) ) ;
#28442=CARTESIAN_POINT ( 'NONE',  ( 25.57999999999999829, 0.000000000000000000, 0.000000000000000000 ) ) ;
#28472=EDGE_CURVE ( 'NONE', #7472, #17145, #21689, .T. ) ;
#28480=CARTESIAN_POINT ( 'NONE',  ( 25.57999999999999829, 0.000000000000000000, 0.000000000000000000 ) ) ;
#28489=VERTEX_POINT ( 'NONE', #22035 ) ;
#28503=AXIS2_PLACEMENT_3D ( 'NONE', #60375, #5959, #11932 ) ;
#28519=EDGE_LOOP ( 'NONE', ( #69390, #59321, #67559, #2255, #1898, #51568 ) ) ;
#28524=VECTOR ( 'NONE', #56454, 1000.000000000000000 ) ;
#28529=CARTESIAN_POINT ( 'NONE',  ( 49.00000000000000000, -0.2000000000089119934, -8.913009219568841313E-12 ) ) ;
#28534=CARTESIAN_POINT ( 'NONE',  ( 28.90000000000000213, -14.06939075806902117, -20.80000000000000426 ) ) ;
#28563=VECTOR ( 'NONE', #25857, 1000.000000000000000 ) ;
#28569=EDGE_CURVE ( 'NONE', #55707, #41932, #44610, .T. ) ;
#28575=ADVANCED_FACE ( 'NONE', ( #39326 ), #35050, .F. ) ;
#28578=VECTOR ( 'NONE', #6613, 1000.000000000000000 ) ;
#28597=DIRECTION ( 'NONE',  ( 1.000000000000000000, -0.000000000000000000, 0.000000000000000000 ) ) ;
#28598=AXIS2_PLACEMENT_3D ( 'NONE', #48148, #69722, #52776 ) ;
#28601=ORIENTED_EDGE ( 'NONE', *, *, #25759, .F. ) ;
#28606=CIRCLE ( 'NONE', #54631, 25.39999999999999858 ) ;
#28607=CARTESIAN_POINT ( 'NONE',  ( 41.09999999999999432, 13.66939075806899950, 20.80000000000000426 ) ) ;
#28612=AXIS2_PLACEMENT_3D ( 'NONE', #65834, #22705, #5429 ) ;
#28614=ORIENTED_EDGE ( 'NONE', *, *, #19816, .F. ) ;
#28617=DIRECTION ( 'NONE',  ( -1.000000000000000000, 0.000000000000000000, 0.000000000000000000 ) ) ;
#28637=DIRECTION ( 'NONE',  ( 0.000000000000000000, 0.000000000000000000, -1.000000000000000000 ) ) ;
#28659=CIRCLE ( 'NONE', #68192, 24.99999999998784972 ) ;
#28660=FILL_AREA_STYLE_COLOUR ( '', #44497 ) ;
#28671=CARTESIAN_POINT ( 'NONE',  ( 19.90000000000000213, -14.06939075806900874, 20.80000000000001137 ) ) ;
#28672=EDGE_CURVE ( 'NONE', #35542, #868, #4314, .T. ) ;
#28682=ORIENTED_EDGE ( 'NONE', *, *, #26754, .T. ) ;
#28693=DIRECTION ( 'NONE',  ( -1.000000000000000000, 0.000000000000000000, 0.000000000000000000 ) ) ;
#28699=LINE ( 'NONE', #44604, #2394 ) ;
#28700=ADVANCED_FACE ( 'NONE', ( #19493 ), #30460, .F. ) ;
#28706=LINE ( 'NONE', #7483, #713 ) ;
#28709=DIRECTION ( 'NONE',  ( 0.000000000000000000, 0.000000000000000000, 1.000000000000000000 ) ) ;
#28711=CARTESIAN_POINT ( 'NONE',  ( 9.899999999999998579, -21.00000000000000000, 13.86939075806900057 ) ) ;
#28713=DIRECTION ( 'NONE',  ( 0.000000000000000000, 0.8320000000000478124, 0.5547756303226741847 ) ) ;
#28724=DIRECTION ( 'NONE',  ( 0.000000000000000000, 0.000000000000000000, 1.000000000000000000 ) ) ;
#28738=CARTESIAN_POINT ( 'NONE',  ( 49.00000000000000000, -21.00000000000000000, 13.86939075806900057 ) ) ;
#28752=ADVANCED_FACE ( 'NONE', ( #14194 ), #9250, .F. ) ;
#28761=CARTESIAN_POINT ( 'NONE',  ( 28.90000000000000213, 0.000000000000000000, 0.000000000000000000 ) ) ;
#28768=ORIENTED_EDGE ( 'NONE', *, *, #57344, .T. ) ;
#28812=DIRECTION ( 'NONE',  ( 0.000000000000000000, 0.000000000000000000, -1.000000000000000000 ) ) ;
#28813=ORIENTED_EDGE ( 'NONE', *, *, #1657, .F. ) ;
#28818=DIRECTION ( 'NONE',  ( -1.000000000000000000, 0.000000000000000000, 0.000000000000000000 ) ) ;
#28821=PLANE ( 'NONE',  #6987 ) ;
#28823=FACE_OUTER_BOUND ( 'NONE', #1780, .T. ) ;
#28828=VECTOR ( 'NONE', #44135, 1000.000000000000000 ) ;
#28829=ORIENTED_EDGE ( 'NONE', *, *, #60198, .T. ) ;
#28831=FACE_OUTER_BOUND ( 'NONE', #20296, .T. ) ;
#28838=PLANE ( 'NONE',  #65351 ) ;
#28839=DIRECTION ( 'NONE',  ( -1.000000000000000000, 0.000000000000000000, 0.000000000000000000 ) ) ;
#28852=ORIENTED_EDGE ( 'NONE', *, *, #68475, .T. ) ;
#28858=VECTOR ( 'NONE', #10232, 1000.000000000000000 ) ;
#28869=DIRECTION ( 'NONE',  ( 0.000000000000000000, 0.000000000000000000, -1.000000000000000000 ) ) ;
#28883=ORIENTED_EDGE ( 'NONE', *, *, #67756, .T. ) ;
#28890=CARTESIAN_POINT ( 'NONE',  ( 34.89999999999999858, 20.60000000000000142, 13.86939075806900057 ) ) ;
#28895=VECTOR ( 'NONE', #23721, 1000.000000000000000 ) ;
#28900=CARTESIAN_POINT ( 'NONE',  ( 41.09999999999999432, -21.00000000000000000, 13.86939075806900057 ) ) ;
#28915=ORIENTED_EDGE ( 'NONE', *, *, #8154, .F. ) ;
#28921=FACE_OUTER_BOUND ( 'NONE', #52138, .T. ) ;
#28923=ORIENTED_EDGE ( 'NONE', *, *, #32903, .T. ) ;
#28924=ORIENTED_EDGE ( 'NONE', *, *, #37530, .F. ) ;
#28931=FACE_OUTER_BOUND ( 'NONE', #67876, .T. ) ;
#28937=CARTESIAN_POINT ( 'NONE',  ( 49.00000000000000000, -0.2000000000089119934, 8.909539772616881237E-12 ) ) ;
#28952=DIRECTION ( 'NONE',  ( 0.000000000000000000, 0.000000000000000000, -1.000000000000000000 ) ) ;
#28954=VERTEX_POINT ( 'NONE', #18712 ) ;
#28967=LINE ( 'NONE', #7389, #34644 ) ;
#28987=VECTOR ( 'NONE', #25175, 1000.000000000000000 ) ;
#29002=CARTESIAN_POINT ( 'NONE',  ( 41.09999999999999432, -0.2000000000000000111, 0.000000000000000000 ) ) ;
#29010=CIRCLE ( 'NONE', #68551, 0.5000000000000000000 ) ;
#29011=AXIS2_PLACEMENT_3D ( 'NONE', #13743, #35291, #14808 ) ;
#29012=CARTESIAN_POINT ( 'NONE',  ( 26.90000000000000213, -0.2000000000089119934, 8.909539772616881237E-12 ) ) ;
#29022=AXIS2_PLACEMENT_3D ( 'NONE', #5605, #54392, #54050 ) ;
#29035=LINE ( 'NONE', #60519, #20839 ) ;
#29041=DIRECTION ( 'NONE',  ( 1.000000000000000000, 0.000000000000000000, 0.000000000000000000 ) ) ;
#29043=ORIENTED_EDGE ( 'NONE', *, *, #41885, .T. ) ;
#29045=AXIS2_PLACEMENT_3D ( 'NONE', #5181, #26744, #48313 ) ;
#29046=VECTOR ( 'NONE', #19660, 1000.000000000000000 ) ;
#29054=CARTESIAN_POINT ( 'NONE',  ( 49.00000000000000000, -0.2000000000089119934, 8.909539772616881237E-12 ) ) ;
#29059=VECTOR ( 'NONE', #65275, 1000.000000000000000 ) ;
#29070=CARTESIAN_POINT ( 'NONE',  ( 49.00000000000000000, -0.1999999999911795112, 8.826273045769999343E-12 ) ) ;
#29082=VERTEX_POINT ( 'NONE', #4224 ) ;
#29089=ORIENTED_EDGE ( 'NONE', *, *, #68656, .F. ) ;
#29095=DIRECTION ( 'NONE',  ( 0.000000000000000000, 1.000000000000000000, 0.000000000000000000 ) ) ;
#29107=CYLINDRICAL_SURFACE ( 'NONE', #33160, 24.99999999998794920 ) ;
#29111=EDGE_CURVE ( 'NONE', #32973, #7937, #40631, .T. ) ;
#29113=AXIS2_PLACEMENT_3D ( 'NONE', #57469, #29546, #19291 ) ;
#29135=DIRECTION ( 'NONE',  ( 0.000000000000000000, 0.000000000000000000, 1.000000000000000000 ) ) ;
#29143=DIRECTION ( 'NONE',  ( 0.000000000000000000, 0.000000000000000000, 1.000000000000000000 ) ) ;
#29150=CARTESIAN_POINT ( 'NONE',  ( 48.99818419603327868, 0.7500000000000000000, -3.928730293367447501 ) ) ;
#29161=VECTOR ( 'NONE', #55099, 1000.000000000000000 ) ;
#29187=DIRECTION ( 'NONE',  ( 0.000000000000000000, 1.000000000000000000, 0.000000000000000000 ) ) ;
#29194=VECTOR ( 'NONE', #59251, 999.9999999999998863 ) ;
#29195=DIRECTION ( 'NONE',  ( 0.000000000000000000, 0.000000000000000000, 1.000000000000000000 ) ) ;
#29208=VERTEX_POINT ( 'NONE', #30378 ) ;
#29215=EDGE_CURVE ( 'NONE', #868, #16845, #63258, .T. ) ;
#29221=DIRECTION ( 'NONE',  ( 1.000000000000000000, -0.000000000000000000, 0.000000000000000000 ) ) ;
#29224=CIRCLE ( 'NONE', #58594, 5.000000000000000000 ) ;
#29246=DIRECTION ( 'NONE',  ( 0.000000000000000000, 0.000000000000000000, -1.000000000000000000 ) ) ;
#29273=ORIENTED_EDGE ( 'NONE', *, *, #38205, .T. ) ;
#29300=ORIENTED_EDGE ( 'NONE', *, *, #21733, .T. ) ;
#29320=PRESENTATION_STYLE_ASSIGNMENT (( #7758 ) ) ;
#29333=CARTESIAN_POINT ( 'NONE',  ( 19.90000000000000213, -0.000000000000000000, -20.80000000000000426 ) ) ;
#29334=( NAMED_UNIT ( * ) PLANE_ANGLE_UNIT ( ) SI_UNIT ( $, .RADIAN. ) );
#29336=VECTOR ( 'NONE', #4080, 1000.000000000000000 ) ;
#29342=ORIENTED_EDGE ( 'NONE', *, *, #29710, .F. ) ;
#29348=DIRECTION ( 'NONE',  ( 0.000000000000000000, 0.000000000000000000, -1.000000000000000000 ) ) ;
#29349=CARTESIAN_POINT ( 'NONE',  ( 22.90000000000000213, -0.1999999999911430404, -8.864436962241481021E-12 ) ) ;
#29353=CARTESIAN_POINT ( 'NONE',  ( 27.00000000000000000, 0.000000000000000000, 0.000000000000000000 ) ) ;
#29360=LINE ( 'NONE', #65813, #36486 ) ;
#29367=CARTESIAN_POINT ( 'NONE',  ( 7.900000000000000355, 21.00000000000000000, 18.00000000000000355 ) ) ;
#29384=ADVANCED_FACE ( 'NONE', ( #22555 ), #33506, .T. ) ;
#29386=ORIENTED_EDGE ( 'NONE', *, *, #25150, .T. ) ;
#29391=ORIENTED_EDGE ( 'NONE', *, *, #41424, .T. ) ;
#29393=VECTOR ( 'NONE', #37034, 1000.000000000000000 ) ;
#29401=CARTESIAN_POINT ( 'NONE',  ( 23.90000000000000213, -0.000000000000000000, 20.80000000000000426 ) ) ;
#29403=DIRECTION ( 'NONE',  ( 1.000000000000000000, 0.000000000000000000, 0.000000000000000000 ) ) ;
#29404=LINE ( 'NONE', #46028, #38023 ) ;
#29408=CIRCLE ( 'NONE', #7953, 25.39999999999999858 ) ;
#29418=PLANE ( 'NONE',  #36293 ) ;
#29420=VECTOR ( 'NONE', #50342, 1000.000000000000000 ) ;
#29421=DIRECTION ( 'NONE',  ( -1.000000000000000000, 0.000000000000000000, 0.000000000000000000 ) ) ;
#29423=DIRECTION ( 'NONE',  ( -0.000000000000000000, -0.7071067811865474617, 0.7071067811865474617 ) ) ;
#29427=VERTEX_POINT ( 'NONE', #2022 ) ;
#29441=LINE ( 'NONE', #51017, #7998 ) ;
#29444=EDGE_CURVE ( 'NONE', #61792, #46863, #3668, .T. ) ;
#29446=VECTOR ( 'NONE', #54389, 1000.000000000000114 ) ;
#29449=CARTESIAN_POINT ( 'NONE',  ( 11.90000000000000036, 20.60000000000000142, 13.86939075806899702 ) ) ;
#29465=EDGE_CURVE ( 'NONE', #52164, #60151, #25113, .T. ) ;
#29468=AXIS2_PLACEMENT_3D ( 'NONE', #43287, #27381, #65551 ) ;
#29476=ORIENTED_EDGE ( 'NONE', *, *, #5303, .T. ) ;
#29480=LINE ( 'NONE', #34780, #10199 ) ;
#29497=EDGE_CURVE ( 'NONE', #62940, #68694, #16904, .T. ) ;
#29506=EDGE_CURVE ( 'NONE', #6091, #30940, #3765, .T. ) ;
#29515=ORIENTED_EDGE ( 'NONE', *, *, #3386, .F. ) ;
#29519=VECTOR ( 'NONE', #33347, 1000.000000000000114 ) ;
#29533=FACE_OUTER_BOUND ( 'NONE', #50049, .T. ) ;
#29539=VERTEX_POINT ( 'NONE', #8007 ) ;
#29546=DIRECTION ( 'NONE',  ( -1.000000000000000000, 0.000000000000000000, 0.000000000000000000 ) ) ;
#29551=DIRECTION ( 'NONE',  ( 0.000000000000000000, 0.000000000000000000, 1.000000000000000000 ) ) ;
#29552=DIRECTION ( 'NONE',  ( 0.000000000000000000, -1.000000000000000000, 0.000000000000000000 ) ) ;
#29556=ORIENTED_EDGE ( 'NONE', *, *, #60975, .T. ) ;
#29563=ORIENTED_EDGE ( 'NONE', *, *, #5490, .F. ) ;
#29564=AXIS2_PLACEMENT_3D ( 'NONE', #42828, #20914, #59790 ) ;
#29573=EDGE_CURVE ( 'NONE', #12180, #6660, #19665, .T. ) ;
#29576=EDGE_CURVE ( 'NONE', #54885, #34850, #25338, .T. ) ;
#29577=EDGE_CURVE ( 'NONE', #43129, #7082, #2706, .T. ) ;
#29578=CARTESIAN_POINT ( 'NONE',  ( 55.00000000000000000, -16.96999999999999886, 21.00000000000000000 ) ) ;
#29581=ADVANCED_FACE ( 'NONE', ( #45487 ), #14385, .T. ) ;
#29593=EDGE_LOOP ( 'NONE', ( #38963, #69691, #69852, #55058 ) ) ;
#29599=DIRECTION ( 'NONE',  ( 0.000000000000000000, -1.000000000000000000, 0.000000000000000000 ) ) ;
#29603=ORIENTED_EDGE ( 'NONE', *, *, #63437, .F. ) ;
#29629=DIRECTION ( 'NONE',  ( -0.7071067811865475727, 0.000000000000000000, 0.7071067811865475727 ) ) ;
#29633=VERTEX_POINT ( 'NONE', #8727 ) ;
#29641=ADVANCED_FACE ( 'NONE', ( #18621 ), #18980, .F. ) ;
#29649=ORIENTED_EDGE ( 'NONE', *, *, #41935, .T. ) ;
#29653=VERTEX_POINT ( 'NONE', #52932 ) ;
#29657=( NAMED_UNIT ( * ) SI_UNIT ( $, .STERADIAN. ) SOLID_ANGLE_UNIT ( ) );
#29661=VECTOR ( 'NONE', #3008, 1000.000000000000000 ) ;
#29680=EDGE_LOOP ( 'NONE', ( #23981, #48712, #3023, #3954 ) ) ;
#29681=CARTESIAN_POINT ( 'NONE',  ( 49.00000000000000000, -0.7500000000000000000, 4.943429983321300014 ) ) ;
#29689=DIRECTION ( 'NONE',  ( -1.000000000000000000, 0.000000000000000000, 0.000000000000000000 ) ) ;
#29691=VERTEX_POINT ( 'NONE', #15777 ) ;
#29693=VERTEX_POINT ( 'NONE', #53276 ) ;
#29696=AXIS2_PLACEMENT_3D ( 'NONE', #67828, #62498, #46594 ) ;
#29702=ORIENTED_EDGE ( 'NONE', *, *, #19313, .F. ) ;
#29710=EDGE_CURVE ( 'NONE', #46512, #31832, #33040, .T. ) ;
#29712=ORIENTED_EDGE ( 'NONE', *, *, #63293, .F. ) ;
#29723=EDGE_LOOP ( 'NONE', ( #59577, #34339, #52443, #12194 ) ) ;
#29729=CARTESIAN_POINT ( 'NONE',  ( 31.89999999999999858, 13.66939075806899240, -20.79999999999999361 ) ) ;
#29747=DIRECTION ( 'NONE',  ( -1.000000000000000000, 0.000000000000000000, 0.000000000000000000 ) ) ;
#29749=CARTESIAN_POINT ( 'NONE',  ( 0.000000000000000000, 20.50000000000000000, 17.79289321881345032 ) ) ;
#29753=DIRECTION ( 'NONE',  ( 0.000000000000000000, 0.000000000000000000, -1.000000000000000000 ) ) ;
#29754=ORIENTED_EDGE ( 'NONE', *, *, #42258, .F. ) ;
#29757=CARTESIAN_POINT ( 'NONE',  ( 26.90000000000000213, -0.1999999999911430404, -8.864436962241481021E-12 ) ) ;
#29764=EDGE_CURVE ( 'NONE', #54988, #19639, #20726, .T. ) ;
#29766=CARTESIAN_POINT ( 'NONE',  ( 2.664535259100375697E-15, 20.50000000000000355, 17.79289321881343611 ) ) ;
#29773=FACE_OUTER_BOUND ( 'NONE', #16287, .T. ) ;
#29774=VECTOR ( 'NONE', #16024, 1000.000000000000000 ) ;
#29786=CARTESIAN_POINT ( 'NONE',  ( 25.57999999999999829, 0.000000000000000000, 0.000000000000000000 ) ) ;
#29796=EDGE_CURVE ( 'NONE', #245, #26524, #22128, .T. ) ;
#29798=CARTESIAN_POINT ( 'NONE',  ( 8.900000000000005684, 21.00000000000000000, 13.98999642601811999 ) ) ;
#29800=CARTESIAN_POINT ( 'NONE',  ( 16.89999999999999858, -0.2000000000089119934, 8.909539772616881237E-12 ) ) ;
#29801=LINE ( 'NONE', #8932, #62410 ) ;
#29806=CIRCLE ( 'NONE', #65935, 0.5000000000000000000 ) ;
#29822=AXIS2_PLACEMENT_3D ( 'NONE', #52047, #62637, #24820 ) ;
#29826=VERTEX_POINT ( 'NONE', #22814 ) ;
#29829=LINE ( 'NONE', #55659, #26599 ) ;
#29859=ADVANCED_FACE ( 'NONE', ( #50376 ), #6210, .F. ) ;
#29860=DIRECTION ( 'NONE',  ( 0.000000000000000000, 0.000000000000000000, 1.000000000000000000 ) ) ;
#29862=VECTOR ( 'NONE', #33979, 1000.000000000000000 ) ;
#29867=LINE ( 'NONE', #46132, #7548 ) ;
#29868=DIRECTION ( 'NONE',  ( -1.000000000000000000, 0.000000000000000000, 0.000000000000000000 ) ) ;
#29882=STYLED_ITEM ( 'NONE', ( #47346 ), #43959 ) ;
#29884=DIRECTION ( 'NONE',  ( -1.000000000000000000, 0.000000000000000000, 0.000000000000000000 ) ) ;
#29888=ORIENTED_EDGE ( 'NONE', *, *, #38200, .T. ) ;
#29892=ADVANCED_FACE ( 'NONE', ( #49355 ), #38723, .T. ) ;
#29902=CARTESIAN_POINT ( 'NONE',  ( 49.00000000000000000, -0.1999999999911795112, 8.826273045769999343E-12 ) ) ;
#29907=CARTESIAN_POINT ( 'NONE',  ( 41.09999999999999432, -21.00000000000000000, 13.86939075806900057 ) ) ;
#29909=VERTEX_POINT ( 'NONE', #69005 ) ;
#29912=AXIS2_PLACEMENT_3D ( 'NONE', #62163, #57917, #13729 ) ;
#29923=AXIS2_PLACEMENT_3D ( 'NONE', #9796, #46900, #14740 ) ;
#29925=DIRECTION ( 'NONE',  ( 1.000000000000000000, -0.000000000000000000, 0.000000000000000000 ) ) ;
#29926=FILL_AREA_STYLE ('',( #14726 ) ) ;
#29927=ORIENTED_EDGE ( 'NONE', *, *, #34944, .F. ) ;
#29933=EDGE_CURVE ( 'NONE', #18545, #33868, #41776, .T. ) ;
#29942=LINE ( 'NONE', #56809, #31152 ) ;
#29958=VERTEX_POINT ( 'NONE', #24563 ) ;
#29976=ORIENTED_EDGE ( 'NONE', *, *, #63006, .F. ) ;
#29987=FACE_OUTER_BOUND ( 'NONE', #31627, .T. ) ;
#29992=ORIENTED_EDGE ( 'NONE', *, *, #56224, .T. ) ;
#30011=AXIS2_PLACEMENT_3D ( 'NONE', #30833, #2298, #15277 ) ;
#30013=LINE ( 'NONE', #51594, #35815 ) ;
#30017=CYLINDRICAL_SURFACE ( 'NONE', #55764, 5.000000000000000000 ) ;
#30021=MECHANICAL_DESIGN_GEOMETRIC_PRESENTATION_REPRESENTATION('',(#69562),#26663);
#30031=CARTESIAN_POINT ( 'NONE',  ( 19.90000000000000213, -0.000000000000000000, 20.80000000000000426 ) ) ;
#30035=DIRECTION ( 'NONE',  ( -1.000000000000000000, 0.000000000000000000, -0.000000000000000000 ) ) ;
#30042=FACE_OUTER_BOUND ( 'NONE', #46525, .T. ) ;
#30051=DIRECTION ( 'NONE',  ( 0.000000000000000000, 1.000000000000000000, -0.000000000000000000 ) ) ;
#30061=ORIENTED_EDGE ( 'NONE', *, *, #54021, .F. ) ;
#30068=DIRECTION ( 'NONE',  ( 0.000000000000000000, -0.7071067811865474617, 0.7071067811865474617 ) ) ;
#30069=CARTESIAN_POINT ( 'NONE',  ( 15.89999999999999680, 20.60000000000000142, -13.86939075806900057 ) ) ;
#30070=FACE_OUTER_BOUND ( 'NONE', #11991, .T. ) ;
#30071=EDGE_LOOP ( 'NONE', ( #7259, #51848, #40675, #33262 ) ) ;
#30073=VECTOR ( 'NONE', #42902, 1000.000000000000000 ) ;
#30082=EDGE_LOOP ( 'NONE', ( #31841, #41213, #28829, #62424 ) ) ;
#30086=VECTOR ( 'NONE', #23134, 1000.000000000000000 ) ;
#30090=EDGE_CURVE ( 'NONE', #31863, #67236, #65829, .T. ) ;
#30101=AXIS2_PLACEMENT_3D ( 'NONE', #48490, #54147, #21622 ) ;
#30114=LINE ( 'NONE', #51330, #12274 ) ;
#30115=EDGE_CURVE ( 'NONE', #62940, #45716, #35638, .T. ) ;
#30116=DIRECTION ( 'NONE',  ( -1.000000000000000000, 0.000000000000000000, 0.000000000000000000 ) ) ;
#30140=ORIENTED_EDGE ( 'NONE', *, *, #51678, .T. ) ;
#30149=ORIENTED_EDGE ( 'NONE', *, *, #58315, .F. ) ;
#30156=CARTESIAN_POINT ( 'NONE',  ( 28.90000000000000213, -21.00000000000000000, 13.86939075806900057 ) ) ;
#30157=EDGE_CURVE ( 'NONE', #22414, #16920, #46257, .T. ) ;
#30164=ORIENTED_EDGE ( 'NONE', *, *, #20688, .F. ) ;
#30183=CARTESIAN_POINT ( 'NONE',  ( 29.89999999999999858, 20.60000000000000142, 13.86939075806899702 ) ) ;
#30201=EDGE_CURVE ( 'NONE', #13751, #64704, #20785, .T. ) ;
#30204=EDGE_CURVE ( 'NONE', #4613, #18545, #4539, .T. ) ;
#30210=DIRECTION ( 'NONE',  ( 0.000000000000000000, 0.000000000000000000, -1.000000000000000000 ) ) ;
#30222=VECTOR ( 'NONE', #34867, 1000.000000000000000 ) ;
#30225=LINE ( 'NONE', #8647, #20958 ) ;
#30231=DIRECTION ( 'NONE',  ( -1.000000000000000000, 0.000000000000000000, 0.000000000000000000 ) ) ;
#30240=CARTESIAN_POINT ( 'NONE',  ( 38.90000000000000568, 20.60000000000000142, 13.86939075806900057 ) ) ;
#30242=SURFACE_STYLE_USAGE ( .BOTH. , #13960 ) ;
#30247=AXIS2_PLACEMENT_3D ( 'NONE', #66380, #50463, #33838 ) ;
#30253=ORIENTED_EDGE ( 'NONE', *, *, #49121, .T. ) ;
#30255=ORIENTED_EDGE ( 'NONE', *, *, #61191, .F. ) ;
#30267=DIRECTION ( 'NONE',  ( 0.000000000000000000, 0.000000000000000000, 1.000000000000000000 ) ) ;
#30272=ORIENTED_EDGE ( 'NONE', *, *, #4980, .T. ) ;
#30285=EDGE_CURVE ( 'NONE', #15679, #3626, #63225, .T. ) ;
#30300=VERTEX_POINT ( 'NONE', #63936 ) ;
#30307=DIRECTION ( 'NONE',  ( 0.000000000000000000, 0.000000000000000000, -1.000000000000000000 ) ) ;
#30310=VERTEX_POINT ( 'NONE', #46601 ) ;
#30328=VERTEX_POINT ( 'NONE', #11219 ) ;
#30336=EDGE_CURVE ( 'NONE', #42085, #16791, #65664, .T. ) ;
#30338=CARTESIAN_POINT ( 'NONE',  ( 39.90000000000000568, -16.96999999999999886, 21.00000000000000000 ) ) ;
#30341=EDGE_CURVE ( 'NONE', #39384, #4186, #46655, .T. ) ;
#30344=CYLINDRICAL_SURFACE ( 'NONE', #26558, 24.99999999998794920 ) ;
#30346=DIRECTION ( 'NONE',  ( 0.000000000000000000, 0.000000000000000000, -1.000000000000000000 ) ) ;
#30348=EDGE_CURVE ( 'NONE', #32705, #60377, #6266, .T. ) ;
#30368=ORIENTED_EDGE ( 'NONE', *, *, #8965, .F. ) ;
#30372=SURFACE_SIDE_STYLE ('',( #46276 ) ) ;
#30378=CARTESIAN_POINT ( 'NONE',  ( 9.899999999999998579, -14.06939075806902117, -20.80000000000000426 ) ) ;
#30386=CARTESIAN_POINT ( 'NONE',  ( 22.90000000000000213, 20.60000000000000142, -13.86939075806900057 ) ) ;
#30390=VERTEX_POINT ( 'NONE', #64978 ) ;
#30397=ORIENTED_EDGE ( 'NONE', *, *, #18313, .T. ) ;
#30399=DIRECTION ( 'NONE',  ( 0.000000000000000000, 0.000000000000000000, 1.000000000000000000 ) ) ;
#30403=LINE ( 'NONE', #51969, #23041 ) ;
#30404=LINE ( 'NONE', #41351, #58716 ) ;
#30408=ORIENTED_EDGE ( 'NONE', *, *, #36587, .T. ) ;
#30415=EDGE_LOOP ( 'NONE', ( #15830, #46890, #5918, #53248 ) ) ;
#30426=DIRECTION ( 'NONE',  ( 1.000000000000000000, -0.000000000000000000, 0.000000000000000000 ) ) ;
#30438=ADVANCED_FACE ( 'NONE', ( #270 ), #59315, .F. ) ;
#30457=VERTEX_POINT ( 'NONE', #55068 ) ;
#30460=PLANE ( 'NONE',  #8081 ) ;
#30463=LINE ( 'NONE', #3598, #18109 ) ;
#30472=DIRECTION ( 'NONE',  ( 0.000000000000000000, 0.000000000000000000, -1.000000000000000000 ) ) ;
#30473=ADVANCED_FACE ( 'NONE', ( #38819 ), #38155, .T. ) ;
#30480=ORIENTED_EDGE ( 'NONE', *, *, #36542, .T. ) ;
#30490=CIRCLE ( 'NONE', #21460, 25.39999999999999858 ) ;
#30499=DIRECTION ( 'NONE',  ( 0.000000000000000000, 0.000000000000000000, -1.000000000000000000 ) ) ;
#30500=ORIENTED_EDGE ( 'NONE', *, *, #66902, .T. ) ;
#30502=DIRECTION ( 'NONE',  ( 0.000000000000000000, 0.000000000000000000, -1.000000000000000000 ) ) ;
#30508=DIRECTION ( 'NONE',  ( 0.000000000000000000, 0.000000000000000000, -1.000000000000000000 ) ) ;
#30511=VERTEX_POINT ( 'NONE', #11590 ) ;
#30513=AXIS2_PLACEMENT_3D ( 'NONE', #46022, #19844, #18795 ) ;
#30546=ORIENTED_EDGE ( 'NONE', *, *, #31604, .T. ) ;
#30552=CARTESIAN_POINT ( 'NONE',  ( 39.00000000000000000, 0.000000000000000000, 0.000000000000000000 ) ) ;
#30553=PLANE ( 'NONE',  #67736 ) ;
#30563=ORIENTED_EDGE ( 'NONE', *, *, #47321, .T. ) ;
#30564=CARTESIAN_POINT ( 'NONE',  ( 49.00000000000000000, 13.66939075806899950, 20.80000000000000426 ) ) ;
#30580=DIRECTION ( 'NONE',  ( 0.000000000000000000, 0.000000000000000000, 1.000000000000000000 ) ) ;
#30589=CIRCLE ( 'NONE', #29468, 24.99999999998784972 ) ;
#30601=FACE_OUTER_BOUND ( 'NONE', #66392, .T. ) ;
#30617=VECTOR ( 'NONE', #39658, 1000.000000000000000 ) ;
#30621=DIRECTION ( 'NONE',  ( 1.000000000000000000, -0.000000000000000000, 0.000000000000000000 ) ) ;
#30623=PLANE ( 'NONE',  #32881 ) ;
#30633=AXIS2_PLACEMENT_3D ( 'NONE', #63383, #19891, #41098 ) ;
#30635=CARTESIAN_POINT ( 'NONE',  ( 41.09999999999999432, 21.00000000000000000, -13.98999642601811999 ) ) ;
#30644=DIRECTION ( 'NONE',  ( 0.000000000000000000, 0.000000000000000000, -1.000000000000000000 ) ) ;
#30656=CARTESIAN_POINT ( 'NONE',  ( 38.90000000000000568, -21.00000000000000000, 13.86939075806900057 ) ) ;
#30657=ORIENTED_EDGE ( 'NONE', *, *, #45707, .F. ) ;
#30666=EDGE_CURVE ( 'NONE', #32098, #868, #39505, .T. ) ;
#30667=PLANE ( 'NONE',  #15848 ) ;
#30668=VECTOR ( 'NONE', #47079, 1000.000000000000000 ) ;
#30673=DIRECTION ( 'NONE',  ( 0.000000000000000000, 0.000000000000000000, 1.000000000000000000 ) ) ;
#30675=EDGE_CURVE ( 'NONE', #35475, #32206, #17176, .T. ) ;
#30691=ADVANCED_FACE ( 'NONE', ( #8371 ), #13337, .T. ) ;
#30696=CARTESIAN_POINT ( 'NONE',  ( 39.00000000000000000, 0.000000000000000000, 5.000000000000000000 ) ) ;
#30702=ORIENTED_EDGE ( 'NONE', *, *, #2025, .F. ) ;
#30715=CARTESIAN_POINT ( 'NONE',  ( 41.09999999999999432, 20.60000000000000142, -13.86939075806900057 ) ) ;
#30724=CARTESIAN_POINT ( 'NONE',  ( 7.900000000000000355, -18.00000000000000355, -21.00000000000000000 ) ) ;
#30734=VERTEX_POINT ( 'NONE', #45865 ) ;
#30750=CARTESIAN_POINT ( 'NONE',  ( 39.90000000000000568, 20.60000000000000142, -13.86939075806900057 ) ) ;
#30753=LINE ( 'NONE', #36764, #51490 ) ;
#30773=ORIENTED_EDGE ( 'NONE', *, *, #64991, .T. ) ;
#30778=FACE_OUTER_BOUND ( 'NONE', #52272, .T. ) ;
#30779=ORIENTED_EDGE ( 'NONE', *, *, #39865, .T. ) ;
#30784=DIRECTION ( 'NONE',  ( 0.000000000000000000, 0.000000000000000000, -1.000000000000000000 ) ) ;
#30799=VERTEX_POINT ( 'NONE', #46905 ) ;
#30802=CARTESIAN_POINT ( 'NONE',  ( 10.00000000000000000, -18.00000000000000355, 21.00000000000000000 ) ) ;
#30803=ORIENTED_EDGE ( 'NONE', *, *, #37308, .F. ) ;
#30804=LINE ( 'NONE', #36099, #52700 ) ;
#30806=DIRECTION ( 'NONE',  ( 0.000000000000000000, 0.000000000000000000, -1.000000000000000000 ) ) ;
#30815=DIRECTION ( 'NONE',  ( 0.000000000000000000, 0.7071067811865474617, 0.7071067811865474617 ) ) ;
#30818=CARTESIAN_POINT ( 'NONE',  ( 39.00000000000000000, -14.48845687959340012, -21.00000000000000000 ) ) ;
#30833=CARTESIAN_POINT ( 'NONE',  ( 49.00000000000000000, -14.06939075806900163, -20.80000000000000426 ) ) ;
#30836=ADVANCED_FACE ( 'NONE', ( #19678 ), #9438, .F. ) ;
#30849=AXIS2_PLACEMENT_3D ( 'NONE', #24366, #63607, #24717 ) ;
#30868=ORIENTED_EDGE ( 'NONE', *, *, #27202, .F. ) ;
#30870=VECTOR ( 'NONE', #26807, 1000.000000000000000 ) ;
#30884=EDGE_CURVE ( 'NONE', #2028, #50683, #49976, .T. ) ;
#30888=CARTESIAN_POINT ( 'NONE',  ( 49.00000000000000000, -0.7500000000000000000, -3.929058411375429216 ) ) ;
#30889=VERTEX_POINT ( 'NONE', #30656 ) ;
#30891=VECTOR ( 'NONE', #31888, 1000.000000000000000 ) ;
#30940=VERTEX_POINT ( 'NONE', #21793 ) ;
#30953=DIRECTION ( 'NONE',  ( 0.000000000000000000, 0.000000000000000000, 1.000000000000000000 ) ) ;
#30955=CARTESIAN_POINT ( 'NONE',  ( 49.00000000000000000, -21.00000000000000000, 13.86939075806900057 ) ) ;
#30956=DIRECTION ( 'NONE',  ( 0.000000000000000000, 0.000000000000000000, 1.000000000000000000 ) ) ;
#30968=UNCERTAINTY_MEASURE_WITH_UNIT (LENGTH_MEASURE( 1.000000000000000082E-05 ), #9341, 'distance_accuracy_value', 'NONE');
#30981=LINE ( 'NONE', #4124, #63138 ) ;
#30984=CARTESIAN_POINT ( 'NONE',  ( 41.09999999999999432, 13.66939075806899950, 20.80000000000000426 ) ) ;
#30988=LINE ( 'NONE', #20725, #26817 ) ;
#30993=ADVANCED_FACE ( 'NONE', ( #575 ), #22145, .F. ) ;
#30996=ORIENTED_EDGE ( 'NONE', *, *, #51267, .T. ) ;
#31003=CARTESIAN_POINT ( 'NONE',  ( 28.90000000000000213, 0.000000000000000000, 2.154935995002245293E-15 ) ) ;
#31006=DIRECTION ( 'NONE',  ( 0.000000000000000000, 0.000000000000000000, 1.000000000000000000 ) ) ;
#31019=VERTEX_POINT ( 'NONE', #49702 ) ;
#31025=CARTESIAN_POINT ( 'NONE',  ( 14.89999999999999680, -0.2000000000089119934, -8.913009219568841313E-12 ) ) ;
#31026=ADVANCED_FACE ( 'NONE', ( #60299 ), #43005, .F. ) ;
#31032=DIRECTION ( 'NONE',  ( -1.000000000000000000, 0.000000000000000000, 0.000000000000000000 ) ) ;
#31044=CARTESIAN_POINT ( 'NONE',  ( 18.89999999999999858, 20.60000000000000142, -13.86939075806900057 ) ) ;
#31052=DIRECTION ( 'NONE',  ( 0.000000000000000000, 0.000000000000000000, 1.000000000000000000 ) ) ;
#31053=CARTESIAN_POINT ( 'NONE',  ( 10.00000000000000000, 21.00000000000000000, -18.00000000000000355 ) ) ;
#31059=ORIENTED_EDGE ( 'NONE', *, *, #24624, .F. ) ;
#31082=EDGE_CURVE ( 'NONE', #67161, #27668, #67360, .T. ) ;
#31085=EDGE_CURVE ( 'NONE', #34215, #43571, #56047, .T. ) ;
#31094=SURFACE_SIDE_STYLE ('',( #57952 ) ) ;
#31100=CARTESIAN_POINT ( 'NONE',  ( 25.90000000000000213, -0.000000000000000000, 20.80000000000000426 ) ) ;
#31102=EDGE_CURVE ( 'NONE', #60595, #49899, #8292, .T. ) ;
#31103=FACE_OUTER_BOUND ( 'NONE', #57257, .T. ) ;
#31104=EDGE_CURVE ( 'NONE', #20722, #60486, #21734, .T. ) ;
#31112=( LENGTH_UNIT ( ) NAMED_UNIT ( * ) SI_UNIT ( .MILLI., .METRE. ) );
#31116=ADVANCED_FACE ( 'NONE', ( #45077 ), #34116, .F. ) ;
#31121=VERTEX_POINT ( 'NONE', #66652 ) ;
#31138=VECTOR ( 'NONE', #58988, 1000.000000000000114 ) ;
#31152=VECTOR ( 'NONE', #12966, 1000.000000000000000 ) ;
#31167=AXIS2_PLACEMENT_3D ( 'NONE', #60340, #39470, #5925 ) ;
#31178=CARTESIAN_POINT ( 'NONE',  ( 32.89999999999999858, 13.66939075806899950, 20.80000000000000426 ) ) ;
#31179=DIRECTION ( 'NONE',  ( 1.000000000000000000, 0.000000000000000000, 0.000000000000000000 ) ) ;
#31184=PLANE ( 'NONE',  #64276 ) ;
#31191=CARTESIAN_POINT ( 'NONE',  ( 8.900000000000005684, -21.00000000000000000, 13.86939075806900057 ) ) ;
#31192=VECTOR ( 'NONE', #45761, 1000.000000000000000 ) ;
#31225=ORIENTED_EDGE ( 'NONE', *, *, #63293, .T. ) ;
#31234=ORIENTED_EDGE ( 'NONE', *, *, #56035, .F. ) ;
#31240=DIRECTION ( 'NONE',  ( 1.000000000000000000, -0.000000000000000000, 0.000000000000000000 ) ) ;
#31241=VERTEX_POINT ( 'NONE', #24921 ) ;
#31256=AXIS2_PLACEMENT_3D ( 'NONE', #58021, #47410, #35748 ) ;
#31270=VERTEX_POINT ( 'NONE', #31299 ) ;
#31282=DIRECTION ( 'NONE',  ( 1.000000000000000000, -0.000000000000000000, 0.000000000000000000 ) ) ;
#31283=CARTESIAN_POINT ( 'NONE',  ( 18.89999999999999858, 20.60000000000000142, 13.86939075806900057 ) ) ;
#31299=CARTESIAN_POINT ( 'NONE',  ( 0.5000000000000000000, 18.00000000000000355, -21.00000000000000000 ) ) ;
#31305=EDGE_CURVE ( 'NONE', #9808, #4698, #42929, .T. ) ;
#31312=ORIENTED_EDGE ( 'NONE', *, *, #42486, .T. ) ;
#31325=ORIENTED_EDGE ( 'NONE', *, *, #51264, .T. ) ;
#31328=LINE ( 'NONE', #10092, #23049 ) ;
#31329=DIRECTION ( 'NONE',  ( 0.000000000000000000, 0.000000000000000000, -1.000000000000000000 ) ) ;
#31330=FACE_OUTER_BOUND ( 'NONE', #22504, .T. ) ;
#31333=ORIENTED_EDGE ( 'NONE', *, *, #12303, .F. ) ;
#31345=DIRECTION ( 'NONE',  ( 0.000000000000000000, -0.7071067811865474617, -0.7071067811865474617 ) ) ;
#31358=AXIS2_PLACEMENT_3D ( 'NONE', #42550, #11743, #33666 ) ;
#31367=CIRCLE ( 'NONE', #61823, 2.458500000000000796 ) ;
#31381=DIRECTION ( 'NONE',  ( 0.000000000000000000, 0.000000000000000000, -1.000000000000000000 ) ) ;
#31392=CYLINDRICAL_SURFACE ( 'NONE', #28190, 24.99999999998784972 ) ;
#31393=DIRECTION ( 'NONE',  ( 0.000000000000000000, 0.000000000000000000, -1.000000000000000000 ) ) ;
#31403=ORIENTED_EDGE ( 'NONE', *, *, #34026, .F. ) ;
#31404=AXIS2_PLACEMENT_3D ( 'NONE', #3898, #3547, #9910 ) ;
#31413=DIRECTION ( 'NONE',  ( -1.000000000000000000, 0.000000000000000000, 0.000000000000000000 ) ) ;
#31414=EDGE_LOOP ( 'NONE', ( #5076, #41713, #16630, #15170 ) ) ;
#31424=CARTESIAN_POINT ( 'NONE',  ( 11.90000000000000036, 13.66939075806899240, 20.79999999999999361 ) ) ;
#31425=DIRECTION ( 'NONE',  ( 0.000000000000000000, 0.000000000000000000, -1.000000000000000000 ) ) ;
#31436=EDGE_CURVE ( 'NONE', #24121, #13405, #38671, .T. ) ;
#31439=EDGE_CURVE ( 'NONE', #58411, #51947, #2586, .T. ) ;
#31449=DIRECTION ( 'NONE',  ( 0.000000000000000000, 0.000000000000000000, -1.000000000000000000 ) ) ;
#31467=DIRECTION ( 'NONE',  ( 0.000000000000000000, 0.000000000000000000, 1.000000000000000000 ) ) ;
#31468=VERTEX_POINT ( 'NONE', #2920 ) ;
#31471=DIRECTION ( 'NONE',  ( 1.000000000000000000, -0.000000000000000000, 0.000000000000000000 ) ) ;
#31488=CARTESIAN_POINT ( 'NONE',  ( 49.00000000000000000, -0.2000000000089119934, -8.913009219568841313E-12 ) ) ;
#31500=ORIENTED_EDGE ( 'NONE', *, *, #50125, .T. ) ;
#31511=EDGE_LOOP ( 'NONE', ( #65520, #66138, #15295, #41501, #68986, #33333, #67648, #65482 ) ) ;
#31540=FACE_OUTER_BOUND ( 'NONE', #66905, .T. ) ;
#31544=ORIENTED_EDGE ( 'NONE', *, *, #35517, .F. ) ;
#31547=DIRECTION ( 'NONE',  ( 0.000000000000000000, 0.000000000000000000, -1.000000000000000000 ) ) ;
#31552=ORIENTED_EDGE ( 'NONE', *, *, #38511, .F. ) ;
#31565=ORIENTED_EDGE ( 'NONE', *, *, #60854, .T. ) ;
#31568=ORIENTED_EDGE ( 'NONE', *, *, #34026, .T. ) ;
#31575=VECTOR ( 'NONE', #9127, 1000.000000000000000 ) ;
#31576=DIRECTION ( 'NONE',  ( 1.000000000000000000, -0.000000000000000000, 0.000000000000000000 ) ) ;
#31594=DIRECTION ( 'NONE',  ( 0.000000000000000000, 0.000000000000000000, -1.000000000000000000 ) ) ;
#31604=EDGE_CURVE ( 'NONE', #68514, #16845, #52062, .T. ) ;
#31611=CARTESIAN_POINT ( 'NONE',  ( 11.90000000000000036, 13.66939075806899240, -20.79999999999999361 ) ) ;
#31615=CIRCLE ( 'NONE', #14638, 5.250000000000000000 ) ;
#31617=ORIENTED_EDGE ( 'NONE', *, *, #57568, .T. ) ;
#31622=SURFACE_STYLE_USAGE ( .BOTH. , #20295 ) ;
#31627=EDGE_LOOP ( 'NONE', ( #19224, #450, #46936, #1828 ) ) ;
#31629=PRESENTATION_STYLE_ASSIGNMENT (( #69804 ) ) ;
#31651=CARTESIAN_POINT ( 'NONE',  ( 39.90000000000000568, -21.00000000000000000, 13.86939075806900057 ) ) ;
#31660=LINE ( 'NONE', #64872, #37816 ) ;
#31666=VECTOR ( 'NONE', #66953, 1000.000000000000000 ) ;
#31670=DIRECTION ( 'NONE',  ( 0.000000000000000000, 0.000000000000000000, 1.000000000000000000 ) ) ;
#31681=UNCERTAINTY_MEASURE_WITH_UNIT (LENGTH_MEASURE( 1.000000000000000082E-05 ), #38648, 'distance_accuracy_value', 'NONE');
#31683=ORIENTED_EDGE ( 'NONE', *, *, #29933, .T. ) ;
#31689=VERTEX_POINT ( 'NONE', #15983 ) ;
#31693=AXIS2_PLACEMENT_3D ( 'NONE', #36461, #53789, #47768 ) ;
#31699=LINE ( 'NONE', #38384, #44892 ) ;
#31700=SURFACE_STYLE_FILL_AREA ( #37010 ) ;
#31703=VECTOR ( 'NONE', #3613, 1000.000000000000000 ) ;
#31713=CARTESIAN_POINT ( 'NONE',  ( 39.90000000000000568, 4.286263797015736595E-16, -3.500000000000000000 ) ) ;
#31717=LINE ( 'NONE', #68492, #59058 ) ;
#31723=CARTESIAN_POINT ( 'NONE',  ( 39.00000000000000000, 6.123233995736766282E-16, -5.000000000000000000 ) ) ;
#31744=AXIS2_PLACEMENT_3D ( 'NONE', #23653, #18338, #39905 ) ;
#31756=LINE ( 'NONE', #5234, #41224 ) ;
#31770=VERTEX_POINT ( 'NONE', #417 ) ;
#31784=( LENGTH_UNIT ( ) NAMED_UNIT ( * ) SI_UNIT ( .MILLI., .METRE. ) );
#31801=CIRCLE ( 'NONE', #1295, 24.99999999998794920 ) ;
#31807=CARTESIAN_POINT ( 'NONE',  ( 40.90000000000000568, 0.000000000000000000, 0.000000000000000000 ) ) ;
#31819=EDGE_CURVE ( 'NONE', #7937, #51374, #34207, .T. ) ;
#31820=ORIENTED_EDGE ( 'NONE', *, *, #29577, .T. ) ;
#31824=EDGE_LOOP ( 'NONE', ( #34923, #17692, #55305, #61259 ) ) ;
#31832=VERTEX_POINT ( 'NONE', #53474 ) ;
#31841=ORIENTED_EDGE ( 'NONE', *, *, #1580, .F. ) ;
#31849=CARTESIAN_POINT ( 'NONE',  ( 40.90000000000000568, -14.48845687959340012, 21.00000000000000000 ) ) ;
#31852=MECHANICAL_DESIGN_GEOMETRIC_PRESENTATION_REPRESENTATION('',(#28384),#14883);
#31863=VERTEX_POINT ( 'NONE', #26948 ) ;
#31867=FACE_OUTER_BOUND ( 'NONE', #28398, .T. ) ;
#31868=ORIENTED_EDGE ( 'NONE', *, *, #12781, .T. ) ;
#31872=FACE_OUTER_BOUND ( 'NONE', #63659, .T. ) ;
#31888=DIRECTION ( 'NONE',  ( -1.000000000000000000, 0.000000000000000000, 0.000000000000000000 ) ) ;
#31902=CIRCLE ( 'NONE', #37551, 3.500000000000000444 ) ;
#31908=ORIENTED_EDGE ( 'NONE', *, *, #66355, .F. ) ;
#31919=CARTESIAN_POINT ( 'NONE',  ( 30.90000000000000213, 20.60000000000000142, -13.86939075806900057 ) ) ;
#31920=DIRECTION ( 'NONE',  ( 0.000000000000000000, 0.000000000000000000, 1.000000000000000000 ) ) ;
#31921=CARTESIAN_POINT ( 'NONE',  ( 24.90000000000000213, 13.66939075806899950, 20.80000000000000426 ) ) ;
#31927=DIRECTION ( 'NONE',  ( 0.000000000000000000, 0.000000000000000000, -1.000000000000000000 ) ) ;
#31935=CARTESIAN_POINT ( 'NONE',  ( 33.89999999999999858, 20.60000000000000142, 2.801416793502919355E-15 ) ) ;
#31945=EDGE_CURVE ( 'NONE', #61504, #53333, #14414, .T. ) ;
#31946=DIRECTION ( 'NONE',  ( 0.000000000000000000, 0.000000000000000000, 1.000000000000000000 ) ) ;
#31950=ORIENTED_EDGE ( 'NONE', *, *, #30341, .F. ) ;
#31952=LINE ( 'NONE', #6115, #48153 ) ;
#31964=EDGE_CURVE ( 'NONE', #14096, #18237, #40918, .T. ) ;
#31965=CARTESIAN_POINT ( 'NONE',  ( 40.90000000000000568, -14.06939075806900874, 20.80000000000001137 ) ) ;
#31966=EDGE_CURVE ( 'NONE', #35449, #62948, #24766, .T. ) ;
#31987=EDGE_LOOP ( 'NONE', ( #34901, #50080, #1526, #40405 ) ) ;
#31990=VECTOR ( 'NONE', #33018, 1000.000000000000000 ) ;
#32006=LINE ( 'NONE', #48267, #3630 ) ;
#32009=EDGE_LOOP ( 'NONE', ( #39472, #54788, #9494, #32694 ) ) ;
#32012=DIRECTION ( 'NONE',  ( -1.000000000000000000, 0.000000000000000000, 0.000000000000000000 ) ) ;
#32015=ORIENTED_EDGE ( 'NONE', *, *, #49359, .T. ) ;
#32024=CIRCLE ( 'NONE', #34252, 0.5000000000000000000 ) ;
#32034=ADVANCED_FACE ( 'NONE', ( #21456 ), #10496, .T. ) ;
#32041=PLANE ( 'NONE',  #47139 ) ;
#32048=DIRECTION ( 'NONE',  ( 1.000000000000000000, -0.000000000000000000, 0.000000000000000000 ) ) ;
#32058=ORIENTED_EDGE ( 'NONE', *, *, #34931, .T. ) ;
#32060=CARTESIAN_POINT ( 'NONE',  ( 49.00000000000000000, 20.60000000000000142, -13.86939075806900057 ) ) ;
#32062=CARTESIAN_POINT ( 'NONE',  ( 49.00000000000000000, 20.60000000000000142, -13.86939075806900057 ) ) ;
#32070=ADVANCED_FACE ( 'NONE', ( #41977 ), #47982, .T. ) ;
#32075=ADVANCED_FACE ( 'NONE', ( #64593 ), #31392, .T. ) ;
#32096=CARTESIAN_POINT ( 'NONE',  ( 23.90000000000000213, 20.60000000000000142, -13.86939075806900057 ) ) ;
#32098=VERTEX_POINT ( 'NONE', #3799 ) ;
#32111=EDGE_CURVE ( 'NONE', #13215, #41070, #68509, .T. ) ;
#32122=VERTEX_POINT ( 'NONE', #6589 ) ;
#32127=FACE_OUTER_BOUND ( 'NONE', #5346, .T. ) ;
#32130=ORIENTED_EDGE ( 'NONE', *, *, #43753, .F. ) ;
#32136=SURFACE_STYLE_FILL_AREA ( #10565 ) ;
#32139=PLANE ( 'NONE',  #54481 ) ;
#32149=DIRECTION ( 'NONE',  ( 1.000000000000000000, -0.000000000000000000, 0.000000000000000000 ) ) ;
#32152=ORIENTED_EDGE ( 'NONE', *, *, #32689, .F. ) ;
#32153=ORIENTED_EDGE ( 'NONE', *, *, #18040, .F. ) ;
#32159=EDGE_CURVE ( 'NONE', #66978, #61720, #27046, .T. ) ;
#32172=CIRCLE ( 'NONE', #29923, 24.99999999998784972 ) ;
#32173=DIRECTION ( 'NONE',  ( 0.000000000000000000, 0.000000000000000000, -1.000000000000000000 ) ) ;
#32178=DIRECTION ( 'NONE',  ( 0.000000000000000000, 0.000000000000000000, 1.000000000000000000 ) ) ;
#32180=EDGE_LOOP ( 'NONE', ( #52328, #38447, #37090, #44474 ) ) ;
#32185=LINE ( 'NONE', #36804, #67163 ) ;
#32186=CARTESIAN_POINT ( 'NONE',  ( 39.00000000000000000, 16.96999999999999886, 21.00000000000000000 ) ) ;
#32204=ADVANCED_FACE ( 'NONE', ( #243 ), #591, .F. ) ;
#32206=VERTEX_POINT ( 'NONE', #60313 ) ;
#32214=CARTESIAN_POINT ( 'NONE',  ( 13.90000000000000213, -0.2000000000089119934, 8.909539772616881237E-12 ) ) ;
#32227=ORIENTED_EDGE ( 'NONE', *, *, #21859, .T. ) ;
#32229=LINE ( 'NONE', #65110, #107 ) ;
#32252=AXIS2_PLACEMENT_3D ( 'NONE', #40252, #57569, #51572 ) ;
#32276=VERTEX_POINT ( 'NONE', #22838 ) ;
#32297=ADVANCED_FACE ( 'NONE', ( #51807 ), #23884, .F. ) ;
#32317=CARTESIAN_POINT ( 'NONE',  ( 49.00000000000000000, 13.66939075806899950, 20.80000000000000426 ) ) ;
#32318=EDGE_LOOP ( 'NONE', ( #1710, #69208, #25386, #18366 ) ) ;
#32319=AXIS2_PLACEMENT_3D ( 'NONE', #5152, #68460, #3747 ) ;
#32355=DIRECTION ( 'NONE',  ( 1.000000000000000000, 0.000000000000000000, 0.000000000000000000 ) ) ;
#32363=VECTOR ( 'NONE', #63076, 1000.000000000000000 ) ;
#32365=ORIENTED_EDGE ( 'NONE', *, *, #59580, .T. ) ;
#32368=ADVANCED_FACE ( 'NONE', ( #28823 ), #45438, .T. ) ;
#32375=DIRECTION ( 'NONE',  ( -0.7071067811865475727, 0.7071067811865475727, 0.000000000000000000 ) ) ;
#32380=VECTOR ( 'NONE', #29403, 1000.000000000000000 ) ;
#32387=ADVANCED_FACE ( 'NONE', ( #9013 ), #36963, .F. ) ;
#32395=ORIENTED_EDGE ( 'NONE', *, *, #7113, .F. ) ;
#32402=DIRECTION ( 'NONE',  ( 0.000000000000000000, 0.000000000000000000, -1.000000000000000000 ) ) ;
#32403=DIRECTION ( 'NONE',  ( 1.000000000000000000, 0.000000000000000000, 0.000000000000000000 ) ) ;
#32406=VECTOR ( 'NONE', #64581, 1000.000000000000000 ) ;
#32410=CARTESIAN_POINT ( 'NONE',  ( 34.89999999999999858, 0.000000000000000000, 2.801416793502919355E-15 ) ) ;
#32411=CARTESIAN_POINT ( 'NONE',  ( 10.90000000000000036, 13.66939075806899950, 20.80000000000000426 ) ) ;
#32436=CARTESIAN_POINT ( 'NONE',  ( 28.90000000000000213, 0.000000000000000000, 2.458500000000000796 ) ) ;
#32438=EDGE_CURVE ( 'NONE', #53130, #19388, #52512, .T. ) ;
#32453=EDGE_LOOP ( 'NONE', ( #69001, #41275, #63533, #24063 ) ) ;
#32465=CARTESIAN_POINT ( 'NONE',  ( 47.00000000000000000, 0.7500000000000000000, -4.943429983321300014 ) ) ;
#32478=SURFACE_STYLE_USAGE ( .BOTH. , #20804 ) ;
#32485=CARTESIAN_POINT ( 'NONE',  ( 46.39999999999999858, 21.00000000000000000, 0.7500000000000000000 ) ) ;
#32489=DIRECTION ( 'NONE',  ( 0.000000000000000000, 0.000000000000000000, 1.000000000000000000 ) ) ;
#32506=DIRECTION ( 'NONE',  ( 0.000000000000000000, 1.000000000000000000, -0.000000000000000000 ) ) ;
#32510=CARTESIAN_POINT ( 'NONE',  ( 41.09999999999999432, 20.60000000000000142, 13.86939075806900057 ) ) ;
#32516=VECTOR ( 'NONE', #7395, 1000.000000000000000 ) ;
#32531=ORIENTED_EDGE ( 'NONE', *, *, #45787, .T. ) ;
#32533=AXIS2_PLACEMENT_3D ( 'NONE', #17581, #26833, #44111 ) ;
#32534=DIRECTION ( 'NONE',  ( -1.000000000000000000, 0.000000000000000000, 0.000000000000000000 ) ) ;
#32538=VERTEX_POINT ( 'NONE', #22080 ) ;
#32541=DIRECTION ( 'NONE',  ( 0.000000000000000000, 0.000000000000000000, -1.000000000000000000 ) ) ;
#32547=LINE ( 'NONE', #27238, #22009 ) ;
#32548=FACE_OUTER_BOUND ( 'NONE', #36024, .T. ) ;
#32549=CIRCLE ( 'NONE', #51716, 24.99999999998794920 ) ;
#32553=CARTESIAN_POINT ( 'NONE',  ( 41.09999999999999432, -21.00000000000000000, 13.86939075806900057 ) ) ;
#32556=CARTESIAN_POINT ( 'NONE',  ( 23.90000000000000213, 13.66939075806899240, -20.79999999999999361 ) ) ;
#32559=ORIENTED_EDGE ( 'NONE', *, *, #58060, .T. ) ;
#32562=DIRECTION ( 'NONE',  ( 1.000000000000000000, -0.000000000000000000, 0.000000000000000000 ) ) ;
#32579=CARTESIAN_POINT ( 'NONE',  ( 28.90000000000000213, 3.010794155703768650E-16, -2.458500000000000796 ) ) ;
#32584=CARTESIAN_POINT ( 'NONE',  ( 41.09999999999999432, 20.60000000000000142, 13.86939075806900057 ) ) ;
#32590=CARTESIAN_POINT ( 'NONE',  ( 41.09999999999999432, 13.66939075806899950, -20.80000000000000426 ) ) ;
#32592=DIRECTION ( 'NONE',  ( -1.000000000000000000, 0.000000000000000000, 0.000000000000000000 ) ) ;
#32596=ORIENTED_EDGE ( 'NONE', *, *, #490, .T. ) ;
#32600=DIRECTION ( 'NONE',  ( -1.000000000000000000, 0.000000000000000000, 0.000000000000000000 ) ) ;
#32607=VERTEX_POINT ( 'NONE', #32680 ) ;
#32622=ORIENTED_EDGE ( 'NONE', *, *, #68341, .F. ) ;
#32628=ORIENTED_EDGE ( 'NONE', *, *, #2822, .F. ) ;
#32651=ORIENTED_EDGE ( 'NONE', *, *, #36284, .F. ) ;
#32673=CARTESIAN_POINT ( 'NONE',  ( 41.09999999999999432, 13.66939075806899950, 20.80000000000000426 ) ) ;
#32680=CARTESIAN_POINT ( 'NONE',  ( 40.90000000000000568, 13.66939075806899240, 20.79999999999999361 ) ) ;
#32682=CARTESIAN_POINT ( 'NONE',  ( 41.09999999999999432, -21.00000000000000000, 13.86939075806900057 ) ) ;
#32683=VECTOR ( 'NONE', #25492, 1000.000000000000114 ) ;
#32686=EDGE_CURVE ( 'NONE', #53157, #11546, #50669, .T. ) ;
#32689=EDGE_CURVE ( 'NONE', #38911, #1574, #39480, .T. ) ;
#32694=ORIENTED_EDGE ( 'NONE', *, *, #61020, .F. ) ;
#32698=AXIS2_PLACEMENT_3D ( 'NONE', #50150, #51196, #17967 ) ;
#32705=VERTEX_POINT ( 'NONE', #7533 ) ;
#32720=ORIENTED_EDGE ( 'NONE', *, *, #18867, .T. ) ;
#32725=VERTEX_POINT ( 'NONE', #29449 ) ;
#32732=LINE ( 'NONE', #43336, #24567 ) ;
#32749=EDGE_CURVE ( 'NONE', #64704, #55424, #45705, .T. ) ;
#32752=CARTESIAN_POINT ( 'NONE',  ( 40.90000000000000568, -0.2000000000089119934, 8.909539772616881237E-12 ) ) ;
#32765=LINE ( 'NONE', #27462, #5900 ) ;
#32774=ADVANCED_FACE ( 'NONE', ( #24506 ), #29107, .T. ) ;
#32776=DIRECTION ( 'NONE',  ( 0.000000000000000000, 0.000000000000000000, -1.000000000000000000 ) ) ;
#32777=VECTOR ( 'NONE', #61463, 1000.000000000000000 ) ;
#32778=VERTEX_POINT ( 'NONE', #51368 ) ;
#32787=VECTOR ( 'NONE', #48815, 1000.000000000000000 ) ;
#32793=VERTEX_POINT ( 'NONE', #61618 ) ;
#32811=AXIS2_PLACEMENT_3D ( 'NONE', #39381, #12504, #34066 ) ;
#32817=DIRECTION ( 'NONE',  ( -1.000000000000000000, 0.000000000000000000, 0.000000000000000000 ) ) ;
#32824=CARTESIAN_POINT ( 'NONE',  ( 21.90000000000000213, 13.66939075806899240, -20.79999999999999361 ) ) ;
#32831=ORIENTED_EDGE ( 'NONE', *, *, #4465, .T. ) ;
#32840=CARTESIAN_POINT ( 'NONE',  ( 49.00000000000000000, -14.06939075806900163, -20.80000000000000426 ) ) ;
#32853=VECTOR ( 'NONE', #47120, 1000.000000000000000 ) ;
#32869=DIRECTION ( 'NONE',  ( -1.000000000000000000, 0.000000000000000000, 0.000000000000000000 ) ) ;
#32881=AXIS2_PLACEMENT_3D ( 'NONE', #7645, #35203, #56784 ) ;
#32903=EDGE_CURVE ( 'NONE', #56261, #55138, #51730, .T. ) ;
#32925=CARTESIAN_POINT ( 'NONE',  ( 41.09999999999999432, 14.08845687959340331, -21.00000000000000000 ) ) ;
#32929=AXIS2_PLACEMENT_3D ( 'NONE', #34785, #24886, #2613 ) ;
#32933=CARTESIAN_POINT ( 'NONE',  ( 10.00000000000000000, 21.00000000000000000, -18.00000000000000355 ) ) ;
#32936=LINE ( 'NONE', #69740, #22752 ) ;
#32937=ORIENTED_EDGE ( 'NONE', *, *, #11211, .F. ) ;
#32943=ORIENTED_EDGE ( 'NONE', *, *, #60854, .F. ) ;
#32946=CIRCLE ( 'NONE', #3574, 24.99999999998794920 ) ;
#32949=CARTESIAN_POINT ( 'NONE',  ( 39.00000000000000000, 0.000000000000000000, 3.500000000000000000 ) ) ;
#32950=EDGE_CURVE ( 'NONE', #14861, #29958, #65476, .T. ) ;
#32951=SURFACE_SIDE_STYLE ('',( #17371 ) ) ;
#32973=VERTEX_POINT ( 'NONE', #17033 ) ;
#32990=CARTESIAN_POINT ( 'NONE',  ( 41.09999999999999432, -21.00000000000000000, 14.57806571531351914 ) ) ;
#32993=VECTOR ( 'NONE', #56543, 1000.000000000000000 ) ;
#32997=ORIENTED_EDGE ( 'NONE', *, *, #57887, .F. ) ;
#32999=DIRECTION ( 'NONE',  ( 0.000000000000000000, 0.000000000000000000, -1.000000000000000000 ) ) ;
#33002=AXIS2_PLACEMENT_3D ( 'NONE', #8147, #18770, #12746 ) ;
#33006=AXIS2_PLACEMENT_3D ( 'NONE', #63910, #9462, #37046 ) ;
#33008=CARTESIAN_POINT ( 'NONE',  ( 39.00000000000000000, -21.00000000000000000, 16.96999999999999886 ) ) ;
#33011=AXIS2_PLACEMENT_3D ( 'NONE', #45165, #38831, #56147 ) ;
#33018=DIRECTION ( 'NONE',  ( 0.000000000000000000, 1.000000000000000000, -0.000000000000000000 ) ) ;
#33021=LINE ( 'NONE', #6148, #8607 ) ;
#33040=CIRCLE ( 'NONE', #8186, 24.99999999998794920 ) ;
#33041=DIRECTION ( 'NONE',  ( -1.000000000000000000, 0.000000000000000000, 0.000000000000000000 ) ) ;
#33042=CARTESIAN_POINT ( 'NONE',  ( 29.89999999999999858, 0.000000000000000000, 2.458500000000000796 ) ) ;
#33044=ORIENTED_EDGE ( 'NONE', *, *, #42272, .F. ) ;
#33050=VERTEX_POINT ( 'NONE', #49219 ) ;
#33054=CARTESIAN_POINT ( 'NONE',  ( 50.00000000000000000, 0.000000000000000000, 0.000000000000000000 ) ) ;
#33060=CARTESIAN_POINT ( 'NONE',  ( 49.00000000000000000, -0.7500000000000000000, -4.943429983321300014 ) ) ;
#33061=ORIENTED_EDGE ( 'NONE', *, *, #21613, .F. ) ;
#33070=FACE_OUTER_BOUND ( 'NONE', #3215, .T. ) ;
#33082=DIRECTION ( 'NONE',  ( 0.000000000000000000, 0.000000000000000000, -1.000000000000000000 ) ) ;
#33085=LINE ( 'NONE', #54660, #61511 ) ;
#33107=VECTOR ( 'NONE', #37721, 1000.000000000000000 ) ;
#33114=EDGE_LOOP ( 'NONE', ( #25116, #1612, #66952, #29563 ) ) ;
#33118=DIRECTION ( 'NONE',  ( 0.000000000000000000, 1.000000000000000000, 0.000000000000000000 ) ) ;
#33122=FACE_OUTER_BOUND ( 'NONE', #56038, .T. ) ;
#33124=EDGE_CURVE ( 'NONE', #25912, #31241, #10611, .T. ) ;
#33149=VERTEX_POINT ( 'NONE', #13099 ) ;
#33150=VERTEX_POINT ( 'NONE', #28671 ) ;
#33160=AXIS2_PLACEMENT_3D ( 'NONE', #18480, #40042, #34751 ) ;
#33161=CIRCLE ( 'NONE', #67024, 3.500000000000000444 ) ;
#33162=CARTESIAN_POINT ( 'NONE',  ( 49.00000000000000000, -0.2000000000089119934, 8.909539772616881237E-12 ) ) ;
#33169=LINE ( 'NONE', #39167, #40092 ) ;
#33174=ORIENTED_EDGE ( 'NONE', *, *, #4507, .T. ) ;
#33183=DIRECTION ( 'NONE',  ( 1.000000000000000000, -0.000000000000000000, 0.000000000000000000 ) ) ;
#33196=ORIENTED_EDGE ( 'NONE', *, *, #15197, .F. ) ;
#33207=ORIENTED_EDGE ( 'NONE', *, *, #52228, .T. ) ;
#33219=AXIS2_PLACEMENT_3D ( 'NONE', #53403, #43119, #48090 ) ;
#33229=CARTESIAN_POINT ( 'NONE',  ( 41.09999999999999432, 13.66939075806899950, -20.80000000000000426 ) ) ;
#33231=ADVANCED_FACE ( 'NONE', ( #57993 ), #19456, .F. ) ;
#33233=ORIENTED_EDGE ( 'NONE', *, *, #20366, .T. ) ;
#33235=DIRECTION ( 'NONE',  ( -1.000000000000000000, 0.000000000000000000, 0.000000000000000000 ) ) ;
#33239=CARTESIAN_POINT ( 'NONE',  ( 25.90000000000000213, -0.1999999999911430404, -8.864436962241481021E-12 ) ) ;
#33253=DIRECTION ( 'NONE',  ( 1.000000000000000000, -0.000000000000000000, 0.000000000000000000 ) ) ;
#33255=EDGE_CURVE ( 'NONE', #361, #53834, #25121, .T. ) ;
#33262=ORIENTED_EDGE ( 'NONE', *, *, #30201, .F. ) ;
#33274=CARTESIAN_POINT ( 'NONE',  ( 39.00000000000000000, -21.00000000000000000, -16.96999999999999886 ) ) ;
#33275=AXIS2_PLACEMENT_3D ( 'NONE', #37056, #54619, #58617 ) ;
#33278=PLANE ( 'NONE',  #52294 ) ;
#33288=VERTEX_POINT ( 'NONE', #9564 ) ;
#33292=ORIENTED_EDGE ( 'NONE', *, *, #45682, .F. ) ;
#33306=VERTEX_POINT ( 'NONE', #41019 ) ;
#33313=DIRECTION ( 'NONE',  ( 1.000000000000000000, -0.000000000000000000, 0.000000000000000000 ) ) ;
#33325=CARTESIAN_POINT ( 'NONE',  ( 49.00000000000000000, -0.7500000000000000000, -3.929058411375430104 ) ) ;
#33328=LINE ( 'NONE', #49251, #49417 ) ;
#33333=ORIENTED_EDGE ( 'NONE', *, *, #58509, .T. ) ;
#33334=LINE ( 'NONE', #44271, #64885 ) ;
#33347=DIRECTION ( 'NONE',  ( 0.000000000000000000, 0.7071067811865474617, -0.7071067811865474617 ) ) ;
#33348=CARTESIAN_POINT ( 'NONE',  ( 12.90000000000000213, -0.1999999999911795112, 8.826273045769999343E-12 ) ) ;
#33361=ORIENTED_EDGE ( 'NONE', *, *, #57009, .F. ) ;
#33371=CARTESIAN_POINT ( 'NONE',  ( 18.89999999999999858, -21.00000000000000000, 13.86939075806900057 ) ) ;
#33372=ORIENTED_EDGE ( 'NONE', *, *, #20897, .F. ) ;
#33373=DIRECTION ( 'NONE',  ( 1.000000000000000000, -0.000000000000000000, 0.000000000000000000 ) ) ;
#33381=ADVANCED_FACE ( 'NONE', ( #60075 ), #54440, .F. ) ;
#33382=CARTESIAN_POINT ( 'NONE',  ( 41.09999999999999432, -21.00000000000000000, 13.86939075806900057 ) ) ;
#33390=EDGE_CURVE ( 'NONE', #35406, #27652, #50166, .T. ) ;
#33402=ORIENTED_EDGE ( 'NONE', *, *, #3889, .T. ) ;
#33416=CONICAL_SURFACE ( 'NONE', #36810, 2.458500000000000796, 1.047019301333029784 ) ;
#33418=LINE ( 'NONE', #55002, #7451 ) ;
#33420=AXIS2_PLACEMENT_3D ( 'NONE', #4116, #68807, #31345 ) ;
#33424=CARTESIAN_POINT ( 'NONE',  ( 10.00000000000000000, 21.00000000000000000, 18.00000000000000355 ) ) ;
#33428=AXIS2_PLACEMENT_3D ( 'NONE', #38146, #6297, #54402 ) ;
#33437=SURFACE_STYLE_USAGE ( .BOTH. , #17863 ) ;
#33464=PLANE ( 'NONE',  #17598 ) ;
#33468=ADVANCED_FACE ( 'NONE', ( #42430 ), #59391, .F. ) ;
#33473=AXIS2_PLACEMENT_3D ( 'NONE', #56361, #17841, #40451 ) ;
#33477=PLANE ( 'NONE',  #36922 ) ;
#33478=LINE ( 'NONE', #55394, #59309 ) ;
#33487=VERTEX_POINT ( 'NONE', #10260 ) ;
#33488=AXIS2_PLACEMENT_3D ( 'NONE', #47093, #68666, #26222 ) ;
#33489=VERTEX_POINT ( 'NONE', #15913 ) ;
#33493=CIRCLE ( 'NONE', #64008, 25.39999999999999858 ) ;
#33494=AXIS2_PLACEMENT_3D ( 'NONE', #6028, #32562, #54127 ) ;
#33498=CARTESIAN_POINT ( 'NONE',  ( 41.09999999999999432, -14.06939075806900163, 20.80000000000000426 ) ) ;
#33501=ORIENTED_EDGE ( 'NONE', *, *, #4214, .T. ) ;
#33506=CYLINDRICAL_SURFACE ( 'NONE', #49934, 24.99999999998784972 ) ;
#33509=EDGE_CURVE ( 'NONE', #61702, #20422, #64878, .T. ) ;
#33520=FACE_OUTER_BOUND ( 'NONE', #14854, .T. ) ;
#33524=DIRECTION ( 'NONE',  ( -1.000000000000000000, 0.000000000000000000, 0.000000000000000000 ) ) ;
#33525=VERTEX_POINT ( 'NONE', #18311 ) ;
#33533=VERTEX_POINT ( 'NONE', #61440 ) ;
#33536=CARTESIAN_POINT ( 'NONE',  ( 41.09999999999999432, -14.06939075806901940, -20.80000000000000426 ) ) ;
#33541=ORIENTED_EDGE ( 'NONE', *, *, #54144, .F. ) ;
#33557=DIRECTION ( 'NONE',  ( 1.000000000000000000, -0.000000000000000000, 0.000000000000000000 ) ) ;
#33561=ORIENTED_EDGE ( 'NONE', *, *, #57472, .T. ) ;
#33565=ADVANCED_FACE ( 'NONE', ( #44156 ), #6672, .F. ) ;
#33573=CARTESIAN_POINT ( 'NONE',  ( 39.90000000000000568, -16.96999999999999886, -21.00000000000000000 ) ) ;
#33585=DIRECTION ( 'NONE',  ( -1.000000000000000000, 0.000000000000000000, 0.000000000000000000 ) ) ;
#33595=SHAPE_REPRESENTATION ( 'Stepper Motor', ( #45918 ), #55023 ) ;
#33600=AXIS2_PLACEMENT_3D ( 'NONE', #32933, #22342, #17020 ) ;
#33617=CARTESIAN_POINT ( 'NONE',  ( 27.00000000000000000, 0.000000000000000000, -2.458500000000000796 ) ) ;
#33619=FACE_BOUND ( 'NONE', #54590, .T. ) ;
#33629=DIRECTION ( 'NONE',  ( -1.000000000000000000, 0.000000000000000000, 0.000000000000000000 ) ) ;
#33630=CARTESIAN_POINT ( 'NONE',  ( 29.89999999999999858, -0.1999999999911430404, -8.864436962241481021E-12 ) ) ;
#33644=ORIENTED_EDGE ( 'NONE', *, *, #26825, .T. ) ;
#33655=VERTEX_POINT ( 'NONE', #68524 ) ;
#33656=CIRCLE ( 'NONE', #61960, 24.99999999998794920 ) ;
#33666=DIRECTION ( 'NONE',  ( 0.000000000000000000, 0.000000000000000000, 1.000000000000000000 ) ) ;
#33684=DIRECTION ( 'NONE',  ( 0.000000000000000000, 0.000000000000000000, 1.000000000000000000 ) ) ;
#33719=EDGE_CURVE ( 'NONE', #11562, #49395, #68871, .T. ) ;
#33720=CARTESIAN_POINT ( 'NONE',  ( 16.89999999999999858, -14.06939075806900163, -20.80000000000000426 ) ) ;
#33737=CIRCLE ( 'NONE', #3261, 24.99999999998794920 ) ;
#33738=ORIENTED_EDGE ( 'NONE', *, *, #68021, .T. ) ;
#33752=ORIENTED_EDGE ( 'NONE', *, *, #17591, .F. ) ;
#33757=DIRECTION ( 'NONE',  ( 0.000000000000000000, 0.8346456692913387654, 0.5507872608668551440 ) ) ;
#33761=ADVANCED_FACE ( 'NONE', ( #39031 ), #44325, .T. ) ;
#33769=EDGE_CURVE ( 'NONE', #24647, #29693, #60934, .T. ) ;
#33772=FILL_AREA_STYLE ('',( #49692 ) ) ;
#33783=CARTESIAN_POINT ( 'NONE',  ( 28.90000000000000213, -0.1999999999911795112, 8.826273045769999343E-12 ) ) ;
#33814=PLANE ( 'NONE',  #55344 ) ;
#33829=VECTOR ( 'NONE', #33524, 1000.000000000000000 ) ;
#33838=DIRECTION ( 'NONE',  ( 0.000000000000000000, 0.5625376724249369076, -0.8267716535433071723 ) ) ;
#33840=DIRECTION ( 'NONE',  ( 0.000000000000000000, 0.000000000000000000, -1.000000000000000000 ) ) ;
#33841=CIRCLE ( 'NONE', #28203, 24.99999999998794920 ) ;
#33854=AXIS2_PLACEMENT_3D ( 'NONE', #48914, #25962, #134 ) ;
#33868=VERTEX_POINT ( 'NONE', #28085 ) ;
#33891=CARTESIAN_POINT ( 'NONE',  ( 40.90000000000000568, 0.000000000000000000, 5.000000000000000000 ) ) ;
#33893=ORIENTED_EDGE ( 'NONE', *, *, #55239, .T. ) ;
#33917=ORIENTED_EDGE ( 'NONE', *, *, #35131, .T. ) ;
#33922=DIRECTION ( 'NONE',  ( 1.000000000000000000, 0.000000000000000000, 0.000000000000000000 ) ) ;
#33932=EDGE_LOOP ( 'NONE', ( #61798, #27547 ) ) ;
#33938=AXIS2_PLACEMENT_3D ( 'NONE', #13776, #13430, #30399 ) ;
#33940=ORIENTED_EDGE ( 'NONE', *, *, #16073, .T. ) ;
#33943=EDGE_LOOP ( 'NONE', ( #26196, #44482, #65242, #15629 ) ) ;
#33944=VECTOR ( 'NONE', #62393, 1000.000000000000000 ) ;
#33946=LINE ( 'NONE', #20047, #7496 ) ;
#33960=( LENGTH_UNIT ( ) NAMED_UNIT ( * ) SI_UNIT ( .MILLI., .METRE. ) );
#33970=FILL_AREA_STYLE ('',( #22355 ) ) ;
#33979=DIRECTION ( 'NONE',  ( 0.000000000000000000, 1.000000000000000000, 0.000000000000000000 ) ) ;
#33985=ORIENTED_EDGE ( 'NONE', *, *, #40714, .T. ) ;
#33987=EDGE_CURVE ( 'NONE', #4186, #39384, #562, .T. ) ;
#33995=EDGE_CURVE ( 'NONE', #7460, #55486, #50333, .T. ) ;
#34001=SURFACE_SIDE_STYLE ('',( #45302 ) ) ;
#34003=EDGE_LOOP ( 'NONE', ( #24379, #51351, #10216, #38533 ) ) ;
#34011=CARTESIAN_POINT ( 'NONE',  ( 39.00000000000000000, -5.250000000000000000, 0.000000000000000000 ) ) ;
#34017=CYLINDRICAL_SURFACE ( 'NONE', #7478, 24.99999999998784972 ) ;
#34020=LINE ( 'NONE', #17776, #48306 ) ;
#34026=EDGE_CURVE ( 'NONE', #9337, #69324, #61628, .T. ) ;
#34029=EDGE_CURVE ( 'NONE', #12098, #9916, #2591, .T. ) ;
#34033=ORIENTED_EDGE ( 'NONE', *, *, #14647, .T. ) ;
#34047=DIRECTION ( 'NONE',  ( 1.000000000000000000, -0.000000000000000000, 0.000000000000000000 ) ) ;
#34064=ORIENTED_EDGE ( 'NONE', *, *, #42882, .F. ) ;
#34065=ADVANCED_FACE ( 'NONE', ( #20603 ), #9304, .T. ) ;
#34066=DIRECTION ( 'NONE',  ( 0.000000000000000000, 0.000000000000000000, 1.000000000000000000 ) ) ;
#34069=ORIENTED_EDGE ( 'NONE', *, *, #42666, .F. ) ;
#34072=CARTESIAN_POINT ( 'NONE',  ( 10.00000000000000000, 21.00000000000000000, -13.98999642601811999 ) ) ;
#34076=ORIENTED_EDGE ( 'NONE', *, *, #10398, .T. ) ;
#34091=DIRECTION ( 'NONE',  ( 0.000000000000000000, 0.000000000000000000, 1.000000000000000000 ) ) ;
#34101=VECTOR ( 'NONE', #67532, 1000.000000000000114 ) ;
#34103=CARTESIAN_POINT ( 'NONE',  ( 12.90000000000000213, 13.66939075806899950, 20.80000000000000426 ) ) ;
#34116=PLANE ( 'NONE',  #17219 ) ;
#34118=DIRECTION ( 'NONE',  ( 0.000000000000000000, 0.000000000000000000, -1.000000000000000000 ) ) ;
#34124=AXIS2_PLACEMENT_3D ( 'NONE', #22892, #29221, #61393 ) ;
#34128=CARTESIAN_POINT ( 'NONE',  ( 8.900000000000005684, -21.00000000000000000, 13.86939075806900057 ) ) ;
#34129=ORIENTED_EDGE ( 'NONE', *, *, #69768, .F. ) ;
#34141=CIRCLE ( 'NONE', #39794, 0.5000000000000000000 ) ;
#34156=LINE ( 'NONE', #18597, #10791 ) ;
#34167=DIRECTION ( 'NONE',  ( -1.000000000000000000, 0.000000000000000000, 0.000000000000000000 ) ) ;
#34170=CARTESIAN_POINT ( 'NONE',  ( 41.09999999999999432, 13.66939075806899950, -20.80000000000000426 ) ) ;
#34195=EDGE_LOOP ( 'NONE', ( #18956, #60688, #25818, #11182 ) ) ;
#34200=CARTESIAN_POINT ( 'NONE',  ( 49.00000000000000000, -14.06939075806900163, -20.80000000000000426 ) ) ;
#34207=CIRCLE ( 'NONE', #15068, 24.99999999998784972 ) ;
#34215=VERTEX_POINT ( 'NONE', #1136 ) ;
#34238=AXIS2_PLACEMENT_3D ( 'NONE', #51616, #67877, #13067 ) ;
#34243=VERTEX_POINT ( 'NONE', #804 ) ;
#34252=AXIS2_PLACEMENT_3D ( 'NONE', #69250, #20806, #37089 ) ;
#34262=LINE ( 'NONE', #6707, #20082 ) ;
#34264=DIRECTION ( 'NONE',  ( -1.000000000000000000, 0.000000000000000000, 0.000000000000000000 ) ) ;
#34278=VERTEX_POINT ( 'NONE', #43089 ) ;
#34279=CARTESIAN_POINT ( 'NONE',  ( 9.899999999999998579, 13.66939075806899240, 20.79999999999999361 ) ) ;
#34282=ORIENTED_EDGE ( 'NONE', *, *, #31604, .F. ) ;
#34285=SURFACE_STYLE_FILL_AREA ( #61159 ) ;
#34299=AXIS2_PLACEMENT_3D ( 'NONE', #56246, #7448, #1800 ) ;
#34303=ORIENTED_EDGE ( 'NONE', *, *, #16394, .F. ) ;
#34312=CARTESIAN_POINT ( 'NONE',  ( 39.90000000000000568, 0.000000000000000000, 5.000000000000000000 ) ) ;
#34324=VERTEX_POINT ( 'NONE', #14836 ) ;
#34325=CIRCLE ( 'NONE', #58079, 3.500000000000000444 ) ;
#34326=DIRECTION ( 'NONE',  ( 1.000000000000000000, -0.000000000000000000, 0.000000000000000000 ) ) ;
#34327=LINE ( 'NONE', #7470, #54869 ) ;
#34337=LINE ( 'NONE', #12425, #15942 ) ;
#34339=ORIENTED_EDGE ( 'NONE', *, *, #67493, .T. ) ;
#34342=VECTOR ( 'NONE', #42068, 1000.000000000000000 ) ;
#34346=LINE ( 'NONE', #28711, #50415 ) ;
#34347=CARTESIAN_POINT ( 'NONE',  ( 32.89999999999999858, 0.000000000000000000, 2.585923194002694273E-15 ) ) ;
#34374=DIRECTION ( 'NONE',  ( 0.000000000000000000, 0.000000000000000000, 1.000000000000000000 ) ) ;
#34391=( GEOMETRIC_REPRESENTATION_CONTEXT ( 3 ) GLOBAL_UNCERTAINTY_ASSIGNED_CONTEXT ( ( #4800 ) ) GLOBAL_UNIT_ASSIGNED_CONTEXT ( ( #66052, #14680, #39190 ) ) REPRESENTATION_CONTEXT ( 'NONE', 'WORKASPACE' ) );
#34393=ORIENTED_EDGE ( 'NONE', *, *, #9526, .F. ) ;
#34398=DIRECTION ( 'NONE',  ( 0.000000000000000000, 0.000000000000000000, 1.000000000000000000 ) ) ;
#34403=EDGE_LOOP ( 'NONE', ( #34393, #42414, #51895, #17103 ) ) ;
#34412=EDGE_CURVE ( 'NONE', #13299, #55616, #47353, .T. ) ;
#34420=CARTESIAN_POINT ( 'NONE',  ( 10.00000000000000000, 18.00000000000000355, -21.00000000000000000 ) ) ;
#34421=DIRECTION ( 'NONE',  ( -1.000000000000000000, 0.000000000000000000, 0.000000000000000000 ) ) ;
#34422=DIRECTION ( 'NONE',  ( 0.000000000000000000, 0.000000000000000000, 1.000000000000000000 ) ) ;
#34447=PLANE ( 'NONE',  #49402 ) ;
#34449=( LENGTH_UNIT ( ) NAMED_UNIT ( * ) SI_UNIT ( .MILLI., .METRE. ) );
#34450=CARTESIAN_POINT ( 'NONE',  ( 40.90000000000000568, 0.000000000000000000, 3.447897592003593022E-15 ) ) ;
#34456=COLOUR_RGB ( '', 0.31764706, 0.68627451, 0.89019608) ;
#34461=CARTESIAN_POINT ( 'NONE',  ( 10.00000000000000000, -18.00000000000000355, -21.00000000000000000 ) ) ;
#34465=FACE_OUTER_BOUND ( 'NONE', #8045, .T. ) ;
#34472=VERTEX_POINT ( 'NONE', #31424 ) ;
#34474=EDGE_CURVE ( 'NONE', #32122, #40849, #69510, .T. ) ;
#34477=VECTOR ( 'NONE', #27539, 1000.000000000000000 ) ;
#34483=ORIENTED_EDGE ( 'NONE', *, *, #45139, .F. ) ;
#34503=ORIENTED_EDGE ( 'NONE', *, *, #22905, .F. ) ;
#34528=CARTESIAN_POINT ( 'NONE',  ( 22.90000000000000213, 20.60000000000000142, 13.86939075806900057 ) ) ;
#34541=DIRECTION ( 'NONE',  ( 1.000000000000000000, -0.000000000000000000, 0.000000000000000000 ) ) ;
#34551=ORIENTED_EDGE ( 'NONE', *, *, #14879, .F. ) ;
#34552=DIRECTION ( 'NONE',  ( -1.000000000000000000, 0.000000000000000000, 0.000000000000000000 ) ) ;
#34554=AXIS2_PLACEMENT_3D ( 'NONE', #23489, #56011, #45041 ) ;
#34556=DIRECTION ( 'NONE',  ( 0.000000000000000000, 0.000000000000000000, 1.000000000000000000 ) ) ;
#34559=VERTEX_POINT ( 'NONE', #60003 ) ;
#34564=EDGE_LOOP ( 'NONE', ( #10081, #15933, #13629, #65890 ) ) ;
#34566=ADVANCED_FACE ( 'NONE', ( #28176 ), #49746, .T. ) ;
#34577=FACE_OUTER_BOUND ( 'NONE', #55733, .T. ) ;
#34580=MECHANICAL_DESIGN_GEOMETRIC_PRESENTATION_REPRESENTATION('',(#15429),#16541);
#34582=CARTESIAN_POINT ( 'NONE',  ( 20.90000000000000213, 0.000000000000000000, 1.292961597001347137E-15 ) ) ;
#34584=CARTESIAN_POINT ( 'NONE',  ( 0.5000000000000000000, 18.00000000000000355, 21.00000000000000000 ) ) ;
#34598=LINE ( 'NONE', #61836, #14486 ) ;
#34610=DIRECTION ( 'NONE',  ( 1.000000000000000000, -0.000000000000000000, 0.000000000000000000 ) ) ;
#34613=CARTESIAN_POINT ( 'NONE',  ( 33.89999999999999858, 3.010794155703768650E-16, -2.458500000000000796 ) ) ;
#34616=EDGE_LOOP ( 'NONE', ( #52787, #30996, #39360, #54168 ) ) ;
#34637=EDGE_CURVE ( 'NONE', #45732, #12812, #44767, .T. ) ;
#34638=DIRECTION ( 'NONE',  ( 0.000000000000000000, 0.000000000000000000, -1.000000000000000000 ) ) ;
#34644=VECTOR ( 'NONE', #24004, 1000.000000000000000 ) ;
#34660=AXIS2_PLACEMENT_3D ( 'NONE', #7652, #14004, #62434 ) ;
#34661=CARTESIAN_POINT ( 'NONE',  ( 32.89999999999999858, 20.60000000000000142, -13.86939075806900057 ) ) ;
#34667=AXIS2_PLACEMENT_3D ( 'NONE', #1755, #7400, #23666 ) ;
#34692=AXIS2_PLACEMENT_3D ( 'NONE', #36635, #29925, #3759 ) ;
#34693=FACE_OUTER_BOUND ( 'NONE', #61018, .T. ) ;
#34738=LINE ( 'NONE', #56313, #41527 ) ;
#34748=EDGE_LOOP ( 'NONE', ( #36574, #26964, #66872, #66771 ) ) ;
#34751=DIRECTION ( 'NONE',  ( 0.000000000000000000, 0.000000000000000000, 1.000000000000000000 ) ) ;
#34760=ORIENTED_EDGE ( 'NONE', *, *, #4944, .T. ) ;
#34767=PLANE ( 'NONE',  #9441 ) ;
#34780=CARTESIAN_POINT ( 'NONE',  ( 8.900000000000005684, 13.66939075806899950, 20.80000000000000426 ) ) ;
#34782=ORIENTED_EDGE ( 'NONE', *, *, #37248, .F. ) ;
#34785=CARTESIAN_POINT ( 'NONE',  ( 31.89999999999999858, 0.000000000000000000, 0.000000000000000000 ) ) ;
#34806=PLANE ( 'NONE',  #30011 ) ;
#34825=CARTESIAN_POINT ( 'NONE',  ( 33.89999999999999858, -0.000000000000000000, -20.80000000000000071 ) ) ;
#34827=DIRECTION ( 'NONE',  ( 0.000000000000000000, 1.000000000000000000, 0.000000000000000000 ) ) ;
#34833=LINE ( 'NONE', #18938, #37505 ) ;
#34834=ORIENTED_EDGE ( 'NONE', *, *, #21580, .T. ) ;
#34841=AXIS2_PLACEMENT_3D ( 'NONE', #23801, #7532, #41102 ) ;
#34850=VERTEX_POINT ( 'NONE', #24964 ) ;
#34859=VERTEX_POINT ( 'NONE', #25685 ) ;
#34867=DIRECTION ( 'NONE',  ( 1.000000000000000000, 0.000000000000000000, 0.000000000000000000 ) ) ;
#34878=CARTESIAN_POINT ( 'NONE',  ( 40.90000000000000568, 0.000000000000000000, 3.500000000000000000 ) ) ;
#34885=ADVANCED_FACE ( 'NONE', ( #42624, #4804 ), #58191, .F. ) ;
#34887=CARTESIAN_POINT ( 'NONE',  ( 40.90000000000000568, 0.000000000000000000, 0.000000000000000000 ) ) ;
#34897=CARTESIAN_POINT ( 'NONE',  ( 49.00000000000000000, -14.06939075806900163, -20.80000000000000426 ) ) ;
#34900=CARTESIAN_POINT ( 'NONE',  ( 30.90000000000000213, 13.66939075806899240, 20.79999999999999361 ) ) ;
#34901=ORIENTED_EDGE ( 'NONE', *, *, #11246, .T. ) ;
#34905=EDGE_LOOP ( 'NONE', ( #25993, #13512, #29476, #39941 ) ) ;
#34910=ADVANCED_FACE ( 'NONE', ( #64553 ), #9766, .T. ) ;
#34917=ORIENTED_EDGE ( 'NONE', *, *, #4244, .F. ) ;
#34919=DIRECTION ( 'NONE',  ( 0.000000000000000000, 0.000000000000000000, -1.000000000000000000 ) ) ;
#34923=ORIENTED_EDGE ( 'NONE', *, *, #20710, .F. ) ;
#34930=ORIENTED_EDGE ( 'NONE', *, *, #53100, .T. ) ;
#34931=EDGE_CURVE ( 'NONE', #10558, #51495, #51484, .T. ) ;
#34938=DIRECTION ( 'NONE',  ( -1.000000000000000000, 0.000000000000000000, 0.000000000000000000 ) ) ;
#34944=EDGE_CURVE ( 'NONE', #24837, #11985, #15358, .T. ) ;
#34973=CARTESIAN_POINT ( 'NONE',  ( 39.90000000000000568, 0.000000000000000000, 0.000000000000000000 ) ) ;
#34977=ORIENTED_EDGE ( 'NONE', *, *, #23611, .F. ) ;
#34978=DIRECTION ( 'NONE',  ( 0.000000000000000000, 1.000000000000000000, 0.000000000000000000 ) ) ;
#34984=CYLINDRICAL_SURFACE ( 'NONE', #33938, 24.99999999998789946 ) ;
#34994=VECTOR ( 'NONE', #41616, 1000.000000000000000 ) ;
#34997=VERTEX_POINT ( 'NONE', #5847 ) ;
#35002=LINE ( 'NONE', #56579, #38909 ) ;
#35008=ORIENTED_EDGE ( 'NONE', *, *, #52090, .F. ) ;
#35024=ORIENTED_EDGE ( 'NONE', *, *, #6047, .T. ) ;
#35034=DIRECTION ( 'NONE',  ( 0.000000000000000000, 0.000000000000000000, -1.000000000000000000 ) ) ;
#35050=CYLINDRICAL_SURFACE ( 'NONE', #21642, 25.39999999999999858 ) ;
#35051=DIRECTION ( 'NONE',  ( -1.000000000000000000, 0.000000000000000000, 0.000000000000000000 ) ) ;
#35065=AXIS2_PLACEMENT_3D ( 'NONE', #53101, #63703, #9963 ) ;
#35067=ORIENTED_EDGE ( 'NONE', *, *, #30204, .F. ) ;
#35079=ORIENTED_EDGE ( 'NONE', *, *, #39865, .F. ) ;
#35082=ORIENTED_EDGE ( 'NONE', *, *, #495, .T. ) ;
#35086=ORIENTED_EDGE ( 'NONE', *, *, #3185, .F. ) ;
#35092=CIRCLE ( 'NONE', #48643, 25.39999999999999858 ) ;
#35105=DIRECTION ( 'NONE',  ( 0.000000000000000000, 0.000000000000000000, -1.000000000000000000 ) ) ;
#35111=ORIENTED_EDGE ( 'NONE', *, *, #60152, .F. ) ;
#35112=ORIENTED_EDGE ( 'NONE', *, *, #45389, .T. ) ;
#35126=LINE ( 'NONE', #50351, #1741 ) ;
#35129=CARTESIAN_POINT ( 'NONE',  ( 40.90000000000000568, -21.00000000000000000, 13.86939075806900057 ) ) ;
#35131=EDGE_CURVE ( 'NONE', #28954, #31270, #18517, .T. ) ;
#35133=DIRECTION ( 'NONE',  ( 0.000000000000000000, 0.000000000000000000, -1.000000000000000000 ) ) ;
#35148=DIRECTION ( 'NONE',  ( 0.000000000000000000, -1.000000000000000000, 0.000000000000000000 ) ) ;
#35151=ORIENTED_EDGE ( 'NONE', *, *, #63292, .F. ) ;
#35156=DIRECTION ( 'NONE',  ( 0.000000000000000000, 0.000000000000000000, 1.000000000000000000 ) ) ;
#35158=DIRECTION ( 'NONE',  ( 0.000000000000000000, -1.000000000000000000, 0.000000000000000000 ) ) ;
#35161=VECTOR ( 'NONE', #55948, 1000.000000000000000 ) ;
#35175=CIRCLE ( 'NONE', #54441, 24.99999999998784972 ) ;
#35180=DIRECTION ( 'NONE',  ( -1.000000000000000000, 0.000000000000000000, 0.000000000000000000 ) ) ;
#35187=CYLINDRICAL_SURFACE ( 'NONE', #29113, 25.39999999999999858 ) ;
#35198=ADVANCED_FACE ( 'NONE', ( #40797 ), #12514, .T. ) ;
#35201=ADVANCED_FACE ( 'NONE', ( #51052 ), #13222, .T. ) ;
#35203=DIRECTION ( 'NONE',  ( 0.000000000000000000, 0.000000000000000000, 1.000000000000000000 ) ) ;
#35218=CARTESIAN_POINT ( 'NONE',  ( 41.09999999999999432, 21.00000000000000000, 13.98999642601811999 ) ) ;
#35228=SURFACE_STYLE_USAGE ( .BOTH. , #57514 ) ;
#35240=DIRECTION ( 'NONE',  ( 0.000000000000000000, 0.000000000000000000, -1.000000000000000000 ) ) ;
#35241=EDGE_CURVE ( 'NONE', #39718, #55138, #45738, .T. ) ;
#35243=PRESENTATION_STYLE_ASSIGNMENT (( #46563 ) ) ;
#35268=LINE ( 'NONE', #12656, #6364 ) ;
#35271=ORIENTED_EDGE ( 'NONE', *, *, #44090, .F. ) ;
#35276=DIRECTION ( 'NONE',  ( 1.000000000000000000, 0.000000000000000000, 0.000000000000000000 ) ) ;
#35291=DIRECTION ( 'NONE',  ( 0.000000000000000000, -0.7071067811865475727, 0.7071067811865475727 ) ) ;
#35295=EDGE_CURVE ( 'NONE', #68514, #11420, #65079, .T. ) ;
#35316=ORIENTED_EDGE ( 'NONE', *, *, #46976, .F. ) ;
#35337=LINE ( 'NONE', #56913, #26197 ) ;
#35343=ORIENTED_EDGE ( 'NONE', *, *, #5300, .F. ) ;
#35349=DIRECTION ( 'NONE',  ( 1.000000000000000000, -0.000000000000000000, 0.000000000000000000 ) ) ;
#35363=DIRECTION ( 'NONE',  ( 0.000000000000000000, 0.000000000000000000, 1.000000000000000000 ) ) ;
#35370=( GEOMETRIC_REPRESENTATION_CONTEXT ( 3 ) GLOBAL_UNCERTAINTY_ASSIGNED_CONTEXT ( ( #41576 ) ) GLOBAL_UNIT_ASSIGNED_CONTEXT ( ( #22887, #61045, #55086 ) ) REPRESENTATION_CONTEXT ( 'NONE', 'WORKASPACE' ) );
#35373=ADVANCED_FACE ( 'NONE', ( #27932 ), #27581, .T. ) ;
#35374=CARTESIAN_POINT ( 'NONE',  ( 39.00000000000000000, 0.000000000000000000, 0.000000000000000000 ) ) ;
#35376=ORIENTED_EDGE ( 'NONE', *, *, #6094, .T. ) ;
#35392=SURFACE_STYLE_FILL_AREA ( #14899 ) ;
#35396=PRESENTATION_STYLE_ASSIGNMENT (( #32478 ) ) ;
#35406=VERTEX_POINT ( 'NONE', #11993 ) ;
#35425=ORIENTED_EDGE ( 'NONE', *, *, #26010, .F. ) ;
#35449=VERTEX_POINT ( 'NONE', #60788 ) ;
#35450=MECHANICAL_DESIGN_GEOMETRIC_PRESENTATION_REPRESENTATION('',(#4992),#45640);
#35463=CARTESIAN_POINT ( 'NONE',  ( 10.90000000000000036, -14.06939075806900163, -20.80000000000000426 ) ) ;
#35465=CIRCLE ( 'NONE', #6162, 24.99999999998794920 ) ;
#35466=CIRCLE ( 'NONE', #29822, 24.99999999998784972 ) ;
#35468=CARTESIAN_POINT ( 'NONE',  ( 39.00000000000000000, -16.96999999999999886, 21.00000000000000000 ) ) ;
#35475=VERTEX_POINT ( 'NONE', #55835 ) ;
#35477=DIRECTION ( 'NONE',  ( -1.000000000000000000, 0.000000000000000000, 0.000000000000000000 ) ) ;
#35499=FACE_OUTER_BOUND ( 'NONE', #14261, .T. ) ;
#35511=VECTOR ( 'NONE', #33629, 1000.000000000000000 ) ;
#35512=ORIENTED_EDGE ( 'NONE', *, *, #11202, .F. ) ;
#35517=EDGE_CURVE ( 'NONE', #7472, #64694, #52726, .T. ) ;
#35518=DIRECTION ( 'NONE',  ( 0.000000000000000000, 0.000000000000000000, -1.000000000000000000 ) ) ;
#35521=CARTESIAN_POINT ( 'NONE',  ( 30.90000000000000213, 3.010794155703768650E-16, -2.458500000000000796 ) ) ;
#35522=EDGE_CURVE ( 'NONE', #36902, #19691, #56531, .T. ) ;
#35524=DIRECTION ( 'NONE',  ( -0.7071067811865476838, -0.4999999999999997780, 0.4999999999999997780 ) ) ;
#35526=STYLED_ITEM ( 'NONE', ( #40107 ), #44406 ) ;
#35528=DIRECTION ( 'NONE',  ( 0.000000000000000000, 1.000000000000000000, 0.000000000000000000 ) ) ;
#35535=VERTEX_POINT ( 'NONE', #19053 ) ;
#35542=VERTEX_POINT ( 'NONE', #19395 ) ;
#35568=CARTESIAN_POINT ( 'NONE',  ( 17.89999999999999858, -0.000000000000000000, 20.80000000000000426 ) ) ;
#35573=CARTESIAN_POINT ( 'NONE',  ( 39.00000000000000000, -16.96999999999999886, -21.00000000000000000 ) ) ;
#35579=CARTESIAN_POINT ( 'NONE',  ( 9.900000000000000355, 0.000000000000000000, 2.154935995002245639E-16 ) ) ;
#35590=CARTESIAN_POINT ( 'NONE',  ( 49.00000000000000000, -0.2000000000089119934, 8.909539772616881237E-12 ) ) ;
#35594=AXIS2_PLACEMENT_3D ( 'NONE', #1361, #65381, #44476 ) ;
#35595=ORIENTED_EDGE ( 'NONE', *, *, #36587, .F. ) ;
#35601=ADVANCED_FACE ( 'NONE', ( #14094 ), #8798, .T. ) ;
#35611=ORIENTED_EDGE ( 'NONE', *, *, #69723, .T. ) ;
#35622=ADVANCED_FACE ( 'NONE', ( #36013 ), #57583, .F. ) ;
#35630=DIRECTION ( 'NONE',  ( 1.000000000000000000, 0.000000000000000000, 0.000000000000000000 ) ) ;
#35633=CARTESIAN_POINT ( 'NONE',  ( 34.89999999999999858, -0.2000000000089119934, -8.913009219568841313E-12 ) ) ;
#35638=LINE ( 'NONE', #67833, #17277 ) ;
#35639=VERTEX_POINT ( 'NONE', #3843 ) ;
#35645=EDGE_CURVE ( 'NONE', #28489, #43571, #25412, .T. ) ;
#35646=CYLINDRICAL_SURFACE ( 'NONE', #51577, 24.99999999998784972 ) ;
#35647=AXIS2_PLACEMENT_3D ( 'NONE', #23535, #13273, #7620 ) ;
#35649=EDGE_CURVE ( 'NONE', #17758, #11032, #15159, .T. ) ;
#35662=DIRECTION ( 'NONE',  ( 0.000000000000000000, 0.000000000000000000, 1.000000000000000000 ) ) ;
#35676=CARTESIAN_POINT ( 'NONE',  ( 25.57999999999999829, 0.000000000000000000, 0.000000000000000000 ) ) ;
#35682=CARTESIAN_POINT ( 'NONE',  ( 11.90000000000000036, -21.00000000000000000, 13.86939075806900057 ) ) ;
#35704=VECTOR ( 'NONE', #58861, 1000.000000000000114 ) ;
#35707=FACE_OUTER_BOUND ( 'NONE', #62319, .T. ) ;
#35708=ORIENTED_EDGE ( 'NONE', *, *, #69472, .T. ) ;
#35713=ORIENTED_EDGE ( 'NONE', *, *, #41114, .F. ) ;
#35718=LINE ( 'NONE', #25119, #46200 ) ;
#35738=DIRECTION ( 'NONE',  ( -1.000000000000000000, 0.000000000000000000, 0.000000000000000000 ) ) ;
#35748=DIRECTION ( 'NONE',  ( 0.000000000000000000, 0.000000000000000000, 1.000000000000000000 ) ) ;
#35755=EDGE_CURVE ( 'NONE', #17475, #9246, #5334, .T. ) ;
#35759=CARTESIAN_POINT ( 'NONE',  ( 33.89999999999999858, 20.60000000000000142, 13.86939075806899702 ) ) ;
#35768=ORIENTED_EDGE ( 'NONE', *, *, #69137, .T. ) ;
#35769=AXIS2_PLACEMENT_3D ( 'NONE', #44040, #17519, #66651 ) ;
#35779=DIRECTION ( 'NONE',  ( -1.000000000000000000, 0.000000000000000000, 0.000000000000000000 ) ) ;
#35782=VECTOR ( 'NONE', #42021, 1000.000000000000000 ) ;
#35793=CARTESIAN_POINT ( 'NONE',  ( 39.90000000000000568, 0.000000000000000000, 0.000000000000000000 ) ) ;
#35800=ORIENTED_EDGE ( 'NONE', *, *, #56025, .T. ) ;
#35807=COLOUR_RGB ( '', 0.08235294, 0.09019608, 0.10196078) ;
#35809=PLANE ( 'NONE',  #49033 ) ;
#35815=VECTOR ( 'NONE', #3155, 1000.000000000000000 ) ;
#35826=ORIENTED_EDGE ( 'NONE', *, *, #20850, .T. ) ;
#35828=VECTOR ( 'NONE', #26737, 1000.000000000000000 ) ;
#35832=PLANE ( 'NONE',  #2858 ) ;
#35836=CARTESIAN_POINT ( 'NONE',  ( 40.90000000000000568, 4.286263797015736595E-16, -3.500000000000000000 ) ) ;
#35839=EDGE_LOOP ( 'NONE', ( #57976, #61109, #19246, #23959 ) ) ;
#35857=PLANE ( 'NONE',  #21913 ) ;
#35858=VECTOR ( 'NONE', #145, 1000.000000000000000 ) ;
#35870=AXIS2_PLACEMENT_3D ( 'NONE', #61757, #13316, #6624 ) ;
#35878=LINE ( 'NONE', #9715, #57534 ) ;
#35883=VECTOR ( 'NONE', #259, 1000.000000000000114 ) ;
#35901=LINE ( 'NONE', #52159, #16107 ) ;
#35908=LINE ( 'NONE', #9384, #56568 ) ;
#35917=FACE_OUTER_BOUND ( 'NONE', #66264, .T. ) ;
#35919=ORIENTED_EDGE ( 'NONE', *, *, #27735, .T. ) ;
#35929=FACE_OUTER_BOUND ( 'NONE', #33114, .T. ) ;
#35932=ORIENTED_EDGE ( 'NONE', *, *, #27444, .F. ) ;
#35935=ADVANCED_FACE ( 'NONE', ( #62085 ), #19312, .T. ) ;
#35938=EDGE_CURVE ( 'NONE', #2849, #43744, #62804, .T. ) ;
#35943=( NAMED_UNIT ( * ) SI_UNIT ( $, .STERADIAN. ) SOLID_ANGLE_UNIT ( ) );
#35949=LINE ( 'NONE', #14389, #68095 ) ;
#35956=DIRECTION ( 'NONE',  ( 0.000000000000000000, 0.000000000000000000, -1.000000000000000000 ) ) ;
#35964=CARTESIAN_POINT ( 'NONE',  ( 49.00000000000000000, 20.60000000000000142, -13.86939075806900057 ) ) ;
#35970=DIRECTION ( 'NONE',  ( -1.000000000000000000, 0.000000000000000000, 0.000000000000000000 ) ) ;
#35990=ORIENTED_EDGE ( 'NONE', *, *, #54459, .T. ) ;
#35993=DIRECTION ( 'NONE',  ( -0.7071067811865474617, 0.000000000000000000, -0.7071067811865474617 ) ) ;
#36003=CARTESIAN_POINT ( 'NONE',  ( 7.900000000000000355, 18.00000000000000355, 21.00000000000000000 ) ) ;
#36013=FACE_OUTER_BOUND ( 'NONE', #20783, .T. ) ;
#36017=ORIENTED_EDGE ( 'NONE', *, *, #12922, .T. ) ;
#36024=EDGE_LOOP ( 'NONE', ( #26088, #63204, #24908, #17883 ) ) ;
#36030=CARTESIAN_POINT ( 'NONE',  ( 31.89999999999999858, -0.000000000000000000, -20.80000000000000071 ) ) ;
#36040=FACE_OUTER_BOUND ( 'NONE', #44605, .T. ) ;
#36046=DIRECTION ( 'NONE',  ( 0.000000000000000000, 0.000000000000000000, -1.000000000000000000 ) ) ;
#36048=CARTESIAN_POINT ( 'NONE',  ( 39.00000000000000000, 0.000000000000000000, 0.000000000000000000 ) ) ;
#36061=CARTESIAN_POINT ( 'NONE',  ( 26.90000000000000213, 0.000000000000000000, -2.285366197183106074 ) ) ;
#36068=AXIS2_PLACEMENT_3D ( 'NONE', #52711, #52344, #42775 ) ;
#36082=ORIENTED_EDGE ( 'NONE', *, *, #22324, .T. ) ;
#36085=AXIS2_PLACEMENT_3D ( 'NONE', #21007, #1189, #5464 ) ;
#36086=CARTESIAN_POINT ( 'NONE',  ( 0.5000000000000000000, 21.00000000000000000, 18.00000000000000355 ) ) ;
#36092=EDGE_LOOP ( 'NONE', ( #14299, #39719, #55620, #59282 ) ) ;
#36093=EDGE_LOOP ( 'NONE', ( #20651, #46238, #65895, #8926 ) ) ;
#36098=ADVANCED_FACE ( 'NONE', ( #20369 ), #33416, .F. ) ;
#36099=CARTESIAN_POINT ( 'NONE',  ( 41.09999999999999432, -21.00000000000000000, 13.86939075806900057 ) ) ;
#36100=VECTOR ( 'NONE', #54286, 1000.000000000000000 ) ;
#36109=DIRECTION ( 'NONE',  ( 0.000000000000000000, 0.000000000000000000, -1.000000000000000000 ) ) ;
#36110=DIRECTION ( 'NONE',  ( 0.000000000000000000, -1.000000000000000000, 0.000000000000000000 ) ) ;
#36138=AXIS2_PLACEMENT_3D ( 'NONE', #34347, #6474, #60197 ) ;
#36165=CARTESIAN_POINT ( 'NONE',  ( 34.89999999999999858, -21.00000000000001421, -13.86939075806900945 ) ) ;
#36169=VERTEX_POINT ( 'NONE', #36997 ) ;
#36172=AXIS2_PLACEMENT_3D ( 'NONE', #6895, #49008, #65938 ) ;
#36179=VECTOR ( 'NONE', #21882, 1000.000000000000000 ) ;
#36197=DIRECTION ( 'NONE',  ( -1.000000000000000000, 0.000000000000000000, 0.000000000000000000 ) ) ;
#36218=CARTESIAN_POINT ( 'NONE',  ( 49.00000000000000000, -0.2000000000089119934, -8.913009219568841313E-12 ) ) ;
#36230=VECTOR ( 'NONE', #68866, 1000.000000000000114 ) ;
#36240=ORIENTED_EDGE ( 'NONE', *, *, #6497, .T. ) ;
#36250=CARTESIAN_POINT ( 'NONE',  ( 37.90000000000000568, -21.00000000000001421, -13.86939075806900945 ) ) ;
#36254=VECTOR ( 'NONE', #16186, 1000.000000000000000 ) ;
#36263=VERTEX_POINT ( 'NONE', #64904 ) ;
#36273=CARTESIAN_POINT ( 'NONE',  ( 49.00000000000000000, 0.000000000000000000, 0.000000000000000000 ) ) ;
#36279=ORIENTED_EDGE ( 'NONE', *, *, #26095, .F. ) ;
#36283=CARTESIAN_POINT ( 'NONE',  ( 27.00000000000000000, 0.000000000000000000, 0.000000000000000000 ) ) ;
#36284=EDGE_CURVE ( 'NONE', #11420, #68516, #33418, .T. ) ;
#36285=DIRECTION ( 'NONE',  ( 0.000000000000000000, 0.000000000000000000, -1.000000000000000000 ) ) ;
#36292=DIRECTION ( 'NONE',  ( 0.000000000000000000, 0.000000000000000000, -1.000000000000000000 ) ) ;
#36293=AXIS2_PLACEMENT_3D ( 'NONE', #17083, #54930, #6485 ) ;
#36322=ADVANCED_FACE ( 'NONE', ( #50012 ), #39743, .F. ) ;
#36328=CLOSED_SHELL ( 'NONE', ( #2052, #32075, #36722, #33468, #16543, #50220, #68748, #11565, #68702, #48077, #17986, #23567 ) ) ;
#36343=DIRECTION ( 'NONE',  ( -1.000000000000000000, 0.000000000000000000, 0.000000000000000000 ) ) ;
#36347=ORIENTED_EDGE ( 'NONE', *, *, #2896, .T. ) ;
#36354=CARTESIAN_POINT ( 'NONE',  ( 16.89999999999999858, -0.1999999999911795112, 8.826273045769999343E-12 ) ) ;
#36357=VERTEX_POINT ( 'NONE', #57062 ) ;
#36358=CARTESIAN_POINT ( 'NONE',  ( 49.00000000000000000, -0.2000000000089119934, -8.913009219568841313E-12 ) ) ;
#36374=VERTEX_POINT ( 'NONE', #61667 ) ;
#36386=( LENGTH_UNIT ( ) NAMED_UNIT ( * ) SI_UNIT ( .MILLI., .METRE. ) );
#36398=SURFACE_STYLE_USAGE ( .BOTH. , #45683 ) ;
#36407=DIRECTION ( 'NONE',  ( 1.000000000000000000, 0.000000000000000000, 0.000000000000000000 ) ) ;
#36454=DIRECTION ( 'NONE',  ( 0.000000000000000000, -0.7071067811865475727, -0.7071067811865475727 ) ) ;
#36455=PRESENTATION_STYLE_ASSIGNMENT (( #56962 ) ) ;
#36456=EDGE_CURVE ( 'NONE', #3551, #45925, #20632, .T. ) ;
#36459=EDGE_LOOP ( 'NONE', ( #31544, #6440, #53322, #8785 ) ) ;
#36460=ADVANCED_FACE ( 'NONE', ( #58122 ), #53189, .F. ) ;
#36461=CARTESIAN_POINT ( 'NONE',  ( 49.00000000000000000, 20.60000000000000142, -13.86939075806900057 ) ) ;
#36466=ADVANCED_FACE ( 'NONE', ( #47513 ), #4039, .T. ) ;
#36467=PLANE ( 'NONE',  #35065 ) ;
#36473=ORIENTED_EDGE ( 'NONE', *, *, #42717, .F. ) ;
#36479=ORIENTED_EDGE ( 'NONE', *, *, #24624, .T. ) ;
#36486=VECTOR ( 'NONE', #1801, 1000.000000000000000 ) ;
#36508=CARTESIAN_POINT ( 'NONE',  ( 8.900000000000005684, 20.60000000000000142, -13.86939075806900057 ) ) ;
#36510=FACE_BOUND ( 'NONE', #61269, .T. ) ;
#36521=EDGE_CURVE ( 'NONE', #10593, #2943, #58308, .T. ) ;
#36528=ORIENTED_EDGE ( 'NONE', *, *, #25253, .F. ) ;
#36541=CARTESIAN_POINT ( 'NONE',  ( 41.09999999999999432, -14.06939075806901940, -20.80000000000000426 ) ) ;
#36542=EDGE_CURVE ( 'NONE', #56320, #3551, #4398, .T. ) ;
#36547=MECHANICAL_DESIGN_GEOMETRIC_PRESENTATION_REPRESENTATION('',(#64768),#38802);
#36556=FACE_OUTER_BOUND ( 'NONE', #6785, .T. ) ;
#36560=ADVANCED_FACE ( 'NONE', ( #64483 ), #15695, .F. ) ;
#36565=PLANE ( 'NONE',  #58206 ) ;
#36567=ORIENTED_EDGE ( 'NONE', *, *, #18323, .T. ) ;
#36568=PLANE ( 'NONE',  #8980 ) ;
#36570=CARTESIAN_POINT ( 'NONE',  ( 37.90000000000000568, 0.000000000000000000, 0.000000000000000000 ) ) ;
#36574=ORIENTED_EDGE ( 'NONE', *, *, #36756, .F. ) ;
#36587=EDGE_CURVE ( 'NONE', #47575, #20267, #41509, .T. ) ;
#36598=VERTEX_POINT ( 'NONE', #5081 ) ;
#36612=ORIENTED_EDGE ( 'NONE', *, *, #51938, .F. ) ;
#36617=UNCERTAINTY_MEASURE_WITH_UNIT (LENGTH_MEASURE( 1.000000000000000082E-05 ), #51449, 'distance_accuracy_value', 'NONE');
#36621=CARTESIAN_POINT ( 'NONE',  ( 49.00000000000000000, -0.2000000000089119934, -8.913009219568841313E-12 ) ) ;
#36626=ORIENTED_EDGE ( 'NONE', *, *, #55740, .F. ) ;
#36630=CARTESIAN_POINT ( 'NONE',  ( 0.5000000000000000000, -21.00000000000000000, 18.00000000000000355 ) ) ;
#36632=CIRCLE ( 'NONE', #44541, 24.99999999998789946 ) ;
#36635=CARTESIAN_POINT ( 'NONE',  ( 23.90000000000000213, -0.2000000000089119934, -8.913009219568841313E-12 ) ) ;
#36636=DIRECTION ( 'NONE',  ( 0.000000000000000000, 0.000000000000000000, -1.000000000000000000 ) ) ;
#36661=DIRECTION ( 'NONE',  ( 1.000000000000000000, -0.000000000000000000, 0.000000000000000000 ) ) ;
#36662=ORIENTED_EDGE ( 'NONE', *, *, #61252, .T. ) ;
#36684=AXIS2_PLACEMENT_3D ( 'NONE', #24305, #6653, #39512 ) ;
#36687=EDGE_LOOP ( 'NONE', ( #9586, #28081, #58700, #8331, #66638, #50958, #7765, #4 ) ) ;
#36689=FACE_OUTER_BOUND ( 'NONE', #11808, .T. ) ;
#36706=ORIENTED_EDGE ( 'NONE', *, *, #57389, .F. ) ;
#36715=DIRECTION ( 'NONE',  ( 1.000000000000000000, 0.000000000000000000, 0.000000000000000000 ) ) ;
#36719=COLOUR_RGB ( '', 0.09019608, 0.27058824, 0.51372549) ;
#36720=DIRECTION ( 'NONE',  ( -1.000000000000000000, 0.000000000000000000, 0.000000000000000000 ) ) ;
#36722=ADVANCED_FACE ( 'NONE', ( #44614 ), #17073, .F. ) ;
#36727=EDGE_CURVE ( 'NONE', #42288, #60085, #28366, .T. ) ;
#36730=LINE ( 'NONE', #52289, #23898 ) ;
#36735=CARTESIAN_POINT ( 'NONE',  ( 25.57999999999999829, 3.010794155703768650E-16, -2.458500000000000796 ) ) ;
#36744=ORIENTED_EDGE ( 'NONE', *, *, #20276, .T. ) ;
#36756=EDGE_CURVE ( 'NONE', #49922, #32098, #34346, .T. ) ;
#36764=CARTESIAN_POINT ( 'NONE',  ( 40.90000000000000568, -21.00000000000000000, 13.86939075806900057 ) ) ;
#36781=CARTESIAN_POINT ( 'NONE',  ( 7.900000000000000355, -21.00000000000000000, -18.00000000000000355 ) ) ;
#36786=EDGE_CURVE ( 'NONE', #53128, #40022, #29404, .T. ) ;
#36797=LINE ( 'NONE', #15226, #10652 ) ;
#36798=ORIENTED_EDGE ( 'NONE', *, *, #6122, .T. ) ;
#36804=CARTESIAN_POINT ( 'NONE',  ( 17.89999999999999858, -21.00000000000000000, 13.86939075806900057 ) ) ;
#36810=AXIS2_PLACEMENT_3D ( 'NONE', #36283, #53606, #26378 ) ;
#36822=FACE_OUTER_BOUND ( 'NONE', #40051, .T. ) ;
#36832=EDGE_CURVE ( 'NONE', #55425, #47809, #51324, .T. ) ;
#36852=LINE ( 'NONE', #20567, #30891 ) ;
#36853=DIRECTION ( 'NONE',  ( -1.000000000000000000, 0.000000000000000000, 0.000000000000000000 ) ) ;
#36859=AXIS2_PLACEMENT_3D ( 'NONE', #34450, #47103, #52407 ) ;
#36870=CARTESIAN_POINT ( 'NONE',  ( 15.90000000000000036, -0.000000000000000000, 20.80000000000000426 ) ) ;
#36873=ORIENTED_EDGE ( 'NONE', *, *, #40367, .T. ) ;
#36875=FACE_OUTER_BOUND ( 'NONE', #52644, .T. ) ;
#36902=VERTEX_POINT ( 'NONE', #35759 ) ;
#36908=ORIENTED_EDGE ( 'NONE', *, *, #16369, .T. ) ;
#36914=AXIS2_PLACEMENT_3D ( 'NONE', #3385, #46160, #67732 ) ;
#36918=ORIENTED_EDGE ( 'NONE', *, *, #64918, .T. ) ;
#36922=AXIS2_PLACEMENT_3D ( 'NONE', #55060, #59306, #54359 ) ;
#36925=CARTESIAN_POINT ( 'NONE',  ( 7.900000000000000355, -0.2000000000000000111, 0.000000000000000000 ) ) ;
#36928=EDGE_CURVE ( 'NONE', #1307, #5466, #19496, .T. ) ;
#36943=VERTEX_POINT ( 'NONE', #19848 ) ;
#36947=CARTESIAN_POINT ( 'NONE',  ( 46.39999999999999858, 21.00000000000000000, -1.750000000000000222 ) ) ;
#36949=ORIENTED_EDGE ( 'NONE', *, *, #69768, .T. ) ;
#36963=PLANE ( 'NONE',  #60937 ) ;
#36979=CARTESIAN_POINT ( 'NONE',  ( 39.00000000000000000, 0.000000000000000000, 0.000000000000000000 ) ) ;
#36982=ORIENTED_EDGE ( 'NONE', *, *, #37142, .T. ) ;
#36989=LINE ( 'NONE', #3745, #61541 ) ;
#36990=EDGE_LOOP ( 'NONE', ( #45379, #68884, #22717, #18177 ) ) ;
#36995=VERTEX_POINT ( 'NONE', #3949 ) ;
#36997=CARTESIAN_POINT ( 'NONE',  ( 18.89999999999999858, -14.06939075806902117, -20.80000000000000426 ) ) ;
#37006=ORIENTED_EDGE ( 'NONE', *, *, #16000, .T. ) ;
#37010=FILL_AREA_STYLE ('',( #63867 ) ) ;
#37015=CIRCLE ( 'NONE', #6522, 24.99999999998789946 ) ;
#37027=VERTEX_POINT ( 'NONE', #10299 ) ;
#37028=FACE_OUTER_BOUND ( 'NONE', #36990, .T. ) ;
#37029=FACE_BOUND ( 'NONE', #53006, .T. ) ;
#37034=DIRECTION ( 'NONE',  ( -1.000000000000000000, 0.000000000000000000, 0.000000000000000000 ) ) ;
#37038=DIRECTION ( 'NONE',  ( 0.000000000000000000, 0.000000000000000000, 1.000000000000000000 ) ) ;
#37046=DIRECTION ( 'NONE',  ( 0.000000000000000000, 0.000000000000000000, -1.000000000000000000 ) ) ;
#37055=DIRECTION ( 'NONE',  ( -1.000000000000000000, 0.000000000000000000, 0.000000000000000000 ) ) ;
#37056=CARTESIAN_POINT ( 'NONE',  ( 49.00000000000000000, -0.2000000000089119934, 8.909539772616881237E-12 ) ) ;
#37060=AXIS2_PLACEMENT_3D ( 'NONE', #22619, #28597, #28952 ) ;
#37089=DIRECTION ( 'NONE',  ( 0.000000000000000000, 0.000000000000000000, -1.000000000000000000 ) ) ;
#37090=ORIENTED_EDGE ( 'NONE', *, *, #61191, .T. ) ;
#37097=CARTESIAN_POINT ( 'NONE',  ( 41.09999999999999432, -14.06939075806900163, 20.80000000000000426 ) ) ;
#37101=DIRECTION ( 'NONE',  ( 0.000000000000000000, -1.000000000000000000, 0.000000000000000000 ) ) ;
#37113=LINE ( 'NONE', #20483, #8347 ) ;
#37121=AXIS2_PLACEMENT_3D ( 'NONE', #33348, #54934, #56299 ) ;
#37140=DIRECTION ( 'NONE',  ( 0.000000000000000000, 0.000000000000000000, -1.000000000000000000 ) ) ;
#37142=EDGE_CURVE ( 'NONE', #47575, #31468, #27860, .T. ) ;
#37153=DIRECTION ( 'NONE',  ( 0.000000000000000000, 0.000000000000000000, -1.000000000000000000 ) ) ;
#37162=EDGE_CURVE ( 'NONE', #64619, #8221, #14341, .T. ) ;
#37163=ORIENTED_EDGE ( 'NONE', *, *, #52228, .F. ) ;
#37164=EDGE_CURVE ( 'NONE', #43746, #33525, #18979, .T. ) ;
#37176=DIRECTION ( 'NONE',  ( 1.000000000000000000, -0.000000000000000000, 0.000000000000000000 ) ) ;
#37198=FACE_OUTER_BOUND ( 'NONE', #47246, .T. ) ;
#37199=ORIENTED_EDGE ( 'NONE', *, *, #46151, .F. ) ;
#37202=CARTESIAN_POINT ( 'NONE',  ( 11.90000000000000036, -14.06939075806900874, 20.80000000000001137 ) ) ;
#37212=AXIS2_PLACEMENT_3D ( 'NONE', #6791, #28365, #42219 ) ;
#37218=ORIENTED_EDGE ( 'NONE', *, *, #39286, .T. ) ;
#37227=CARTESIAN_POINT ( 'NONE',  ( 39.90000000000000568, 0.000000000000000000, 0.000000000000000000 ) ) ;
#37229=ORIENTED_EDGE ( 'NONE', *, *, #20268, .T. ) ;
#37242=ORIENTED_EDGE ( 'NONE', *, *, #67945, .F. ) ;
#37246=CARTESIAN_POINT ( 'NONE',  ( 21.90000000000000213, 20.60000000000000142, -13.86939075806900057 ) ) ;
#37248=EDGE_CURVE ( 'NONE', #24345, #6900, #49852, .T. ) ;
#37263=CARTESIAN_POINT ( 'NONE',  ( 13.90000000000000036, -0.000000000000000000, 20.80000000000000426 ) ) ;
#37270=ADVANCED_FACE ( 'NONE', ( #63163 ), #40887, .F. ) ;
#37273=SURFACE_STYLE_FILL_AREA ( #52481 ) ;
#37274=EDGE_CURVE ( 'NONE', #19077, #62836, #57155, .T. ) ;
#37278=CARTESIAN_POINT ( 'NONE',  ( 36.90000000000000568, -0.1999999999911430404, -8.864436962241481021E-12 ) ) ;
#37279=EDGE_LOOP ( 'NONE', ( #41979, #25406, #29386, #39616 ) ) ;
#37281=( NAMED_UNIT ( * ) PLANE_ANGLE_UNIT ( ) SI_UNIT ( $, .RADIAN. ) );
#37308=EDGE_CURVE ( 'NONE', #17145, #67710, #38126, .T. ) ;
#37310=ORIENTED_EDGE ( 'NONE', *, *, #59524, .T. ) ;
#37314=EDGE_CURVE ( 'NONE', #44206, #37330, #69170, .T. ) ;
#37320=CARTESIAN_POINT ( 'NONE',  ( 0.000000000000000000, -20.50000000000002487, -17.79289321881347163 ) ) ;
#37324=VECTOR ( 'NONE', #57599, 1000.000000000000000 ) ;
#37327=ORIENTED_EDGE ( 'NONE', *, *, #42837, .F. ) ;
#37330=VERTEX_POINT ( 'NONE', #16477 ) ;
#37332=UNCERTAINTY_MEASURE_WITH_UNIT (LENGTH_MEASURE( 1.000000000000000082E-05 ), #67173, 'distance_accuracy_value', 'NONE');
#37338=DIRECTION ( 'NONE',  ( 1.000000000000000000, 0.000000000000000000, 0.000000000000000000 ) ) ;
#37344=EDGE_CURVE ( 'NONE', #11005, #48516, #30988, .T. ) ;
#37362=VECTOR ( 'NONE', #67709, 1000.000000000000000 ) ;
#37366=CARTESIAN_POINT ( 'NONE',  ( 41.09999999999999432, -21.00000000000000000, -13.86939075806900057 ) ) ;
#37367=CIRCLE ( 'NONE', #46381, 24.99999999998784972 ) ;
#37376=DIRECTION ( 'NONE',  ( 0.000000000000000000, 0.000000000000000000, 1.000000000000000000 ) ) ;
#37380=AXIS2_PLACEMENT_3D ( 'NONE', #42710, #37761, #31425 ) ;
#37382=ORIENTED_EDGE ( 'NONE', *, *, #17282, .F. ) ;
#37389=DIRECTION ( 'NONE',  ( -1.000000000000000000, 0.000000000000000000, 0.000000000000000000 ) ) ;
#37393=DIRECTION ( 'NONE',  ( -1.000000000000000000, 0.000000000000000000, 0.000000000000000000 ) ) ;
#37404=LINE ( 'NONE', #31044, #24321 ) ;
#37417=AXIS2_PLACEMENT_3D ( 'NONE', #45224, #51235, #57246 ) ;
#37430=AXIS2_PLACEMENT_3D ( 'NONE', #36621, #26725, #41928 ) ;
#37443=VECTOR ( 'NONE', #52473, 1000.000000000000000 ) ;
#37444=( NAMED_UNIT ( * ) PLANE_ANGLE_UNIT ( ) SI_UNIT ( $, .RADIAN. ) );
#37453=DIRECTION ( 'NONE',  ( -1.000000000000000000, 0.000000000000000000, 0.000000000000000000 ) ) ;
#37460=CLOSED_SHELL ( 'NONE', ( #11585, #30836, #44700, #60281, #55413, #25649 ) ) ;
#37464=PLANE ( 'NONE',  #50799 ) ;
#37467=ORIENTED_EDGE ( 'NONE', *, *, #38294, .F. ) ;
#37470=ORIENTED_EDGE ( 'NONE', *, *, #31819, .T. ) ;
#37482=CARTESIAN_POINT ( 'NONE',  ( 10.00000000000000000, 18.00000000000000355, -21.00000000000000000 ) ) ;
#37483=DIRECTION ( 'NONE',  ( 1.000000000000000000, -0.000000000000000000, 0.000000000000000000 ) ) ;
#37484=AXIS2_PLACEMENT_3D ( 'NONE', #7909, #34421, #56015 ) ;
#37491=VERTEX_POINT ( 'NONE', #22126 ) ;
#37505=VECTOR ( 'NONE', #14342, 1000.000000000000000 ) ;
#37508=DIRECTION ( 'NONE',  ( -1.000000000000000000, 0.000000000000000000, 0.000000000000000000 ) ) ;
#37516=CARTESIAN_POINT ( 'NONE',  ( 39.00000000000000000, 0.000000000000000000, 0.000000000000000000 ) ) ;
#37530=EDGE_CURVE ( 'NONE', #29693, #63246, #12534, .T. ) ;
#37551=AXIS2_PLACEMENT_3D ( 'NONE', #42086, #69311, #52008 ) ;
#37558=CARTESIAN_POINT ( 'NONE',  ( 32.89999999999999858, -14.06939075806900874, 20.80000000000001137 ) ) ;
#37571=ADVANCED_FACE ( 'NONE', ( #23506 ), #66635, .F. ) ;
#37580=ORIENTED_EDGE ( 'NONE', *, *, #2025, .T. ) ;
#37583=AXIS2_PLACEMENT_3D ( 'NONE', #33162, #32817, #21180 ) ;
#37590=ORIENTED_EDGE ( 'NONE', *, *, #3698, .F. ) ;
#37592=CARTESIAN_POINT ( 'NONE',  ( 26.90000000000000213, 0.000000000000000000, 0.000000000000000000 ) ) ;
#37596=VECTOR ( 'NONE', #29868, 1000.000000000000000 ) ;
#37613=FACE_OUTER_BOUND ( 'NONE', #46864, .T. ) ;
#37620=PLANE ( 'NONE',  #5245 ) ;
#37626=DIRECTION ( 'NONE',  ( 0.000000000000000000, 0.000000000000000000, -1.000000000000000000 ) ) ;
#37632=VECTOR ( 'NONE', #1735, 1000.000000000000000 ) ;
#37641=PLANE ( 'NONE',  #6352 ) ;
#37643=LINE ( 'NONE', #59203, #10604 ) ;
#37645=VECTOR ( 'NONE', #54894, 1000.000000000000000 ) ;
#37652=EDGE_LOOP ( 'NONE', ( #26021, #54008 ) ) ;
#37658=ORIENTED_EDGE ( 'NONE', *, *, #13586, .T. ) ;
#37667=ORIENTED_EDGE ( 'NONE', *, *, #59381, .T. ) ;
#37680=CARTESIAN_POINT ( 'NONE',  ( 41.09999999999999432, 20.60000000000000142, -13.86939075806900057 ) ) ;
#37689=DIRECTION ( 'NONE',  ( 0.000000000000000000, 0.000000000000000000, -1.000000000000000000 ) ) ;
#37692=CARTESIAN_POINT ( 'NONE',  ( -6.661338147750939243E-15, 17.79289321881346808, 20.50000000000000000 ) ) ;
#37718=LINE ( 'NONE', #11178, #40031 ) ;
#37721=DIRECTION ( 'NONE',  ( -1.000000000000000000, 0.000000000000000000, 0.000000000000000000 ) ) ;
#37725=VERTEX_POINT ( 'NONE', #20642 ) ;
#37738=CARTESIAN_POINT ( 'NONE',  ( 39.00000000000000000, 0.000000000000000000, 0.000000000000000000 ) ) ;
#37742=VERTEX_POINT ( 'NONE', #31965 ) ;
#37746=FACE_OUTER_BOUND ( 'NONE', #63298, .T. ) ;
#37748=CARTESIAN_POINT ( 'NONE',  ( 41.09999999999999432, -0.2000000000000000111, 0.000000000000000000 ) ) ;
#37757=ORIENTED_EDGE ( 'NONE', *, *, #682, .F. ) ;
#37761=DIRECTION ( 'NONE',  ( 1.000000000000000000, -0.000000000000000000, 0.000000000000000000 ) ) ;
#37768=PLANE ( 'NONE',  #24734 ) ;
#37775=PRESENTATION_STYLE_ASSIGNMENT (( #53005 ) ) ;
#37778=VECTOR ( 'NONE', #32178, 1000.000000000000000 ) ;
#37788=CARTESIAN_POINT ( 'NONE',  ( 7.900000000000000355, 14.08845687959340331, 21.00000000000000000 ) ) ;
#37790=DIRECTION ( 'NONE',  ( 0.000000000000000000, 0.000000000000000000, -1.000000000000000000 ) ) ;
#37807=DIRECTION ( 'NONE',  ( 0.000000000000000000, 0.000000000000000000, 1.000000000000000000 ) ) ;
#37816=VECTOR ( 'NONE', #53234, 1000.000000000000000 ) ;
#37826=DIRECTION ( 'NONE',  ( 0.000000000000000000, 0.000000000000000000, -1.000000000000000000 ) ) ;
#37849=CIRCLE ( 'NONE', #38946, 5.000000000000000000 ) ;
#37852=DIRECTION ( 'NONE',  ( 0.000000000000000000, 0.000000000000000000, 1.000000000000000000 ) ) ;
#37863=LINE ( 'NONE', #20895, #4136 ) ;
#37900=ORIENTED_EDGE ( 'NONE', *, *, #420, .F. ) ;
#37905=LINE ( 'NONE', #21638, #35511 ) ;
#37910=CARTESIAN_POINT ( 'NONE',  ( 8.900000000000005684, -21.00000000000000000, -18.00000000000000355 ) ) ;
#37913=AXIS2_PLACEMENT_3D ( 'NONE', #10447, #32375, #22105 ) ;
#37925=ORIENTED_EDGE ( 'NONE', *, *, #57890, .F. ) ;
#37926=DIRECTION ( 'NONE',  ( 0.5001543609659999667, 0.000000000000000000, -0.8659362650950080953 ) ) ;
#37933=PLANE ( 'NONE',  #16207 ) ;
#37946=CARTESIAN_POINT ( 'NONE',  ( 24.90000000000000213, 0.000000000000000000, 1.723948796001796511E-15 ) ) ;
#37949=ADVANCED_FACE ( 'NONE', ( #12446 ), #11762, .T. ) ;
#37959=CARTESIAN_POINT ( 'NONE',  ( 41.09999999999999432, -0.2000000000000000111, 0.000000000000000000 ) ) ;
#37960=VECTOR ( 'NONE', #10072, 1000.000000000000000 ) ;
#37974=VECTOR ( 'NONE', #69582, 1000.000000000000000 ) ;
#37975=PLANE ( 'NONE',  #51745 ) ;
#37978=DIRECTION ( 'NONE',  ( 0.000000000000000000, 0.000000000000000000, -1.000000000000000000 ) ) ;
#37981=EDGE_CURVE ( 'NONE', #32607, #37742, #34020, .T. ) ;
#37990=DIRECTION ( 'NONE',  ( 1.000000000000000000, -0.000000000000000000, 0.000000000000000000 ) ) ;
#38004=DIRECTION ( 'NONE',  ( 0.000000000000000000, 0.000000000000000000, 1.000000000000000000 ) ) ;
#38016=AXIS2_PLACEMENT_3D ( 'NONE', #7769, #18028, #2469 ) ;
#38023=VECTOR ( 'NONE', #2192, 1000.000000000000000 ) ;
#38032=UNCERTAINTY_MEASURE_WITH_UNIT (LENGTH_MEASURE( 1.000000000000000082E-05 ), #51157, 'distance_accuracy_value', 'NONE');
#38039=DIRECTION ( 'NONE',  ( 0.000000000000000000, 0.000000000000000000, -1.000000000000000000 ) ) ;
#38051=CARTESIAN_POINT ( 'NONE',  ( 39.00000000000000000, -21.00000000000000000, 16.96999999999999886 ) ) ;
#38053=ORIENTED_EDGE ( 'NONE', *, *, #33509, .F. ) ;
#38072=AXIS2_PLACEMENT_3D ( 'NONE', #32214, #38560, #22304 ) ;
#38079=DIRECTION ( 'NONE',  ( -1.000000000000000000, 0.000000000000000000, 0.000000000000000000 ) ) ;
#38104=DIRECTION ( 'NONE',  ( 1.000000000000000000, -0.000000000000000000, 0.000000000000000000 ) ) ;
#38117=CARTESIAN_POINT ( 'NONE',  ( 40.90000000000000568, 0.000000000000000000, 5.250000000000000000 ) ) ;
#38121=VECTOR ( 'NONE', #38710, 1000.000000000000000 ) ;
#38126=CIRCLE ( 'NONE', #39206, 24.99999999998789946 ) ;
#38138=CARTESIAN_POINT ( 'NONE',  ( 37.90000000000000568, 13.66939075806899240, -20.79999999999999361 ) ) ;
#38146=CARTESIAN_POINT ( 'NONE',  ( 30.90000000000000213, -0.2000000000089119934, -8.913009219568841313E-12 ) ) ;
#38150=( NAMED_UNIT ( * ) SI_UNIT ( $, .STERADIAN. ) SOLID_ANGLE_UNIT ( ) );
#38155=CYLINDRICAL_SURFACE ( 'NONE', #54450, 24.99999999998789946 ) ;
#38162=CARTESIAN_POINT ( 'NONE',  ( 41.09999999999999432, 20.60000000000000142, -13.86939075806900057 ) ) ;
#38164=VECTOR ( 'NONE', #64426, 1000.000000000000000 ) ;
#38177=FACE_OUTER_BOUND ( 'NONE', #50781, .T. ) ;
#38200=EDGE_CURVE ( 'NONE', #13993, #36263, #12191, .T. ) ;
#38204=LINE ( 'NONE', #23301, #6562 ) ;
#38205=EDGE_CURVE ( 'NONE', #12098, #57808, #38204, .T. ) ;
#38215=ORIENTED_EDGE ( 'NONE', *, *, #29215, .T. ) ;
#38228=LINE ( 'NONE', #50194, #9085 ) ;
#38233=EDGE_LOOP ( 'NONE', ( #38262, #3000 ) ) ;
#38245=CARTESIAN_POINT ( 'NONE',  ( 49.00000000000000000, -0.2000000000089119934, -8.913009219568841313E-12 ) ) ;
#38253=PLANE ( 'NONE',  #33600 ) ;
#38258=ORIENTED_EDGE ( 'NONE', *, *, #52744, .F. ) ;
#38262=ORIENTED_EDGE ( 'NONE', *, *, #58516, .T. ) ;
#38290=CARTESIAN_POINT ( 'NONE',  ( 18.89999999999999858, 13.66939075806899240, 20.79999999999999361 ) ) ;
#38294=EDGE_CURVE ( 'NONE', #49868, #11985, #34598, .T. ) ;
#38301=VERTEX_POINT ( 'NONE', #36003 ) ;
#38312=CARTESIAN_POINT ( 'NONE',  ( 26.90000000000000213, 13.66939075806899240, 20.79999999999999361 ) ) ;
#38319=ORIENTED_EDGE ( 'NONE', *, *, #6413, .F. ) ;
#38327=DIRECTION ( 'NONE',  ( 1.000000000000000000, -0.000000000000000000, -0.000000000000000000 ) ) ;
#38343=CARTESIAN_POINT ( 'NONE',  ( 41.09999999999999432, -14.06939075806900163, 20.80000000000000426 ) ) ;
#38348=ORIENTED_EDGE ( 'NONE', *, *, #44426, .T. ) ;
#38351=ORIENTED_EDGE ( 'NONE', *, *, #26, .T. ) ;
#38353=CYLINDRICAL_SURFACE ( 'NONE', #49012, 24.99999999998789946 ) ;
#38355=VECTOR ( 'NONE', #32534, 1000.000000000000000 ) ;
#38384=CARTESIAN_POINT ( 'NONE',  ( 41.09999999999999432, 20.60000000000000142, 13.86939075806900057 ) ) ;
#38406=DIRECTION ( 'NONE',  ( -1.000000000000000000, 0.000000000000000000, 0.000000000000000000 ) ) ;
#38411=VECTOR ( 'NONE', #32506, 1000.000000000000000 ) ;
#38424=CIRCLE ( 'NONE', #23, 24.99999999998794920 ) ;
#38425=AXIS2_PLACEMENT_3D ( 'NONE', #48281, #57475, #9038 ) ;
#38440=CIRCLE ( 'NONE', #26030, 2.285366197183106074 ) ;
#38443=ORIENTED_EDGE ( 'NONE', *, *, #51742, .T. ) ;
#38447=ORIENTED_EDGE ( 'NONE', *, *, #34637, .T. ) ;
#38448=ORIENTED_EDGE ( 'NONE', *, *, #46201, .F. ) ;
#38451=CARTESIAN_POINT ( 'NONE',  ( 39.90000000000000568, -16.96999999999999886, -21.00000000000000000 ) ) ;
#38453=AXIS2_PLACEMENT_3D ( 'NONE', #22292, #13032, #56190 ) ;
#38458=AXIS2_PLACEMENT_3D ( 'NONE', #34461, #24583, #46484 ) ;
#38469=DIRECTION ( 'NONE',  ( 0.000000000000000000, -1.000000000000000000, 0.000000000000000000 ) ) ;
#38472=VERTEX_POINT ( 'NONE', #62183 ) ;
#38483=CARTESIAN_POINT ( 'NONE',  ( 21.90000000000000213, -21.00000000000000000, 13.86939075806900057 ) ) ;
#38484=EDGE_CURVE ( 'NONE', #48107, #60085, #33656, .T. ) ;
#38488=PLANE ( 'NONE',  #28503 ) ;
#38491=ORIENTED_EDGE ( 'NONE', *, *, #22569, .F. ) ;
#38498=DIRECTION ( 'NONE',  ( 0.000000000000000000, 0.000000000000000000, -1.000000000000000000 ) ) ;
#38503=VECTOR ( 'NONE', #56274, 1000.000000000000000 ) ;
#38504=ORIENTED_EDGE ( 'NONE', *, *, #50653, .T. ) ;
#38507=EDGE_LOOP ( 'NONE', ( #12987, #15137, #37580, #63400 ) ) ;
#38511=EDGE_CURVE ( 'NONE', #1369, #2916, #22474, .T. ) ;
#38517=FACE_OUTER_BOUND ( 'NONE', #14455, .T. ) ;
#38524=ORIENTED_EDGE ( 'NONE', *, *, #45682, .T. ) ;
#38533=ORIENTED_EDGE ( 'NONE', *, *, #56616, .F. ) ;
#38534=CARTESIAN_POINT ( 'NONE',  ( 33.89999999999999858, -21.00000000000001421, -13.86939075806900945 ) ) ;
#38539=ORIENTED_EDGE ( 'NONE', *, *, #46969, .T. ) ;
#38544=EDGE_LOOP ( 'NONE', ( #22878, #14216 ) ) ;
#38554=VERTEX_POINT ( 'NONE', #21417 ) ;
#38560=DIRECTION ( 'NONE',  ( 1.000000000000000000, -0.000000000000000000, 0.000000000000000000 ) ) ;
#38567=CARTESIAN_POINT ( 'NONE',  ( 39.90000000000000568, 21.00000000000000000, 16.96999999999999886 ) ) ;
#38587=DIRECTION ( 'NONE',  ( 1.000000000000000000, -0.000000000000000000, 0.000000000000000000 ) ) ;
#38593=FACE_OUTER_BOUND ( 'NONE', #19042, .T. ) ;
#38595=CARTESIAN_POINT ( 'NONE',  ( 40.90000000000000568, 0.000000000000000000, 3.447897592003593022E-15 ) ) ;
#38613=ORIENTED_EDGE ( 'NONE', *, *, #66491, .T. ) ;
#38615=CIRCLE ( 'NONE', #66854, 24.99999999998784972 ) ;
#38616=CLOSED_SHELL ( 'NONE', ( #9412, #36322, #22863, #25965, #59949, #11522 ) ) ;
#38618=DIRECTION ( 'NONE',  ( 0.000000000000000000, 1.000000000000000000, 0.000000000000000000 ) ) ;
#38637=VERTEX_POINT ( 'NONE', #5515 ) ;
#38642=VECTOR ( 'NONE', #8738, 1000.000000000000000 ) ;
#38643=CARTESIAN_POINT ( 'NONE',  ( 49.00000000000000000, 13.66939075806899950, 20.80000000000000426 ) ) ;
#38644=PLANE ( 'NONE',  #14697 ) ;
#38648=( LENGTH_UNIT ( ) NAMED_UNIT ( * ) SI_UNIT ( .MILLI., .METRE. ) );
#38659=EDGE_LOOP ( 'NONE', ( #44107, #3167, #8503, #56083 ) ) ;
#38661=EDGE_CURVE ( 'NONE', #31121, #19077, #17900, .T. ) ;
#38671=LINE ( 'NONE', #65877, #16125 ) ;
#38686=ORIENTED_EDGE ( 'NONE', *, *, #29215, .F. ) ;
#38690=VECTOR ( 'NONE', #54655, 1000.000000000000000 ) ;
#38693=EDGE_LOOP ( 'NONE', ( #50837, #2437, #9571, #62857 ) ) ;
#38710=DIRECTION ( 'NONE',  ( -1.000000000000000000, 0.000000000000000000, 0.000000000000000000 ) ) ;
#38715=EDGE_CURVE ( 'NONE', #63302, #14096, #39067, .T. ) ;
#38718=DIRECTION ( 'NONE',  ( 0.000000000000000000, 0.000000000000000000, -1.000000000000000000 ) ) ;
#38723=CYLINDRICAL_SURFACE ( 'NONE', #17223, 24.99999999998789946 ) ;
#38724=LINE ( 'NONE', #21779, #53977 ) ;
#38751=ORIENTED_EDGE ( 'NONE', *, *, #57305, .T. ) ;
#38755=CARTESIAN_POINT ( 'NONE',  ( 10.00000000000000000, 21.00000000000000000, 18.00000000000000355 ) ) ;
#38756=CYLINDRICAL_SURFACE ( 'NONE', #19859, 24.99999999998794920 ) ;
#38758=CIRCLE ( 'NONE', #61298, 2.458500000000000796 ) ;
#38762=ORIENTED_EDGE ( 'NONE', *, *, #57755, .T. ) ;
#38763=CARTESIAN_POINT ( 'NONE',  ( 24.90000000000000213, -0.2000000000089119934, 8.909539772616881237E-12 ) ) ;
#38765=EDGE_LOOP ( 'NONE', ( #59917, #43037, #25936, #28614 ) ) ;
#38766=CIRCLE ( 'NONE', #17308, 24.99999999998784972 ) ;
#38769=EDGE_LOOP ( 'NONE', ( #16746, #27600, #7136, #58397 ) ) ;
#38770=DIRECTION ( 'NONE',  ( 1.000000000000000000, -0.000000000000000000, 0.000000000000000000 ) ) ;
#38772=DIRECTION ( 'NONE',  ( 0.000000000000000000, 0.000000000000000000, 1.000000000000000000 ) ) ;
#38774=ORIENTED_EDGE ( 'NONE', *, *, #12781, .F. ) ;
#38794=AXIS2_PLACEMENT_3D ( 'NONE', #56933, #30426, #19112 ) ;
#38802=( GEOMETRIC_REPRESENTATION_CONTEXT ( 3 ) GLOBAL_UNCERTAINTY_ASSIGNED_CONTEXT ( ( #46519 ) ) GLOBAL_UNIT_ASSIGNED_CONTEXT ( ( #57798, #52506, #4431 ) ) REPRESENTATION_CONTEXT ( 'NONE', 'WORKASPACE' ) );
#38809=VECTOR ( 'NONE', #65607, 1000.000000000000000 ) ;
#38815=CARTESIAN_POINT ( 'NONE',  ( 25.57999999999999829, 0.000000000000000000, 2.458500000000000796 ) ) ;
#38819=FACE_OUTER_BOUND ( 'NONE', #36459, .T. ) ;
#38821=DIRECTION ( 'NONE',  ( 0.000000000000000000, -1.000000000000000000, 0.000000000000000000 ) ) ;
#38831=DIRECTION ( 'NONE',  ( 1.000000000000000000, -0.000000000000000000, 0.000000000000000000 ) ) ;
#38851=ORIENTED_EDGE ( 'NONE', *, *, #49956, .F. ) ;
#38852=DIRECTION ( 'NONE',  ( 0.000000000000000000, 0.000000000000000000, -1.000000000000000000 ) ) ;
#38869=ORIENTED_EDGE ( 'NONE', *, *, #34474, .F. ) ;
#38890=LINE ( 'NONE', #1079, #32516 ) ;
#38909=VECTOR ( 'NONE', #66490, 1000.000000000000000 ) ;
#38911=VERTEX_POINT ( 'NONE', #3684 ) ;
#38924=CARTESIAN_POINT ( 'NONE',  ( 20.90000000000000213, 13.66939075806899240, -20.79999999999999361 ) ) ;
#38926=VERTEX_POINT ( 'NONE', #21696 ) ;
#38931=CYLINDRICAL_SURFACE ( 'NONE', #25028, 0.5000000000000000000 ) ;
#38940=AXIS2_PLACEMENT_3D ( 'NONE', #47374, #42069, #52701 ) ;
#38944=DIRECTION ( 'NONE',  ( -1.000000000000000000, 0.000000000000000000, 0.000000000000000000 ) ) ;
#38946=AXIS2_PLACEMENT_3D ( 'NONE', #35793, #25904, #67976 ) ;
#38963=ORIENTED_EDGE ( 'NONE', *, *, #2472, .T. ) ;
#38973=ORIENTED_EDGE ( 'NONE', *, *, #7274, .T. ) ;
#38983=DIRECTION ( 'NONE',  ( 0.000000000000000000, 1.000000000000000000, 0.000000000000000000 ) ) ;
#38989=CYLINDRICAL_SURFACE ( 'NONE', #50973, 24.99999999998784972 ) ;
#38991=VECTOR ( 'NONE', #14762, 1000.000000000000000 ) ;
#39011=FACE_OUTER_BOUND ( 'NONE', #10757, .T. ) ;
#39031=FACE_OUTER_BOUND ( 'NONE', #58421, .T. ) ;
#39060=AXIS2_PLACEMENT_3D ( 'NONE', #19701, #20764, #53652 ) ;
#39067=LINE ( 'NONE', #60632, #67580 ) ;
#39071=ORIENTED_EDGE ( 'NONE', *, *, #14840, .F. ) ;
#39075=EDGE_LOOP ( 'NONE', ( #29391, #47447, #36017, #55819 ) ) ;
#39076=DIRECTION ( 'NONE',  ( 1.000000000000000000, -0.000000000000000000, -0.000000000000000000 ) ) ;
#39085=EDGE_CURVE ( 'NONE', #12819, #14861, #42209, .T. ) ;
#39090=ORIENTED_EDGE ( 'NONE', *, *, #63011, .T. ) ;
#39097=CARTESIAN_POINT ( 'NONE',  ( 10.90000000000000036, 20.60000000000000142, 13.86939075806900057 ) ) ;
#39103=AXIS2_PLACEMENT_3D ( 'NONE', #28265, #55832, #45559 ) ;
#39104=DIRECTION ( 'NONE',  ( 1.000000000000000000, -0.000000000000000000, 0.000000000000000000 ) ) ;
#39160=FACE_OUTER_BOUND ( 'NONE', #17623, .T. ) ;
#39167=CARTESIAN_POINT ( 'NONE',  ( 30.90000000000000213, 13.66939075806899950, 20.80000000000000426 ) ) ;
#39176=ORIENTED_EDGE ( 'NONE', *, *, #30675, .T. ) ;
#39178=DIRECTION ( 'NONE',  ( 0.000000000000000000, 0.000000000000000000, -1.000000000000000000 ) ) ;
#39180=PLANE ( 'NONE',  #64660 ) ;
#39190=( NAMED_UNIT ( * ) SI_UNIT ( $, .STERADIAN. ) SOLID_ANGLE_UNIT ( ) );
#39193=CYLINDRICAL_SURFACE ( 'NONE', #59358, 24.99999999998784972 ) ;
#39205=CARTESIAN_POINT ( 'NONE',  ( 41.09999999999999432, 20.60000000000000142, -13.86939075806900057 ) ) ;
#39206=AXIS2_PLACEMENT_3D ( 'NONE', #51150, #14730, #36292 ) ;
#39208=CYLINDRICAL_SURFACE ( 'NONE', #46230, 24.99999999998784972 ) ;
#39227=DIRECTION ( 'NONE',  ( -0.000000000000000000, -1.000000000000000000, 0.000000000000000000 ) ) ;
#39232=CIRCLE ( 'NONE', #44881, 24.99999999998784972 ) ;
#39233=( LENGTH_UNIT ( ) NAMED_UNIT ( * ) SI_UNIT ( .MILLI., .METRE. ) );
#39235=DIRECTION ( 'NONE',  ( 1.000000000000000000, 0.000000000000000000, 0.000000000000000000 ) ) ;
#39236=ORIENTED_EDGE ( 'NONE', *, *, #58315, .T. ) ;
#39241=PLANE ( 'NONE',  #48620 ) ;
#39247=FILL_AREA_STYLE ('',( #17684 ) ) ;
#39261=LINE ( 'NONE', #22996, #9748 ) ;
#39263=SURFACE_SIDE_STYLE ('',( #34285 ) ) ;
#39273=LINE ( 'NONE', #777, #49416 ) ;
#39286=EDGE_CURVE ( 'NONE', #10779, #34850, #30114, .T. ) ;
#39290=CARTESIAN_POINT ( 'NONE',  ( 9.900000000000000355, 14.08845687959340331, -21.00000000000000000 ) ) ;
#39291=VERTEX_POINT ( 'NONE', #8188 ) ;
#39297=EDGE_CURVE ( 'NONE', #48502, #10676, #9258, .T. ) ;
#39303=EDGE_CURVE ( 'NONE', #5931, #12238, #68795, .T. ) ;
#39305=ORIENTED_EDGE ( 'NONE', *, *, #19605, .F. ) ;
#39309=AXIS2_PLACEMENT_3D ( 'NONE', #40854, #28839, #18948 ) ;
#39315=EDGE_CURVE ( 'NONE', #46458, #21641, #28150, .T. ) ;
#39321=CARTESIAN_POINT ( 'NONE',  ( 46.39999999999999858, 33.00000000000000000, 1.250000000000000000 ) ) ;
#39326=FACE_OUTER_BOUND ( 'NONE', #43463, .T. ) ;
#39330=ORIENTED_EDGE ( 'NONE', *, *, #67858, .T. ) ;
#39340=ORIENTED_EDGE ( 'NONE', *, *, #5480, .T. ) ;
#39356=EDGE_CURVE ( 'NONE', #50683, #62375, #47088, .T. ) ;
#39360=ORIENTED_EDGE ( 'NONE', *, *, #69634, .T. ) ;
#39371=ORIENTED_EDGE ( 'NONE', *, *, #8882, .T. ) ;
#39374=ORIENTED_EDGE ( 'NONE', *, *, #42272, .T. ) ;
#39377=CARTESIAN_POINT ( 'NONE',  ( 50.00000000000000711, 0.7500000000000000000, 4.943429983321300902 ) ) ;
#39379=VERTEX_POINT ( 'NONE', #69345 ) ;
#39381=CARTESIAN_POINT ( 'NONE',  ( 49.00000000000000000, -0.1999999999911795112, 8.826273045769999343E-12 ) ) ;
#39384=VERTEX_POINT ( 'NONE', #32579 ) ;
#39397=CARTESIAN_POINT ( 'NONE',  ( 39.90000000000000568, 0.000000000000000000, 0.000000000000000000 ) ) ;
#39417=DIRECTION ( 'NONE',  ( 0.000000000000000000, 0.1500000000000006328, -0.9886859966642592701 ) ) ;
#39418=( NAMED_UNIT ( * ) PLANE_ANGLE_UNIT ( ) SI_UNIT ( $, .RADIAN. ) );
#39435=CARTESIAN_POINT ( 'NONE',  ( 55.00000000000000000, -16.96999999999999886, -21.00000000000000000 ) ) ;
#39469=ORIENTED_EDGE ( 'NONE', *, *, #14879, .T. ) ;
#39470=DIRECTION ( 'NONE',  ( -1.000000000000000000, 0.000000000000000000, 0.000000000000000000 ) ) ;
#39472=ORIENTED_EDGE ( 'NONE', *, *, #19516, .F. ) ;
#39474=ORIENTED_EDGE ( 'NONE', *, *, #4507, .F. ) ;
#39480=CIRCLE ( 'NONE', #67755, 2.458500000000000796 ) ;
#39485=FILL_AREA_STYLE_COLOUR ( '', #55722 ) ;
#39499=DIRECTION ( 'NONE',  ( 1.000000000000000000, -0.000000000000000000, 0.000000000000000000 ) ) ;
#39504=VECTOR ( 'NONE', #29552, 1000.000000000000000 ) ;
#39505=LINE ( 'NONE', #40554, #38642 ) ;
#39512=DIRECTION ( 'NONE',  ( 0.000000000000000000, 0.000000000000000000, -1.000000000000000000 ) ) ;
#39525=FACE_OUTER_BOUND ( 'NONE', #4366, .T. ) ;
#39567=SURFACE_STYLE_FILL_AREA ( #12688 ) ;
#39574=CARTESIAN_POINT ( 'NONE',  ( 41.09999999999999432, -14.06939075806900163, 20.80000000000000426 ) ) ;
#39616=ORIENTED_EDGE ( 'NONE', *, *, #41435, .F. ) ;
#39638=VECTOR ( 'NONE', #58232, 1000.000000000000000 ) ;
#39658=DIRECTION ( 'NONE',  ( 0.000000000000000000, 0.000000000000000000, -1.000000000000000000 ) ) ;
#39670=AXIS2_PLACEMENT_3D ( 'NONE', #3059, #67413, #24967 ) ;
#39680=ORIENTED_EDGE ( 'NONE', *, *, #13982, .T. ) ;
#39684=EDGE_CURVE ( 'NONE', #38554, #62211, #42845, .T. ) ;
#39685=COLOUR_RGB ( '', 0.09019608, 0.27058824, 0.51372549) ;
#39687=ORIENTED_EDGE ( 'NONE', *, *, #44528, .F. ) ;
#39703=ORIENTED_EDGE ( 'NONE', *, *, #25150, .F. ) ;
#39704=EDGE_CURVE ( 'NONE', #21321, #34472, #25086, .T. ) ;
#39712=ORIENTED_EDGE ( 'NONE', *, *, #37314, .F. ) ;
#39713=ORIENTED_EDGE ( 'NONE', *, *, #32111, .T. ) ;
#39718=VERTEX_POINT ( 'NONE', #56891 ) ;
#39719=ORIENTED_EDGE ( 'NONE', *, *, #32689, .T. ) ;
#39725=ORIENTED_EDGE ( 'NONE', *, *, #11211, .T. ) ;
#39726=ADVANCED_FACE ( 'NONE', ( #62543 ), #18719, .T. ) ;
#39728=LINE ( 'NONE', #34072, #31666 ) ;
#39734=FACE_OUTER_BOUND ( 'NONE', #68544, .T. ) ;
#39735=FACE_OUTER_BOUND ( 'NONE', #45763, .T. ) ;
#39742=AXIS2_PLACEMENT_3D ( 'NONE', #58536, #5127, #42605 ) ;
#39743=CYLINDRICAL_SURFACE ( 'NONE', #660, 25.39999999999999858 ) ;
#39754=CIRCLE ( 'NONE', #68041, 24.99999999998784972 ) ;
#39769=ORIENTED_EDGE ( 'NONE', *, *, #43121, .T. ) ;
#39773=CARTESIAN_POINT ( 'NONE',  ( 47.00000000000000000, -0.7500000000000000000, -3.418698582794335028 ) ) ;
#39785=PLANE ( 'NONE',  #22801 ) ;
#39790=DIRECTION ( 'NONE',  ( -1.000000000000000000, 0.000000000000000000, 0.000000000000000000 ) ) ;
#39791=DIRECTION ( 'NONE',  ( 0.000000000000000000, 1.000000000000000000, 0.000000000000000000 ) ) ;
#39794=AXIS2_PLACEMENT_3D ( 'NONE', #47559, #20673, #26688 ) ;
#39798=AXIS2_PLACEMENT_3D ( 'NONE', #31003, #47967, #21441 ) ;
#39799=CYLINDRICAL_SURFACE ( 'NONE', #46334, 24.99999999998794920 ) ;
#39820=EDGE_CURVE ( 'NONE', #4332, #53128, #58321, .T. ) ;
#39825=CARTESIAN_POINT ( 'NONE',  ( 9.900000000000000355, 21.00000000000000000, 18.00000000000000355 ) ) ;
#39847=ORIENTED_EDGE ( 'NONE', *, *, #3518, .T. ) ;
#39849=FACE_OUTER_BOUND ( 'NONE', #23602, .T. ) ;
#39856=DIRECTION ( 'NONE',  ( 0.000000000000000000, 0.000000000000000000, -1.000000000000000000 ) ) ;
#39862=EDGE_CURVE ( 'NONE', #38301, #53157, #63976, .T. ) ;
#39865=EDGE_CURVE ( 'NONE', #29082, #29826, #6787, .T. ) ;
#39878=VECTOR ( 'NONE', #56175, 1000.000000000000000 ) ;
#39881=CARTESIAN_POINT ( 'NONE',  ( 49.00000000000000000, -0.1999999999911795112, 8.826273045769999343E-12 ) ) ;
#39883=LINE ( 'NONE', #61450, #39878 ) ;
#39895=VECTOR ( 'NONE', #35970, 1000.000000000000000 ) ;
#39905=DIRECTION ( 'NONE',  ( 0.000000000000000000, 0.000000000000000000, -1.000000000000000000 ) ) ;
#39934=PRESENTATION_STYLE_ASSIGNMENT (( #18374 ) ) ;
#39941=ORIENTED_EDGE ( 'NONE', *, *, #14715, .F. ) ;
#39948=VECTOR ( 'NONE', #19061, 1000.000000000000000 ) ;
#39978=VECTOR ( 'NONE', #38498, 1000.000000000000000 ) ;
#39985=CIRCLE ( 'NONE', #68284, 25.39999999999999858 ) ;
#39991=SURFACE_STYLE_USAGE ( .BOTH. , #34001 ) ;
#40002=CARTESIAN_POINT ( 'NONE',  ( 39.00000000000000000, -21.00000000000000000, -16.96999999999999886 ) ) ;
#40005=DIRECTION ( 'NONE',  ( 1.000000000000000000, -0.000000000000000000, 0.000000000000000000 ) ) ;
#40011=CARTESIAN_POINT ( 'NONE',  ( 0.5000000000000000000, -18.00000000000000355, -21.00000000000000000 ) ) ;
#40012=CARTESIAN_POINT ( 'NONE',  ( 49.00000000000000000, -0.2000000000089119934, 8.909539772616881237E-12 ) ) ;
#40015=CARTESIAN_POINT ( 'NONE',  ( 41.09999999999999432, 20.60000000000000142, 13.86939075806900057 ) ) ;
#40016=DIRECTION ( 'NONE',  ( 0.000000000000000000, 0.000000000000000000, -1.000000000000000000 ) ) ;
#40017=VERTEX_POINT ( 'NONE', #49772 ) ;
#40020=SURFACE_STYLE_FILL_AREA ( #18460 ) ;
#40022=VERTEX_POINT ( 'NONE', #22899 ) ;
#40026=VERTEX_POINT ( 'NONE', #44452 ) ;
#40031=VECTOR ( 'NONE', #26411, 1000.000000000000000 ) ;
#40042=DIRECTION ( 'NONE',  ( -1.000000000000000000, 0.000000000000000000, 0.000000000000000000 ) ) ;
#40050=VERTEX_POINT ( 'NONE', #14394 ) ;
#40051=EDGE_LOOP ( 'NONE', ( #17393, #2038, #65670, #602 ) ) ;
#40052=AXIS2_PLACEMENT_3D ( 'NONE', #28761, #18152, #2245 ) ;
#40053=ORIENTED_EDGE ( 'NONE', *, *, #46259, .F. ) ;
#40092=VECTOR ( 'NONE', #49085, 1000.000000000000000 ) ;
#40107=PRESENTATION_STYLE_ASSIGNMENT (( #33437 ) ) ;
#40110=ORIENTED_EDGE ( 'NONE', *, *, #21042, .T. ) ;
#40112=CARTESIAN_POINT ( 'NONE',  ( 0.5000000000000000000, -21.00000000000000000, -18.00000000000000355 ) ) ;
#40118=DIRECTION ( 'NONE',  ( 1.000000000000000000, -0.000000000000000000, 0.000000000000000000 ) ) ;
#40120=CARTESIAN_POINT ( 'NONE',  ( 10.00000000000000000, -18.00000000000000355, 21.00000000000000000 ) ) ;
#40123=DIRECTION ( 'NONE',  ( 0.000000000000000000, 0.7071067811865475727, -0.7071067811865475727 ) ) ;
#40132=EDGE_CURVE ( 'NONE', #46985, #38472, #15843, .T. ) ;
#40144=DIRECTION ( 'NONE',  ( -1.000000000000000000, 0.000000000000000000, 0.000000000000000000 ) ) ;
#40155=CIRCLE ( 'NONE', #39060, 24.99999999998794920 ) ;
#40160=EDGE_CURVE ( 'NONE', #60266, #21334, #5, .T. ) ;
#40170=EDGE_LOOP ( 'NONE', ( #64470, #9470, #43297, #19829 ) ) ;
#40173=DIRECTION ( 'NONE',  ( 0.000000000000000000, 0.000000000000000000, -1.000000000000000000 ) ) ;
#40182=ORIENTED_EDGE ( 'NONE', *, *, #37314, .T. ) ;
#40183=ORIENTED_EDGE ( 'NONE', *, *, #3386, .T. ) ;
#40186=DIRECTION ( 'NONE',  ( 0.000000000000000000, 0.000000000000000000, 1.000000000000000000 ) ) ;
#40200=CARTESIAN_POINT ( 'NONE',  ( 37.90000000000000568, 0.000000000000000000, 3.232403992503367940E-15 ) ) ;
#40211=VECTOR ( 'NONE', #35477, 1000.000000000000000 ) ;
#40212=FACE_OUTER_BOUND ( 'NONE', #20932, .T. ) ;
#40214=CARTESIAN_POINT ( 'NONE',  ( 32.89999999999999858, -21.00000000000000000, 13.86939075806900057 ) ) ;
#40215=EDGE_LOOP ( 'NONE', ( #39071, #69801, #55549, #2974 ) ) ;
#40240=CARTESIAN_POINT ( 'NONE',  ( 38.90000000000000568, -0.1999999999911795112, 8.826273045769999343E-12 ) ) ;
#40246=VECTOR ( 'NONE', #69470, 1000.000000000000000 ) ;
#40249=SHAPE_DEFINITION_REPRESENTATION ( #61615, #33595 ) ;
#40250=AXIS2_PLACEMENT_3D ( 'NONE', #17673, #39235, #12340 ) ;
#40252=CARTESIAN_POINT ( 'NONE',  ( 39.00000000000000000, 21.00000000000000000, -16.96999999999999886 ) ) ;
#40264=LINE ( 'NONE', #28607, #45859 ) ;
#40272=EDGE_CURVE ( 'NONE', #32725, #34472, #50844, .T. ) ;
#40274=CARTESIAN_POINT ( 'NONE',  ( 36.90000000000000568, 3.010794155703768650E-16, -2.458500000000000796 ) ) ;
#40292=FACE_OUTER_BOUND ( 'NONE', #21124, .T. ) ;
#40296=AXIS2_PLACEMENT_3D ( 'NONE', #45839, #50790, #28869 ) ;
#40297=ORIENTED_EDGE ( 'NONE', *, *, #58060, .F. ) ;
#40321=CARTESIAN_POINT ( 'NONE',  ( 46.39999999999999858, 21.00000000000000000, -2.250000000000000444 ) ) ;
#40338=CARTESIAN_POINT ( 'NONE',  ( 39.90000000000000568, 16.96999999999999886, 21.00000000000000000 ) ) ;
#40342=ORIENTED_EDGE ( 'NONE', *, *, #61163, .T. ) ;
#40343=ORIENTED_EDGE ( 'NONE', *, *, #12218, .T. ) ;
#40347=ORIENTED_EDGE ( 'NONE', *, *, #43585, .T. ) ;
#40367=EDGE_CURVE ( 'NONE', #60151, #19555, #5527, .T. ) ;
#40405=ORIENTED_EDGE ( 'NONE', *, *, #21582, .F. ) ;
#40407=ADVANCED_FACE ( 'NONE', ( #44367 ), #48660, .F. ) ;
#40411=EDGE_LOOP ( 'NONE', ( #61363, #60005, #38973, #33061 ) ) ;
#40416=DIRECTION ( 'NONE',  ( -1.000000000000000000, 0.000000000000000000, 0.000000000000000000 ) ) ;
#40420=AXIS2_PLACEMENT_3D ( 'NONE', #36979, #26349, #42256 ) ;
#40421=( NAMED_UNIT ( * ) SI_UNIT ( $, .STERADIAN. ) SOLID_ANGLE_UNIT ( ) );
#40423=ORIENTED_EDGE ( 'NONE', *, *, #2200, .F. ) ;
#40426=ORIENTED_EDGE ( 'NONE', *, *, #385, .T. ) ;
#40436=VERTEX_POINT ( 'NONE', #50380 ) ;
#40439=VERTEX_POINT ( 'NONE', #9267 ) ;
#40451=DIRECTION ( 'NONE',  ( 0.000000000000000000, 0.000000000000000000, -1.000000000000000000 ) ) ;
#40452=ORIENTED_EDGE ( 'NONE', *, *, #3950, .T. ) ;
#40457=CARTESIAN_POINT ( 'NONE',  ( 47.00000000000000000, 0.7500000000000000000, -5.000000000000000000 ) ) ;
#40461=CARTESIAN_POINT ( 'NONE',  ( 48.50000000000000000, 0.7500000000000000000, -3.418698582794335028 ) ) ;
#40481=EDGE_CURVE ( 'NONE', #2624, #35475, #55409, .T. ) ;
#40483=( NAMED_UNIT ( * ) SI_UNIT ( $, .STERADIAN. ) SOLID_ANGLE_UNIT ( ) );
#40487=EDGE_CURVE ( 'NONE', #43744, #63779, #7233, .T. ) ;
#40494=ADVANCED_FACE ( 'NONE', ( #25537 ), #40739, .F. ) ;
#40503=EDGE_CURVE ( 'NONE', #29633, #33288, #47487, .T. ) ;
#40531=CARTESIAN_POINT ( 'NONE',  ( 49.00000000000000000, -14.06939075806900163, -20.80000000000000426 ) ) ;
#40537=LINE ( 'NONE', #35218, #63723 ) ;
#40541=VECTOR ( 'NONE', #12242, 1000.000000000000000 ) ;
#40542=ADVANCED_FACE ( 'NONE', ( #37198 ), #48149, .F. ) ;
#40554=CARTESIAN_POINT ( 'NONE',  ( 10.00000000000000000, -21.00000000000000000, -18.00000000000000355 ) ) ;
#40561=EDGE_CURVE ( 'NONE', #55382, #61299, #67823, .T. ) ;
#40574=EDGE_CURVE ( 'NONE', #33150, #42593, #10316, .T. ) ;
#40575=CARTESIAN_POINT ( 'NONE',  ( 39.00000000000000000, 16.96999999999999886, 21.00000000000000000 ) ) ;
#40581=DIRECTION ( 'NONE',  ( 0.000000000000000000, 0.000000000000000000, 1.000000000000000000 ) ) ;
#40582=ORIENTED_EDGE ( 'NONE', *, *, #45403, .F. ) ;
#40586=ORIENTED_EDGE ( 'NONE', *, *, #1370, .F. ) ;
#40602=FACE_OUTER_BOUND ( 'NONE', #48665, .T. ) ;
#40607=DIRECTION ( 'NONE',  ( 0.000000000000000000, 0.000000000000000000, -1.000000000000000000 ) ) ;
#40611=CARTESIAN_POINT ( 'NONE',  ( 26.90000000000000213, 2.904780276981809389E-16, 2.285366197183106074 ) ) ;
#40615=EDGE_CURVE ( 'NONE', #10693, #39291, #32229, .T. ) ;
#40624=FILL_AREA_STYLE_COLOUR ( '', #61307 ) ;
#40630=AXIS2_PLACEMENT_3D ( 'NONE', #3682, #14639, #9335 ) ;
#40631=LINE ( 'NONE', #57247, #32993 ) ;
#40634=LINE ( 'NONE', #19416, #37324 ) ;
#40637=ORIENTED_EDGE ( 'NONE', *, *, #20710, .T. ) ;
#40644=LINE ( 'NONE', #8823, #67994 ) ;
#40658=AXIS2_PLACEMENT_3D ( 'NONE', #61693, #67703, #7948 ) ;
#40661=ORIENTED_EDGE ( 'NONE', *, *, #35938, .T. ) ;
#40665=AXIS2_PLACEMENT_3D ( 'NONE', #42410, #32149, #63996 ) ;
#40666=SURFACE_STYLE_FILL_AREA ( #67551 ) ;
#40669=ORIENTED_EDGE ( 'NONE', *, *, #4548, .F. ) ;
#40675=ORIENTED_EDGE ( 'NONE', *, *, #7618, .T. ) ;
#40703=CARTESIAN_POINT ( 'NONE',  ( 35.89999999999999858, -0.2000000000089119934, 8.909539772616881237E-12 ) ) ;
#40707=AXIS2_PLACEMENT_3D ( 'NONE', #63691, #36454, #43152 ) ;
#40714=EDGE_CURVE ( 'NONE', #20883, #64619, #13068, .T. ) ;
#40716=CARTESIAN_POINT ( 'NONE',  ( 8.900000000000005684, -21.00000000000000000, 13.86939075806900057 ) ) ;
#40722=PLANE ( 'NONE',  #44059 ) ;
#40723=EDGE_CURVE ( 'NONE', #36943, #42522, #23805, .T. ) ;
#40739=PLANE ( 'NONE',  #68945 ) ;
#40742=CARTESIAN_POINT ( 'NONE',  ( 34.89999999999999858, -0.1999999999911430404, -8.864436962241481021E-12 ) ) ;
#40743=EDGE_LOOP ( 'NONE', ( #528, #41920 ) ) ;
#40744=AXIS2_PLACEMENT_3D ( 'NONE', #52992, #15151, #36715 ) ;
#40758=ORIENTED_EDGE ( 'NONE', *, *, #2084, .T. ) ;
#40761=CIRCLE ( 'NONE', #40812, 24.99999999998794920 ) ;
#40769=( LENGTH_UNIT ( ) NAMED_UNIT ( * ) SI_UNIT ( .MILLI., .METRE. ) );
#40776=AXIS2_PLACEMENT_3D ( 'NONE', #3039, #41559, #30953 ) ;
#40777=ORIENTED_EDGE ( 'NONE', *, *, #21730, .T. ) ;
#40780=VECTOR ( 'NONE', #25646, 1000.000000000000000 ) ;
#40797=FACE_OUTER_BOUND ( 'NONE', #37279, .T. ) ;
#40803=ORIENTED_EDGE ( 'NONE', *, *, #14178, .T. ) ;
#40812=AXIS2_PLACEMENT_3D ( 'NONE', #27342, #48907, #467 ) ;
#40815=ORIENTED_EDGE ( 'NONE', *, *, #28356, .T. ) ;
#40820=CLOSED_SHELL ( 'NONE', ( #20147, #5082, #2254, #26894, #49280, #24404, #5629, #250, #10513, #53869, #10261, #49319, #61990, #32204, #35622, #50916, #65673, #53575 ) ) ;
#40830=DIRECTION ( 'NONE',  ( 1.000000000000000000, -0.000000000000000000, 0.000000000000000000 ) ) ;
#40836=CARTESIAN_POINT ( 'NONE',  ( 12.90000000000000213, -14.06939075806902117, -20.80000000000000426 ) ) ;
#40839=ORIENTED_EDGE ( 'NONE', *, *, #16029, .T. ) ;
#40849=VERTEX_POINT ( 'NONE', #30750 ) ;
#40854=CARTESIAN_POINT ( 'NONE',  ( 49.00000000000000000, -0.1999999999911795112, 8.826273045769999343E-12 ) ) ;
#40857=ORIENTED_EDGE ( 'NONE', *, *, #17849, .F. ) ;
#40858=CARTESIAN_POINT ( 'NONE',  ( 55.00000000000000000, 21.00000000000000000, -16.96999999999999886 ) ) ;
#40859=CARTESIAN_POINT ( 'NONE',  ( 41.09999999999999432, 20.60000000000000142, 13.86939075806900057 ) ) ;
#40863=VECTOR ( 'NONE', #64675, 1000.000000000000114 ) ;
#40879=DIRECTION ( 'NONE',  ( 0.000000000000000000, 0.000000000000000000, 1.000000000000000000 ) ) ;
#40882=ADVANCED_FACE ( 'NONE', ( #61875 ), #34984, .T. ) ;
#40887=PLANE ( 'NONE',  #25656 ) ;
#40895=ORIENTED_EDGE ( 'NONE', *, *, #9153, .F. ) ;
#40916=VECTOR ( 'NONE', #10080, 1000.000000000000114 ) ;
#40918=LINE ( 'NONE', #57193, #54163 ) ;
#40922=AXIS2_PLACEMENT_3D ( 'NONE', #49781, #12621, #66725 ) ;
#40931=ORIENTED_EDGE ( 'NONE', *, *, #54459, .F. ) ;
#40966=ADVANCED_FACE ( 'NONE', ( #15553 ), #26492, .F. ) ;
#40969=VERTEX_POINT ( 'NONE', #59363 ) ;
#40981=DIRECTION ( 'NONE',  ( -1.000000000000000000, 0.000000000000000000, 0.000000000000000000 ) ) ;
#40985=EDGE_LOOP ( 'NONE', ( #12411, #63494, #58607, #4016, #15380, #6969, #7519, #36744 ) ) ;
#40986=DIRECTION ( 'NONE',  ( 0.6785983445458467767, -0.6785983445458462215, 0.2810846377148228381 ) ) ;
#40990=VERTEX_POINT ( 'NONE', #20830 ) ;
#40994=ORIENTED_EDGE ( 'NONE', *, *, #63292, .T. ) ;
#40995=FACE_OUTER_BOUND ( 'NONE', #49060, .T. ) ;
#40997=VECTOR ( 'NONE', #42357, 1000.000000000000000 ) ;
#41019=CARTESIAN_POINT ( 'NONE',  ( 32.89999999999999858, 13.66939075806899240, 20.79999999999999361 ) ) ;
#41020=PLANE ( 'NONE',  #38794 ) ;
#41034=ORIENTED_EDGE ( 'NONE', *, *, #50073, .F. ) ;
#41039=FACE_OUTER_BOUND ( 'NONE', #57564, .T. ) ;
#41045=DIRECTION ( 'NONE',  ( 0.000000000000000000, -1.000000000000000000, 0.000000000000000000 ) ) ;
#41050=FACE_BOUND ( 'NONE', #68784, .T. ) ;
#41070=VERTEX_POINT ( 'NONE', #11594 ) ;
#41079=CARTESIAN_POINT ( 'NONE',  ( 29.89999999999999858, 20.60000000000000142, -13.86939075806900057 ) ) ;
#41083=CYLINDRICAL_SURFACE ( 'NONE', #42627, 24.99999999998794920 ) ;
#41090=AXIS2_PLACEMENT_3D ( 'NONE', #9654, #31576, #30508 ) ;
#41098=DIRECTION ( 'NONE',  ( 0.000000000000000000, 0.000000000000000000, -1.000000000000000000 ) ) ;
#41102=DIRECTION ( 'NONE',  ( -1.000000000000000000, 0.000000000000000000, 0.000000000000000000 ) ) ;
#41114=EDGE_CURVE ( 'NONE', #33288, #19106, #54751, .T. ) ;
#41127=ORIENTED_EDGE ( 'NONE', *, *, #1580, .T. ) ;
#41136=AXIS2_PLACEMENT_3D ( 'NONE', #66761, #7358, #2068 ) ;
#41139=ORIENTED_EDGE ( 'NONE', *, *, #29444, .F. ) ;
#41156=ORIENTED_EDGE ( 'NONE', *, *, #27735, .F. ) ;
#41168=DIRECTION ( 'NONE',  ( 1.000000000000000000, -0.000000000000000000, 0.000000000000000000 ) ) ;
#41172=CYLINDRICAL_SURFACE ( 'NONE', #62414, 0.5000000000000000000 ) ;
#41192=CARTESIAN_POINT ( 'NONE',  ( 31.89999999999999858, -14.06939075806902117, -20.80000000000000426 ) ) ;
#41202=LINE ( 'NONE', #4449, #46154 ) ;
#41212=VERTEX_POINT ( 'NONE', #46908 ) ;
#41213=ORIENTED_EDGE ( 'NONE', *, *, #14715, .T. ) ;
#41214=LINE ( 'NONE', #9047, #53089 ) ;
#41224=VECTOR ( 'NONE', #36343, 1000.000000000000000 ) ;
#41225=MECHANICAL_DESIGN_GEOMETRIC_PRESENTATION_REPRESENTATION('',(#60455),#46880);
#41228=DIRECTION ( 'NONE',  ( 0.000000000000000000, 0.7071067811865475727, -0.7071067811865475727 ) ) ;
#41232=( LENGTH_UNIT ( ) NAMED_UNIT ( * ) SI_UNIT ( .MILLI., .METRE. ) );
#41235=COLOUR_RGB ( '', 0.08235294, 0.09019608, 0.10196078) ;
#41237=DIRECTION ( 'NONE',  ( 0.000000000000000000, 0.000000000000000000, -1.000000000000000000 ) ) ;
#41240=DIRECTION ( 'NONE',  ( 0.000000000000000000, 0.000000000000000000, -1.000000000000000000 ) ) ;
#41255=DIRECTION ( 'NONE',  ( 1.000000000000000000, 0.000000000000000000, 0.000000000000000000 ) ) ;
#41262=( LENGTH_UNIT ( ) NAMED_UNIT ( * ) SI_UNIT ( .MILLI., .METRE. ) );
#41274=COLOUR_RGB ( '', 0.31764706, 0.68627451, 0.89019608) ;
#41275=ORIENTED_EDGE ( 'NONE', *, *, #64762, .F. ) ;
#41279=CARTESIAN_POINT ( 'NONE',  ( 9.900000000000000355, -18.00000000000000355, 21.00000000000000000 ) ) ;
#41288=EDGE_CURVE ( 'NONE', #245, #60080, #2384, .T. ) ;
#41310=ORIENTED_EDGE ( 'NONE', *, *, #14794, .F. ) ;
#41323=ORIENTED_EDGE ( 'NONE', *, *, #32686, .F. ) ;
#41340=CIRCLE ( 'NONE', #18777, 5.250000000000000000 ) ;
#41351=CARTESIAN_POINT ( 'NONE',  ( 39.00000000000000000, 21.00000000000000000, 16.96999999999999886 ) ) ;
#41354=CARTESIAN_POINT ( 'NONE',  ( 39.90000000000000568, -21.00000000000000000, -16.96999999999999886 ) ) ;
#41365=PLANE ( 'NONE',  #42277 ) ;
#41370=ORIENTED_EDGE ( 'NONE', *, *, #45997, .T. ) ;
#41373=VECTOR ( 'NONE', #36720, 1000.000000000000000 ) ;
#41388=ORIENTED_EDGE ( 'NONE', *, *, #20690, .F. ) ;
#41395=DIRECTION ( 'NONE',  ( 0.000000000000000000, 1.000000000000000000, -0.000000000000000000 ) ) ;
#41399=CARTESIAN_POINT ( 'NONE',  ( 10.90000000000000036, 0.000000000000000000, 2.154935995002245639E-16 ) ) ;
#41413=AXIS2_PLACEMENT_3D ( 'NONE', #40531, #40879, #51503 ) ;
#41418=CARTESIAN_POINT ( 'NONE',  ( 49.00000000000000000, 20.60000000000000142, -13.86939075806900057 ) ) ;
#41423=DIRECTION ( 'NONE',  ( 1.000000000000000000, -0.000000000000000000, 0.000000000000000000 ) ) ;
#41424=EDGE_CURVE ( 'NONE', #17228, #21641, #53295, .T. ) ;
#41425=CARTESIAN_POINT ( 'NONE',  ( 26.90000000000000213, -21.00000000000001421, -13.86939075806900945 ) ) ;
#41431=EDGE_CURVE ( 'NONE', #26279, #4186, #25722, .T. ) ;
#41435=EDGE_CURVE ( 'NONE', #23148, #16609, #44035, .T. ) ;
#41440=CARTESIAN_POINT ( 'NONE',  ( 39.00000000000000000, 16.96999999999999886, 21.00000000000000000 ) ) ;
#41450=EDGE_CURVE ( 'NONE', #68247, #29691, #27100, .T. ) ;
#41485=CARTESIAN_POINT ( 'NONE',  ( 49.00000000000000000, 13.66939075806899950, 20.80000000000000426 ) ) ;
#41492=AXIS2_PLACEMENT_3D ( 'NONE', #24059, #63304, #30068 ) ;
#41499=DIRECTION ( 'NONE',  ( 0.000000000000000000, 0.000000000000000000, -1.000000000000000000 ) ) ;
#41501=ORIENTED_EDGE ( 'NONE', *, *, #54711, .T. ) ;
#41502=LINE ( 'NONE', #52836, #63470 ) ;
#41508=CARTESIAN_POINT ( 'NONE',  ( 46.39999999999999858, 21.00000000000000000, -0.7500000000000000000 ) ) ;
#41509=LINE ( 'NONE', #37263, #32363 ) ;
#41510=DIRECTION ( 'NONE',  ( 1.000000000000000000, 0.000000000000000000, 0.000000000000000000 ) ) ;
#41524=CARTESIAN_POINT ( 'NONE',  ( 47.00000000000000000, 0.000000000000000000, 3.500000000000000000 ) ) ;
#41526=DIRECTION ( 'NONE',  ( 1.000000000000000000, 0.000000000000000000, 0.000000000000000000 ) ) ;
#41527=VECTOR ( 'NONE', #8211, 1000.000000000000000 ) ;
#41551=DIRECTION ( 'NONE',  ( 0.000000000000000000, 0.000000000000000000, -1.000000000000000000 ) ) ;
#41552=DIRECTION ( 'NONE',  ( -1.000000000000000000, 0.000000000000000000, 0.000000000000000000 ) ) ;
#41559=DIRECTION ( 'NONE',  ( -1.000000000000000000, 0.000000000000000000, 0.000000000000000000 ) ) ;
#41574=EDGE_LOOP ( 'NONE', ( #59461, #53823, #17709, #53250 ) ) ;
#41576=UNCERTAINTY_MEASURE_WITH_UNIT (LENGTH_MEASURE( 1.000000000000000082E-05 ), #22887, 'distance_accuracy_value', 'NONE');
#41581=CYLINDRICAL_SURFACE ( 'NONE', #37430, 24.99999999998784972 ) ;
#41586=CARTESIAN_POINT ( 'NONE',  ( 9.899999999999998579, -0.2000000000000000111, 0.000000000000000000 ) ) ;
#41590=PRESENTATION_STYLE_ASSIGNMENT (( #69514 ) ) ;
#41592=SURFACE_STYLE_USAGE ( .BOTH. , #46889 ) ;
#41596=EDGE_CURVE ( 'NONE', #63119, #24837, #17874, .T. ) ;
#41603=ORIENTED_EDGE ( 'NONE', *, *, #28354, .F. ) ;
#41614=ORIENTED_EDGE ( 'NONE', *, *, #4025, .F. ) ;
#41615=CARTESIAN_POINT ( 'NONE',  ( 30.90000000000000213, 13.66939075806899240, -20.79999999999999361 ) ) ;
#41616=DIRECTION ( 'NONE',  ( -1.000000000000000000, 0.000000000000000000, 0.000000000000000000 ) ) ;
#41626=CARTESIAN_POINT ( 'NONE',  ( 49.00000000000000000, -0.1999999999911430404, -8.864436962241481021E-12 ) ) ;
#41646=CARTESIAN_POINT ( 'NONE',  ( 8.900000000000005684, -14.48845687959340012, -21.00000000000000000 ) ) ;
#41647=ADVANCED_FACE ( 'NONE', ( #8295 ), #67002, .F. ) ;
#41675=DIRECTION ( 'NONE',  ( 0.000000000000000000, 0.7071067811865474617, -0.7071067811865474617 ) ) ;
#41677=DIRECTION ( 'NONE',  ( -0.7071067811865476838, -0.4999999999999997780, -0.4999999999999997780 ) ) ;
#41688=CARTESIAN_POINT ( 'NONE',  ( 8.900000000000005684, 13.66939075806899240, -20.79999999999999361 ) ) ;
#41703=CARTESIAN_POINT ( 'NONE',  ( 14.89999999999999680, 13.66939075806899240, 20.79999999999999361 ) ) ;
#41708=ORIENTED_EDGE ( 'NONE', *, *, #59779, .F. ) ;
#41713=ORIENTED_EDGE ( 'NONE', *, *, #57009, .T. ) ;
#41718=VERTEX_POINT ( 'NONE', #30240 ) ;
#41731=CARTESIAN_POINT ( 'NONE',  ( 46.39999999999999858, 21.00000000000000000, 0.2500000000000000000 ) ) ;
#41736=ADVANCED_FACE ( 'NONE', ( #18925 ), #50395, .F. ) ;
#41740=DIRECTION ( 'NONE',  ( 0.000000000000000000, 0.000000000000000000, -1.000000000000000000 ) ) ;
#41752=EDGE_LOOP ( 'NONE', ( #6263, #62340, #2867, #38686 ) ) ;
#41773=DIRECTION ( 'NONE',  ( 0.000000000000000000, 0.7071067811865475727, -0.7071067811865475727 ) ) ;
#41776=LINE ( 'NONE', #31191, #56790 ) ;
#41785=DIRECTION ( 'NONE',  ( 0.000000000000000000, -1.000000000000000000, 0.000000000000000000 ) ) ;
#41795=EDGE_LOOP ( 'NONE', ( #13004, #31568, #17193, #62610 ) ) ;
#41796=PLANE ( 'NONE',  #52859 ) ;
#41797=VECTOR ( 'NONE', #55250, 1000.000000000000000 ) ;
#41817=ORIENTED_EDGE ( 'NONE', *, *, #67747, .T. ) ;
#41823=AXIS2_PLACEMENT_3D ( 'NONE', #55836, #34610, #16978 ) ;
#41835=VECTOR ( 'NONE', #7614, 1000.000000000000000 ) ;
#41839=DIRECTION ( 'NONE',  ( 0.000000000000000000, -1.000000000000000000, 0.000000000000000000 ) ) ;
#41848=EDGE_LOOP ( 'NONE', ( #62104, #1145, #24135, #42619 ) ) ;
#41862=VECTOR ( 'NONE', #22876, 1000.000000000000000 ) ;
#41867=DIRECTION ( 'NONE',  ( 0.000000000000000000, 0.000000000000000000, -1.000000000000000000 ) ) ;
#41870=ADVANCED_FACE ( 'NONE', ( #25987 ), #58522, .T. ) ;
#41876=ORIENTED_EDGE ( 'NONE', *, *, #56411, .T. ) ;
#41885=EDGE_CURVE ( 'NONE', #21334, #17758, #52872, .T. ) ;
#41886=DIRECTION ( 'NONE',  ( 0.000000000000000000, 1.000000000000000000, 0.000000000000000000 ) ) ;
#41888=VECTOR ( 'NONE', #25033, 1000.000000000000000 ) ;
#41892=CARTESIAN_POINT ( 'NONE',  ( 12.90000000000000213, -0.2000000000089119934, 8.909539772616881237E-12 ) ) ;
#41893=VERTEX_POINT ( 'NONE', #46359 ) ;
#41899=AXIS2_PLACEMENT_3D ( 'NONE', #12263, #33840, #6967 ) ;
#41918=EDGE_LOOP ( 'NONE', ( #53445, #47828, #33893, #10990 ) ) ;
#41920=ORIENTED_EDGE ( 'NONE', *, *, #25115, .F. ) ;
#41921=CARTESIAN_POINT ( 'NONE',  ( 38.90000000000000568, -21.00000000000001421, -13.86939075806900945 ) ) ;
#41928=DIRECTION ( 'NONE',  ( 0.000000000000000000, 0.000000000000000000, 1.000000000000000000 ) ) ;
#41932=VERTEX_POINT ( 'NONE', #14539 ) ;
#41935=EDGE_CURVE ( 'NONE', #33525, #9808, #35092, .T. ) ;
#41945=SURFACE_STYLE_USAGE ( .BOTH. , #20377 ) ;
#41957=CARTESIAN_POINT ( 'NONE',  ( 0.000000000000000000, 17.79289321881345032, 20.50000000000000000 ) ) ;
#41964=CARTESIAN_POINT ( 'NONE',  ( 41.09999999999999432, -0.2000000000000000111, 0.000000000000000000 ) ) ;
#41972=FACE_OUTER_BOUND ( 'NONE', #59417, .T. ) ;
#41975=COLOUR_RGB ( '', 0.66274510, 0.83137255, 0.94901961) ;
#41977=FACE_OUTER_BOUND ( 'NONE', #2005, .T. ) ;
#41979=ORIENTED_EDGE ( 'NONE', *, *, #26676, .F. ) ;
#41981=LINE ( 'NONE', #63200, #43095 ) ;
#41984=AXIS2_PLACEMENT_3D ( 'NONE', #3195, #8837, #36407 ) ;
#41999=CARTESIAN_POINT ( 'NONE',  ( 35.89999999999999858, -14.06939075806902117, -20.80000000000000426 ) ) ;
#42001=ORIENTED_EDGE ( 'NONE', *, *, #15016, .T. ) ;
#42021=DIRECTION ( 'NONE',  ( 0.000000000000000000, -1.000000000000000000, 0.000000000000000000 ) ) ;
#42024=EDGE_LOOP ( 'NONE', ( #22087, #14281, #63987, #35713 ) ) ;
#42027=DIRECTION ( 'NONE',  ( 0.000000000000000000, 0.000000000000000000, -1.000000000000000000 ) ) ;
#42046=ADVANCED_FACE ( 'NONE', ( #5349 ), #47072, .T. ) ;
#42055=PRESENTATION_STYLE_ASSIGNMENT (( #36398 ) ) ;
#42065=ORIENTED_EDGE ( 'NONE', *, *, #45856, .T. ) ;
#42068=DIRECTION ( 'NONE',  ( 0.000000000000000000, 1.000000000000000000, -0.000000000000000000 ) ) ;
#42069=DIRECTION ( 'NONE',  ( 1.000000000000000000, -0.000000000000000000, 0.000000000000000000 ) ) ;
#42082=CARTESIAN_POINT ( 'NONE',  ( 17.89999999999999858, -0.2000000000089119934, 8.909539772616881237E-12 ) ) ;
#42085=VERTEX_POINT ( 'NONE', #10627 ) ;
#42086=CARTESIAN_POINT ( 'NONE',  ( 47.00000000000000000, 0.000000000000000000, 0.000000000000000000 ) ) ;
#42095=ORIENTED_EDGE ( 'NONE', *, *, #1620, .T. ) ;
#42100=ORIENTED_EDGE ( 'NONE', *, *, #13767, .F. ) ;
#42118=ORIENTED_EDGE ( 'NONE', *, *, #27654, .T. ) ;
#42121=EDGE_LOOP ( 'NONE', ( #43670, #26985, #18818, #23740 ) ) ;
#42125=CIRCLE ( 'NONE', #51148, 24.99999999998784972 ) ;
#42134=VERTEX_POINT ( 'NONE', #52746 ) ;
#42139=ORIENTED_EDGE ( 'NONE', *, *, #24114, .F. ) ;
#42144=DIRECTION ( 'NONE',  ( 0.000000000000000000, 0.000000000000000000, -1.000000000000000000 ) ) ;
#42152=LINE ( 'NONE', #46402, #23905 ) ;
#42156=ORIENTED_EDGE ( 'NONE', *, *, #18541, .T. ) ;
#42168=AXIS2_PLACEMENT_3D ( 'NONE', #35590, #51164, #19336 ) ;
#42179=EDGE_LOOP ( 'NONE', ( #67207, #53532, #29992, #22237 ) ) ;
#42193=CARTESIAN_POINT ( 'NONE',  ( 27.90000000000000213, -14.06939075806900874, 20.80000000000001137 ) ) ;
#42196=ORIENTED_EDGE ( 'NONE', *, *, #66004, .T. ) ;
#42202=CARTESIAN_POINT ( 'NONE',  ( 41.09999999999999432, 13.66939075806899950, -20.80000000000000426 ) ) ;
#42209=LINE ( 'NONE', #13147, #63133 ) ;
#42215=CARTESIAN_POINT ( 'NONE',  ( 23.90000000000000213, -14.06939075806902117, -20.80000000000000426 ) ) ;
#42217=( NAMED_UNIT ( * ) SI_UNIT ( $, .STERADIAN. ) SOLID_ANGLE_UNIT ( ) );
#42219=DIRECTION ( 'NONE',  ( 0.000000000000000000, 0.000000000000000000, -1.000000000000000000 ) ) ;
#42232=CARTESIAN_POINT ( 'NONE',  ( 41.09999999999999432, 13.66939075806899950, -20.80000000000000426 ) ) ;
#42253=ORIENTED_EDGE ( 'NONE', *, *, #66819, .T. ) ;
#42255=DIRECTION ( 'NONE',  ( 0.000000000000000000, 1.000000000000000000, 0.000000000000000000 ) ) ;
#42256=DIRECTION ( 'NONE',  ( 0.000000000000000000, 0.000000000000000000, -1.000000000000000000 ) ) ;
#42258=EDGE_CURVE ( 'NONE', #33149, #27652, #11654, .T. ) ;
#42272=EDGE_CURVE ( 'NONE', #24688, #26801, #65598, .T. ) ;
#42277=AXIS2_PLACEMENT_3D ( 'NONE', #50588, #45976, #8845 ) ;
#42287=CARTESIAN_POINT ( 'NONE',  ( 36.90000000000000568, 0.000000000000000000, 0.000000000000000000 ) ) ;
#42288=VERTEX_POINT ( 'NONE', #377 ) ;
#42303=ORIENTED_EDGE ( 'NONE', *, *, #148, .F. ) ;
#42313=CARTESIAN_POINT ( 'NONE',  ( 25.57999999999999829, 0.000000000000000000, 2.458500000000000796 ) ) ;
#42314=FACE_OUTER_BOUND ( 'NONE', #17470, .T. ) ;
#42320=EDGE_LOOP ( 'NONE', ( #814, #60850, #35611, #53923 ) ) ;
#42346=ORIENTED_EDGE ( 'NONE', *, *, #64441, .T. ) ;
#42357=DIRECTION ( 'NONE',  ( 1.000000000000000000, 0.000000000000000000, 0.000000000000000000 ) ) ;
#42361=COLOUR_RGB ( '', 0.08235294, 0.09019608, 0.10196078) ;
#42365=AXIS2_PLACEMENT_3D ( 'NONE', #29757, #1852, #51331 ) ;
#42366=LINE ( 'NONE', #69598, #25601 ) ;
#42387=EDGE_CURVE ( 'NONE', #4916, #54625, #6464, .T. ) ;
#42389=ORIENTED_EDGE ( 'NONE', *, *, #44844, .F. ) ;
#42393=SURFACE_SIDE_STYLE ('',( #32136 ) ) ;
#42397=VECTOR ( 'NONE', #31413, 1000.000000000000000 ) ;
#42402=EDGE_CURVE ( 'NONE', #4698, #43746, #126, .T. ) ;
#42409=EDGE_CURVE ( 'NONE', #14789, #42432, #40761, .T. ) ;
#42410=CARTESIAN_POINT ( 'NONE',  ( 39.90000000000000568, 0.000000000000000000, 3.447897592003593022E-15 ) ) ;
#42414=ORIENTED_EDGE ( 'NONE', *, *, #13541, .T. ) ;
#42417=ORIENTED_EDGE ( 'NONE', *, *, #33255, .T. ) ;
#42424=ORIENTED_EDGE ( 'NONE', *, *, #53991, .T. ) ;
#42430=FACE_OUTER_BOUND ( 'NONE', #56731, .T. ) ;
#42432=VERTEX_POINT ( 'NONE', #6111 ) ;
#42447=CARTESIAN_POINT ( 'NONE',  ( 8.900000000000002132, 18.00000000000000355, -21.00000000000000000 ) ) ;
#42462=MANIFOLD_SOLID_BREP ( 'LPattern1[10]', #54417 ) ;
#42465=DIRECTION ( 'NONE',  ( 0.000000000000000000, 0.000000000000000000, -1.000000000000000000 ) ) ;
#42475=ORIENTED_EDGE ( 'NONE', *, *, #15851, .T. ) ;
#42479=EDGE_CURVE ( 'NONE', #57287, #10693, #8175, .T. ) ;
#42486=EDGE_CURVE ( 'NONE', #11546, #36357, #34337, .T. ) ;
#42489=ORIENTED_EDGE ( 'NONE', *, *, #541, .F. ) ;
#42492=EDGE_CURVE ( 'NONE', #44196, #1707, #28699, .T. ) ;
#42497=ORIENTED_EDGE ( 'NONE', *, *, #12947, .F. ) ;
#42509=ORIENTED_EDGE ( 'NONE', *, *, #3950, .F. ) ;
#42515=DIRECTION ( 'NONE',  ( 0.000000000000000000, 0.000000000000000000, 1.000000000000000000 ) ) ;
#42519=DIRECTION ( 'NONE',  ( 0.000000000000000000, 1.000000000000000000, 0.000000000000000000 ) ) ;
#42522=VERTEX_POINT ( 'NONE', #39321 ) ;
#42526=CARTESIAN_POINT ( 'NONE',  ( 9.899999999999998579, -21.00000000000000000, 13.86939075806900057 ) ) ;
#42533=ADVANCED_FACE ( 'NONE', ( #55927 ), #49924, .T. ) ;
#42535=VERTEX_POINT ( 'NONE', #2185 ) ;
#42536=AXIS2_PLACEMENT_3D ( 'NONE', #29800, #24507, #13889 ) ;
#42550=CARTESIAN_POINT ( 'NONE',  ( 49.00000000000000000, -21.00000000000000000, 13.86939075806900057 ) ) ;
#42559=DIRECTION ( 'NONE',  ( 0.000000000000000000, 0.000000000000000000, -1.000000000000000000 ) ) ;
#42573=DIRECTION ( 'NONE',  ( 0.000000000000000000, 0.000000000000000000, -1.000000000000000000 ) ) ;
#42586=CYLINDRICAL_SURFACE ( 'NONE', #53814, 24.99999999998784972 ) ;
#42589=SURFACE_STYLE_FILL_AREA ( #58864 ) ;
#42593=VERTEX_POINT ( 'NONE', #15250 ) ;
#42595=VECTOR ( 'NONE', #69813, 1000.000000000000000 ) ;
#42603=AXIS2_PLACEMENT_3D ( 'NONE', #37482, #10595, #26520 ) ;
#42605=DIRECTION ( 'NONE',  ( 0.000000000000000000, 0.000000000000000000, -1.000000000000000000 ) ) ;
#42619=ORIENTED_EDGE ( 'NONE', *, *, #14980, .F. ) ;
#42624=FACE_BOUND ( 'NONE', #56581, .T. ) ;
#42626=LINE ( 'NONE', #64213, #22261 ) ;
#42627=AXIS2_PLACEMENT_3D ( 'NONE', #8201, #67266, #61949 ) ;
#42643=EDGE_LOOP ( 'NONE', ( #43229, #37242, #59740, #38053 ) ) ;
#42650=ORIENTED_EDGE ( 'NONE', *, *, #49827, .T. ) ;
#42652=CARTESIAN_POINT ( 'NONE',  ( 29.89999999999999858, -0.1999999999911795112, 8.826273045769999343E-12 ) ) ;
#42666=EDGE_CURVE ( 'NONE', #19943, #60403, #31801, .T. ) ;
#42691=MANIFOLD_SOLID_BREP ( 'LPattern1[22]', #38616 ) ;
#42704=CARTESIAN_POINT ( 'NONE',  ( 39.90000000000000568, -21.00000000000000355, -14.57806571531352269 ) ) ;
#42705=CARTESIAN_POINT ( 'NONE',  ( 7.899999999999999467, -14.48845687959340012, 21.00000000000000000 ) ) ;
#42706=ORIENTED_EDGE ( 'NONE', *, *, #26095, .T. ) ;
#42710=CARTESIAN_POINT ( 'NONE',  ( 20.90000000000000213, -0.1999999999911430404, -8.864436962241481021E-12 ) ) ;
#42715=CARTESIAN_POINT ( 'NONE',  ( 10.90000000000000036, -21.00000000000000000, 13.86939075806900057 ) ) ;
#42717=EDGE_CURVE ( 'NONE', #58001, #41070, #49842, .T. ) ;
#42729=DIRECTION ( 'NONE',  ( 0.000000000000000000, -1.000000000000000000, 0.000000000000000000 ) ) ;
#42730=EDGE_CURVE ( 'NONE', #18454, #8699, #60035, .T. ) ;
#42732=CARTESIAN_POINT ( 'NONE',  ( 27.00000000000000000, 0.000000000000000000, -2.458500000000000796 ) ) ;
#42737=ADVANCED_FACE ( 'NONE', ( #31867 ), #58736, .F. ) ;
#42740=CARTESIAN_POINT ( 'NONE',  ( 41.09999999999999432, -21.00000000000000000, -13.86939075806900057 ) ) ;
#42763=CARTESIAN_POINT ( 'NONE',  ( 9.900000000000000355, -21.00000000000000000, -18.00000000000000355 ) ) ;
#42764=ORIENTED_EDGE ( 'NONE', *, *, #30157, .T. ) ;
#42775=DIRECTION ( 'NONE',  ( 0.000000000000000000, 0.000000000000000000, -1.000000000000000000 ) ) ;
#42776=CARTESIAN_POINT ( 'NONE',  ( 50.00000000000000711, 0.7500000000000000000, -4.943429983321300902 ) ) ;
#42785=ORIENTED_EDGE ( 'NONE', *, *, #13381, .T. ) ;
#42807=MANIFOLD_SOLID_BREP ( 'LPattern1[20]', #65660 ) ;
#42809=CARTESIAN_POINT ( 'NONE',  ( 39.00000000000000000, 0.000000000000000000, 0.000000000000000000 ) ) ;
#42824=ORIENTED_EDGE ( 'NONE', *, *, #23725, .T. ) ;
#42828=CARTESIAN_POINT ( 'NONE',  ( 8.900000000000002132, 0.000000000000000000, 0.000000000000000000 ) ) ;
#42829=ORIENTED_EDGE ( 'NONE', *, *, #20897, .T. ) ;
#42834=CARTESIAN_POINT ( 'NONE',  ( 39.90000000000000568, 0.000000000000000000, 3.447897592003593022E-15 ) ) ;
#42837=EDGE_CURVE ( 'NONE', #43994, #44242, #44521, .T. ) ;
#42838=VECTOR ( 'NONE', #49884, 1000.000000000000000 ) ;
#42845=CIRCLE ( 'NONE', #50750, 5.250000000000000000 ) ;
#42847=CARTESIAN_POINT ( 'NONE',  ( 38.90000000000000568, -0.2000000000089119934, -8.913009219568841313E-12 ) ) ;
#42849=DIRECTION ( 'NONE',  ( -1.000000000000000000, 0.000000000000000000, 0.000000000000000000 ) ) ;
#42857=FACE_OUTER_BOUND ( 'NONE', #4737, .T. ) ;
#42866=ORIENTED_EDGE ( 'NONE', *, *, #371, .F. ) ;
#42879=LINE ( 'NONE', #65498, #54637 ) ;
#42882=EDGE_CURVE ( 'NONE', #66079, #57523, #32946, .T. ) ;
#42884=ORIENTED_EDGE ( 'NONE', *, *, #34029, .F. ) ;
#42891=CIRCLE ( 'NONE', #2250, 25.39999999999999858 ) ;
#42893=EDGE_CURVE ( 'NONE', #34559, #61917, #36730, .T. ) ;
#42902=DIRECTION ( 'NONE',  ( 0.000000000000000000, 0.000000000000000000, 1.000000000000000000 ) ) ;
#42908=EDGE_LOOP ( 'NONE', ( #10784, #31908, #3110, #58781 ) ) ;
#42919=EDGE_CURVE ( 'NONE', #53158, #34278, #63439, .T. ) ;
#42920=EDGE_LOOP ( 'NONE', ( #787, #46724, #22930, #22434 ) ) ;
#42921=MANIFOLD_SOLID_BREP ( 'LPattern1[12]', #5853 ) ;
#42925=ADVANCED_FACE ( 'NONE', ( #2789 ), #3158, .T. ) ;
#42926=ORIENTED_EDGE ( 'NONE', *, *, #14356, .F. ) ;
#42929=LINE ( 'NONE', #60223, #31990 ) ;
#42930=ORIENTED_EDGE ( 'NONE', *, *, #65053, .F. ) ;
#42932=DIRECTION ( 'NONE',  ( 0.000000000000000000, 0.000000000000000000, -1.000000000000000000 ) ) ;
#42939=ORIENTED_EDGE ( 'NONE', *, *, #31085, .T. ) ;
#42942=LINE ( 'NONE', #32682, #755 ) ;
#42947=LINE ( 'NONE', #57810, #63497 ) ;
#42963=VERTEX_POINT ( 'NONE', #30724 ) ;
#42967=UNCERTAINTY_MEASURE_WITH_UNIT (LENGTH_MEASURE( 1.000000000000000082E-05 ), #31784, 'distance_accuracy_value', 'NONE');
#42991=FACE_OUTER_BOUND ( 'NONE', #9623, .T. ) ;
#43000=FACE_BOUND ( 'NONE', #38233, .T. ) ;
#43001=LINE ( 'NONE', #20393, #24010 ) ;
#43002=EDGE_CURVE ( 'NONE', #32778, #23370, #67851, .T. ) ;
#43005=CYLINDRICAL_SURFACE ( 'NONE', #69173, 5.250000000000000000 ) ;
#43007=DIRECTION ( 'NONE',  ( 1.000000000000000000, -0.000000000000000000, 0.000000000000000000 ) ) ;
#43012=CARTESIAN_POINT ( 'NONE',  ( 41.09999999999999432, 20.60000000000000142, -13.86939075806900057 ) ) ;
#43015=ORIENTED_EDGE ( 'NONE', *, *, #2366, .T. ) ;
#43026=ORIENTED_EDGE ( 'NONE', *, *, #66660, .F. ) ;
#43035=MANIFOLD_SOLID_BREP ( 'LPattern1[4]', #36328 ) ;
#43037=ORIENTED_EDGE ( 'NONE', *, *, #36928, .T. ) ;
#43039=DIRECTION ( 'NONE',  ( 0.000000000000000000, 0.000000000000000000, -1.000000000000000000 ) ) ;
#43040=FACE_OUTER_BOUND ( 'NONE', #26794, .T. ) ;
#43055=LINE ( 'NONE', #32465, #58838 ) ;
#43059=EDGE_LOOP ( 'NONE', ( #25758, #39305, #26129, #26417, #12606, #56402, #21884, #12935 ) ) ;
#43067=EDGE_CURVE ( 'NONE', #9337, #34243, #16899, .T. ) ;
#43079=DIRECTION ( 'NONE',  ( -1.000000000000000000, 0.000000000000000000, 0.000000000000000000 ) ) ;
#43086=STYLED_ITEM ( 'NONE', ( #36455 ), #42691 ) ;
#43089=CARTESIAN_POINT ( 'NONE',  ( 40.90000000000000568, 6.123233995736766282E-16, -5.000000000000000000 ) ) ;
#43095=VECTOR ( 'NONE', #68513, 1000.000000000000000 ) ;
#43097=CARTESIAN_POINT ( 'NONE',  ( 18.89999999999999858, -0.1999999999911430404, -8.864436962241481021E-12 ) ) ;
#43107=CIRCLE ( 'NONE', #23919, 2.458500000000000796 ) ;
#43110=EDGE_CURVE ( 'NONE', #2257, #44787, #32024, .T. ) ;
#43113=ORIENTED_EDGE ( 'NONE', *, *, #35649, .F. ) ;
#43116=ORIENTED_EDGE ( 'NONE', *, *, #40503, .T. ) ;
#43119=DIRECTION ( 'NONE',  ( -1.000000000000000000, 0.000000000000000000, 0.000000000000000000 ) ) ;
#43121=EDGE_CURVE ( 'NONE', #10117, #27398, #50100, .T. ) ;
#43124=CARTESIAN_POINT ( 'NONE',  ( 41.09999999999999432, 13.66939075806899950, 20.80000000000000426 ) ) ;
#43127=ORIENTED_EDGE ( 'NONE', *, *, #47251, .T. ) ;
#43129=VERTEX_POINT ( 'NONE', #12954 ) ;
#43131=EDGE_CURVE ( 'NONE', #46953, #31241, #60356, .T. ) ;
#43135=EDGE_CURVE ( 'NONE', #49649, #41718, #60714, .T. ) ;
#43141=CIRCLE ( 'NONE', #23950, 24.99999999998784972 ) ;
#43151=MANIFOLD_SOLID_BREP ( 'LPattern1[17]', #17148 ) ;
#43152=DIRECTION ( 'NONE',  ( 0.000000000000000000, 0.7071067811865474617, -0.7071067811865474617 ) ) ;
#43153=DIRECTION ( 'NONE',  ( -1.000000000000000000, 0.000000000000000000, 0.000000000000000000 ) ) ;
#43156=ORIENTED_EDGE ( 'NONE', *, *, #11665, .F. ) ;
#43160=EDGE_CURVE ( 'NONE', #20722, #48934, #23228, .T. ) ;
#43179=FACE_OUTER_BOUND ( 'NONE', #25637, .T. ) ;
#43183=EDGE_CURVE ( 'NONE', #30940, #22451, #44436, .T. ) ;
#43189=VECTOR ( 'NONE', #38944, 1000.000000000000000 ) ;
#43207=EDGE_CURVE ( 'NONE', #8437, #33149, #49130, .T. ) ;
#43212=AXIS2_PLACEMENT_3D ( 'NONE', #67924, #62973, #8513 ) ;
#43214=LINE ( 'NONE', #60513, #63490 ) ;
#43215=ORIENTED_EDGE ( 'NONE', *, *, #53936, .T. ) ;
#43222=CARTESIAN_POINT ( 'NONE',  ( 49.00000000000000000, -21.00000000000000000, 13.86939075806900057 ) ) ;
#43229=ORIENTED_EDGE ( 'NONE', *, *, #11487, .F. ) ;
#43230=LINE ( 'NONE', #61115, #61017 ) ;
#43237=DIRECTION ( 'NONE',  ( 0.000000000000000000, 0.000000000000000000, -1.000000000000000000 ) ) ;
#43239=EDGE_CURVE ( 'NONE', #43994, #31863, #2700, .T. ) ;
#43244=ORIENTED_EDGE ( 'NONE', *, *, #16600, .T. ) ;
#43266=VECTOR ( 'NONE', #43840, 1000.000000000000000 ) ;
#43268=MANIFOLD_SOLID_BREP ( 'Move Face1[1]', #61136 ) ;
#43273=DIRECTION ( 'NONE',  ( 0.000000000000000000, 0.000000000000000000, -1.000000000000000000 ) ) ;
#43275=ORIENTED_EDGE ( 'NONE', *, *, #62750, .T. ) ;
#43287=CARTESIAN_POINT ( 'NONE',  ( 34.89999999999999858, -0.2000000000089119934, 8.909539772616881237E-12 ) ) ;
#43297=ORIENTED_EDGE ( 'NONE', *, *, #5300, .T. ) ;
#43300=CARTESIAN_POINT ( 'NONE',  ( 39.00000000000000000, 0.000000000000000000, 0.000000000000000000 ) ) ;
#43303=CIRCLE ( 'NONE', #52347, 25.39999999999999858 ) ;
#43315=VECTOR ( 'NONE', #1654, 1000.000000000000000 ) ;
#43333=DIRECTION ( 'NONE',  ( -1.000000000000000000, 0.000000000000000000, 0.000000000000000000 ) ) ;
#43336=CARTESIAN_POINT ( 'NONE',  ( 16.89999999999999858, -21.00000000000000000, 13.86939075806900057 ) ) ;
#43343=DIRECTION ( 'NONE',  ( 0.000000000000000000, 0.000000000000000000, -1.000000000000000000 ) ) ;
#43349=CIRCLE ( 'NONE', #65908, 25.39999999999999858 ) ;
#43359=ADVANCED_FACE ( 'NONE', ( #53270 ), #22395, .T. ) ;
#43367=ORIENTED_EDGE ( 'NONE', *, *, #9036, .F. ) ;
#43373=ORIENTED_EDGE ( 'NONE', *, *, #52076, .F. ) ;
#43379=CARTESIAN_POINT ( 'NONE',  ( 38.90000000000000568, -0.1999999999911430404, -8.864436962241481021E-12 ) ) ;
#43380=MANIFOLD_SOLID_BREP ( 'LPattern1[11]', #57781 ) ;
#43385=LINE ( 'NONE', #64969, #39504 ) ;
#43397=LINE ( 'NONE', #28177, #41862 ) ;
#43399=ORIENTED_EDGE ( 'NONE', *, *, #42479, .F. ) ;
#43400=EDGE_CURVE ( 'NONE', #62836, #2764, #24284, .T. ) ;
#43402=VECTOR ( 'NONE', #32600, 1000.000000000000000 ) ;
#43407=CARTESIAN_POINT ( 'NONE',  ( 28.90000000000000213, 13.66939075806899950, 20.80000000000000426 ) ) ;
#43415=CARTESIAN_POINT ( 'NONE',  ( 39.90000000000000568, -14.48845687959340012, -21.00000000000000000 ) ) ;
#43419=CARTESIAN_POINT ( 'NONE',  ( 25.90000000000000213, 0.000000000000000000, 1.939442395502021001E-15 ) ) ;
#43420=ORIENTED_EDGE ( 'NONE', *, *, #18040, .T. ) ;
#43427=FACE_BOUND ( 'NONE', #60992, .T. ) ;
#43434=AXIS2_PLACEMENT_3D ( 'NONE', #34897, #56478, #8026 ) ;
#43442=VECTOR ( 'NONE', #63004, 1000.000000000000000 ) ;
#43450=EDGE_CURVE ( 'NONE', #64422, #63119, #2831, .T. ) ;
#43457=DIRECTION ( 'NONE',  ( 0.000000000000000000, 0.000000000000000000, -1.000000000000000000 ) ) ;
#43463=EDGE_LOOP ( 'NONE', ( #16518, #47699, #26642, #5883 ) ) ;
#43468=ORIENTED_EDGE ( 'NONE', *, *, #45787, .F. ) ;
#43475=CARTESIAN_POINT ( 'NONE',  ( 25.57999999999999829, 3.010794155703768650E-16, -2.458500000000000796 ) ) ;
#43483=CIRCLE ( 'NONE', #9634, 24.99999999998794920 ) ;
#43496=CARTESIAN_POINT ( 'NONE',  ( 32.89999999999999858, 0.000000000000000000, 0.000000000000000000 ) ) ;
#43518=LINE ( 'NONE', #11677, #5298 ) ;
#43525=DIRECTION ( 'NONE',  ( -1.000000000000000000, 0.000000000000000000, 0.000000000000000000 ) ) ;
#43527=CARTESIAN_POINT ( 'NONE',  ( 49.00000000000000000, 20.60000000000000142, -13.86939075806900057 ) ) ;
#43551=VECTOR ( 'NONE', #35034, 1000.000000000000000 ) ;
#43557=AXIS2_PLACEMENT_3D ( 'NONE', #67566, #19115, #56936 ) ;
#43568=LINE ( 'NONE', #65153, #16304 ) ;
#43571=VERTEX_POINT ( 'NONE', #41425 ) ;
#43582=DIRECTION ( 'NONE',  ( 0.000000000000000000, 0.000000000000000000, -1.000000000000000000 ) ) ;
#43585=EDGE_CURVE ( 'NONE', #2849, #19378, #52393, .T. ) ;
#43587=CARTESIAN_POINT ( 'NONE',  ( 8.900000000000005684, 20.60000000000000142, -13.86939075806900057 ) ) ;
#43598=DIRECTION ( 'NONE',  ( 1.000000000000000000, -0.000000000000000000, -0.000000000000000000 ) ) ;
#43600=EDGE_CURVE ( 'NONE', #56111, #4682, #3248, .T. ) ;
#43614=DIRECTION ( 'NONE',  ( 1.000000000000000000, -0.000000000000000000, 0.000000000000000000 ) ) ;
#43629=ORIENTED_EDGE ( 'NONE', *, *, #68534, .F. ) ;
#43651=EDGE_LOOP ( 'NONE', ( #65771, #8209, #44187, #38448 ) ) ;
#43670=ORIENTED_EDGE ( 'NONE', *, *, #45339, .F. ) ;
#43679=CIRCLE ( 'NONE', #13166, 24.99999999998784972 ) ;
#43698=AXIS2_PLACEMENT_3D ( 'NONE', #20039, #9794, #15086 ) ;
#43700=CARTESIAN_POINT ( 'NONE',  ( 41.09999999999999432, 13.66939075806899950, -20.80000000000000426 ) ) ;
#43713=ORIENTED_EDGE ( 'NONE', *, *, #44058, .T. ) ;
#43739=CARTESIAN_POINT ( 'NONE',  ( 49.00000000000000000, 0.7500000000000000000, 4.943429983321300014 ) ) ;
#43742=CYLINDRICAL_SURFACE ( 'NONE', #780, 25.39999999999999858 ) ;
#43744=VERTEX_POINT ( 'NONE', #11333 ) ;
#43745=ORIENTED_EDGE ( 'NONE', *, *, #43135, .T. ) ;
#43746=VERTEX_POINT ( 'NONE', #38567 ) ;
#43748=CIRCLE ( 'NONE', #22307, 24.99999999998784972 ) ;
#43751=ORIENTED_EDGE ( 'NONE', *, *, #30348, .T. ) ;
#43753=EDGE_CURVE ( 'NONE', #45421, #33487, #54493, .T. ) ;
#43758=ORIENTED_EDGE ( 'NONE', *, *, #44132, .F. ) ;
#43765=CARTESIAN_POINT ( 'NONE',  ( 39.00000000000000000, 0.000000000000000000, 0.000000000000000000 ) ) ;
#43769=ORIENTED_EDGE ( 'NONE', *, *, #62045, .T. ) ;
#43795=EDGE_LOOP ( 'NONE', ( #54608, #46372, #2521, #42497 ) ) ;
#43798=LINE ( 'NONE', #65374, #39978 ) ;
#43802=EDGE_CURVE ( 'NONE', #10620, #40436, #45946, .T. ) ;
#43818=ORIENTED_EDGE ( 'NONE', *, *, #14178, .F. ) ;
#43826=CARTESIAN_POINT ( 'NONE',  ( 27.90000000000000213, 3.010794155703768650E-16, -2.458500000000000796 ) ) ;
#43827=ORIENTED_EDGE ( 'NONE', *, *, #40481, .F. ) ;
#43828=ORIENTED_EDGE ( 'NONE', *, *, #48335, .T. ) ;
#43840=DIRECTION ( 'NONE',  ( 0.000000000000000000, 0.000000000000000000, -1.000000000000000000 ) ) ;
#43848=MANIFOLD_SOLID_BREP ( 'LPattern1[16]', #53262 ) ;
#43867=ADVANCED_FACE ( 'NONE', ( #13058 ), #19759, .F. ) ;
#43884=DIRECTION ( 'NONE',  ( 0.000000000000000000, 0.000000000000000000, -1.000000000000000000 ) ) ;
#43890=VERTEX_POINT ( 'NONE', #30386 ) ;
#43928=EDGE_CURVE ( 'NONE', #33150, #42432, #62544, .T. ) ;
#43945=VERTEX_POINT ( 'NONE', #46997 ) ;
#43959=MANIFOLD_SOLID_BREP ( 'LPattern1[9]', #3582 ) ;
#43965=CIRCLE ( 'NONE', #48474, 24.99999999998784972 ) ;
#43972=VERTEX_POINT ( 'NONE', #41688 ) ;
#43987=FACE_OUTER_BOUND ( 'NONE', #34403, .T. ) ;
#43994=VERTEX_POINT ( 'NONE', #38483 ) ;
#43999=ORIENTED_EDGE ( 'NONE', *, *, #31945, .F. ) ;
#44022=ORIENTED_EDGE ( 'NONE', *, *, #61020, .T. ) ;
#44029=LINE ( 'NONE', #65608, #69301 ) ;
#44035=CIRCLE ( 'NONE', #52079, 0.5000000000000000000 ) ;
#44037=DIRECTION ( 'NONE',  ( 1.000000000000000000, -0.000000000000000000, 0.000000000000000000 ) ) ;
#44040=CARTESIAN_POINT ( 'NONE',  ( 39.00000000000000000, 21.00000000000000000, 16.96999999999999886 ) ) ;
#44050=VECTOR ( 'NONE', #60951, 1000.000000000000114 ) ;
#44058=EDGE_CURVE ( 'NONE', #16445, #26978, #44709, .T. ) ;
#44059=AXIS2_PLACEMENT_3D ( 'NONE', #41418, #24813, #67602 ) ;
#44080=CARTESIAN_POINT ( 'NONE',  ( 8.900000000000002132, 21.00000000000000000, -18.00000000000000355 ) ) ;
#44082=ORIENTED_EDGE ( 'NONE', *, *, #49365, .T. ) ;
#44090=EDGE_CURVE ( 'NONE', #30799, #6900, #58267, .T. ) ;
#44107=ORIENTED_EDGE ( 'NONE', *, *, #68261, .F. ) ;
#44111=DIRECTION ( 'NONE',  ( -1.000000000000000000, 0.000000000000000000, 0.000000000000000000 ) ) ;
#44121=DIRECTION ( 'NONE',  ( 0.000000000000000000, 0.000000000000000000, 1.000000000000000000 ) ) ;
#44123=DIRECTION ( 'NONE',  ( 1.000000000000000000, -0.000000000000000000, 0.000000000000000000 ) ) ;
#44132=EDGE_CURVE ( 'NONE', #27390, #21280, #16476, .T. ) ;
#44135=DIRECTION ( 'NONE',  ( 1.000000000000000000, 0.000000000000000000, 0.000000000000000000 ) ) ;
#44146=ORIENTED_EDGE ( 'NONE', *, *, #56202, .T. ) ;
#44156=FACE_OUTER_BOUND ( 'NONE', #42643, .T. ) ;
#44181=MANIFOLD_SOLID_BREP ( 'LPattern1[2]', #47640 ) ;
#44182=DIRECTION ( 'NONE',  ( 0.000000000000000000, 0.000000000000000000, -1.000000000000000000 ) ) ;
#44187=ORIENTED_EDGE ( 'NONE', *, *, #28333, .F. ) ;
#44196=VERTEX_POINT ( 'NONE', #14027 ) ;
#44203=DIRECTION ( 'NONE',  ( 0.000000000000000000, 1.000000000000000000, -0.000000000000000000 ) ) ;
#44206=VERTEX_POINT ( 'NONE', #41957 ) ;
#44210=DIRECTION ( 'NONE',  ( 0.000000000000000000, 0.000000000000000000, -1.000000000000000000 ) ) ;
#44218=DIRECTION ( 'NONE',  ( 0.000000000000000000, -1.000000000000000000, 0.000000000000000000 ) ) ;
#44222=DIRECTION ( 'NONE',  ( -0.000000000000000000, -0.7071067811865474617, 0.7071067811865474617 ) ) ;
#44227=ORIENTED_EDGE ( 'NONE', *, *, #2896, .F. ) ;
#44242=VERTEX_POINT ( 'NONE', #3772 ) ;
#44246=ORIENTED_EDGE ( 'NONE', *, *, #28569, .F. ) ;
#44248=CIRCLE ( 'NONE', #13758, 24.99999999998784972 ) ;
#44252=CARTESIAN_POINT ( 'NONE',  ( 35.89999999999999858, -0.2000000000089119934, -8.913009219568841313E-12 ) ) ;
#44270=EDGE_CURVE ( 'NONE', #24121, #32538, #32172, .T. ) ;
#44271=CARTESIAN_POINT ( 'NONE',  ( 25.90000000000000213, -21.00000000000000000, 13.86939075806900057 ) ) ;
#44273=CARTESIAN_POINT ( 'NONE',  ( 11.90000000000000036, -21.00000000000000000, 13.86939075806900057 ) ) ;
#44281=( NAMED_UNIT ( * ) SI_UNIT ( $, .STERADIAN. ) SOLID_ANGLE_UNIT ( ) );
#44288=CYLINDRICAL_SURFACE ( 'NONE', #61922, 24.99999999998794920 ) ;
#44310=ORIENTED_EDGE ( 'NONE', *, *, #18867, .F. ) ;
#44315=LINE ( 'NONE', #51024, #54525 ) ;
#44316=VERTEX_POINT ( 'NONE', #47611 ) ;
#44319=LINE ( 'NONE', #33720, #4796 ) ;
#44325=CYLINDRICAL_SURFACE ( 'NONE', #33275, 24.99999999998784972 ) ;
#44327=VECTOR ( 'NONE', #43333, 1000.000000000000000 ) ;
#44331=VERTEX_POINT ( 'NONE', #69870 ) ;
#44341=ORIENTED_EDGE ( 'NONE', *, *, #39356, .T. ) ;
#44345=DIRECTION ( 'NONE',  ( -1.000000000000000000, 0.000000000000000000, 0.000000000000000000 ) ) ;
#44352=VECTOR ( 'NONE', #21862, 1000.000000000000000 ) ;
#44357=DIRECTION ( 'NONE',  ( 0.000000000000000000, -1.000000000000000000, 0.000000000000000000 ) ) ;
#44367=FACE_OUTER_BOUND ( 'NONE', #61968, .T. ) ;
#44375=PLANE ( 'NONE',  #35769 ) ;
#44385=VECTOR ( 'NONE', #9649, 1000.000000000000000 ) ;
#44395=DIRECTION ( 'NONE',  ( 1.000000000000000000, 0.000000000000000000, 0.000000000000000000 ) ) ;
#44406=MANIFOLD_SOLID_BREP ( 'LPattern1[24]', #2453 ) ;
#44409=CARTESIAN_POINT ( 'NONE',  ( 49.00000000000000000, -0.2000000000089119934, -8.913009219568841313E-12 ) ) ;
#44426=EDGE_CURVE ( 'NONE', #38926, #68454, #33085, .T. ) ;
#44432=AXIS2_PLACEMENT_3D ( 'NONE', #55866, #19431, #23346 ) ;
#44436=LINE ( 'NONE', #50457, #13933 ) ;
#44444=DIRECTION ( 'NONE',  ( 0.000000000000000000, -1.000000000000000000, 0.000000000000000000 ) ) ;
#44452=CARTESIAN_POINT ( 'NONE',  ( 35.89999999999999858, -21.00000000000000000, 13.86939075806900057 ) ) ;
#44457=DIRECTION ( 'NONE',  ( 0.000000000000000000, 0.000000000000000000, -1.000000000000000000 ) ) ;
#44468=PLANE ( 'NONE',  #12978 ) ;
#44474=ORIENTED_EDGE ( 'NONE', *, *, #5137, .F. ) ;
#44475=ADVANCED_FACE ( 'NONE', ( #56733 ), #26571, .F. ) ;
#44476=DIRECTION ( 'NONE',  ( 0.000000000000000000, 0.000000000000000000, 1.000000000000000000 ) ) ;
#44482=ORIENTED_EDGE ( 'NONE', *, *, #6442, .T. ) ;
#44485=VERTEX_POINT ( 'NONE', #45774 ) ;
#44494=DIRECTION ( 'NONE',  ( 1.000000000000000000, -0.000000000000000000, 0.000000000000000000 ) ) ;
#44497=COLOUR_RGB ( '', 0.72549020, 0.75294118, 0.79215686) ;
#44499=ORIENTED_EDGE ( 'NONE', *, *, #62848, .F. ) ;
#44502=ORIENTED_EDGE ( 'NONE', *, *, #6497, .F. ) ;
#44505=CARTESIAN_POINT ( 'NONE',  ( 40.90000000000000568, 20.60000000000000142, -13.86939075806900057 ) ) ;
#44513=LINE ( 'NONE', #11312, #16171 ) ;
#44521=LINE ( 'NONE', #50878, #56654 ) ;
#44528=EDGE_CURVE ( 'NONE', #40439, #48107, #30225, .T. ) ;
#44535=ORIENTED_EDGE ( 'NONE', *, *, #27887, .F. ) ;
#44541=AXIS2_PLACEMENT_3D ( 'NONE', #944, #43007, #47972 ) ;
#44546=ORIENTED_EDGE ( 'NONE', *, *, #68261, .T. ) ;
#44547=DIRECTION ( 'NONE',  ( -1.000000000000000000, 0.000000000000000000, 0.000000000000000000 ) ) ;
#44548=CARTESIAN_POINT ( 'NONE',  ( 39.00000000000000000, 0.000000000000000000, 3.500000000000000000 ) ) ;
#44550=ADVANCED_FACE ( 'NONE', ( #35499 ), #51077, .F. ) ;
#44556=DIRECTION ( 'NONE',  ( 1.000000000000000000, -0.000000000000000000, 0.000000000000000000 ) ) ;
#44590=CARTESIAN_POINT ( 'NONE',  ( 41.09999999999999432, -21.00000000000000000, -13.86939075806900057 ) ) ;
#44591=ORIENTED_EDGE ( 'NONE', *, *, #39315, .T. ) ;
#44597=ORIENTED_EDGE ( 'NONE', *, *, #7274, .F. ) ;
#44598=ORIENTED_EDGE ( 'NONE', *, *, #2801, .F. ) ;
#44604=CARTESIAN_POINT ( 'NONE',  ( 41.09999999999999432, -14.06939075806901940, -20.80000000000000426 ) ) ;
#44605=EDGE_LOOP ( 'NONE', ( #46492, #42475, #64114, #57058 ) ) ;
#44610=LINE ( 'NONE', #44273, #30617 ) ;
#44614=FACE_OUTER_BOUND ( 'NONE', #1107, .T. ) ;
#44618=ORIENTED_EDGE ( 'NONE', *, *, #39862, .F. ) ;
#44637=ORIENTED_EDGE ( 'NONE', *, *, #22324, .F. ) ;
#44638=MANIFOLD_SOLID_BREP ( 'LPattern1[14]', #52131 ) ;
#44684=DIRECTION ( 'NONE',  ( -1.000000000000000000, 0.000000000000000000, 0.000000000000000000 ) ) ;
#44692=EDGE_LOOP ( 'NONE', ( #20896, #49820 ) ) ;
#44695=CIRCLE ( 'NONE', #9707, 5.000000000000000000 ) ;
#44700=ADVANCED_FACE ( 'NONE', ( #15007 ), #36565, .F. ) ;
#44708=ORIENTED_EDGE ( 'NONE', *, *, #67747, .F. ) ;
#44709=CIRCLE ( 'NONE', #33428, 24.99999999998784972 ) ;
#44714=LINE ( 'NONE', #18199, #38809 ) ;
#44722=COLOUR_RGB ( '', 0.40784314, 0.44705882, 0.49803922) ;
#44732=DIRECTION ( 'NONE',  ( -0.000000000000000000, -1.000000000000000000, 0.000000000000000000 ) ) ;
#44750=CARTESIAN_POINT ( 'NONE',  ( 39.90000000000000568, -0.2000000000000000111, 0.000000000000000000 ) ) ;
#44760=ORIENTED_EDGE ( 'NONE', *, *, #54891, .T. ) ;
#44767=LINE ( 'NONE', #16538, #19832 ) ;
#44769=AXIS2_PLACEMENT_3D ( 'NONE', #14916, #52048, #52398 ) ;
#44786=CARTESIAN_POINT ( 'NONE',  ( 39.90000000000000568, 16.96999999999999886, -21.00000000000000000 ) ) ;
#44787=VERTEX_POINT ( 'NONE', #6492 ) ;
#44790=VECTOR ( 'NONE', #2704, 1000.000000000000000 ) ;
#44812=CARTESIAN_POINT ( 'NONE',  ( 39.00000000000000000, 21.00000000000000000, 16.96999999999999886 ) ) ;
#44816=DIRECTION ( 'NONE',  ( 1.000000000000000000, 0.000000000000000000, 0.000000000000000000 ) ) ;
#44819=FACE_OUTER_BOUND ( 'NONE', #809, .T. ) ;
#44820=VERTEX_POINT ( 'NONE', #54939 ) ;
#44829=DIRECTION ( 'NONE',  ( 0.000000000000000000, 0.000000000000000000, 1.000000000000000000 ) ) ;
#44844=EDGE_CURVE ( 'NONE', #1369, #30511, #58176, .T. ) ;
#44855=( NAMED_UNIT ( * ) SI_UNIT ( $, .STERADIAN. ) SOLID_ANGLE_UNIT ( ) );
#44863=EDGE_CURVE ( 'NONE', #10779, #20267, #11947, .T. ) ;
#44868=EDGE_CURVE ( 'NONE', #16007, #18237, #30753, .T. ) ;
#44869=EDGE_CURVE ( 'NONE', #23171, #51803, #25808, .T. ) ;
#44871=ORIENTED_EDGE ( 'NONE', *, *, #55239, .F. ) ;
#44877=DIRECTION ( 'NONE',  ( 0.000000000000000000, 0.000000000000000000, -1.000000000000000000 ) ) ;
#44878=MANIFOLD_SOLID_BREP ( 'Move Face1[2]', #45347 ) ;
#44881=AXIS2_PLACEMENT_3D ( 'NONE', #47186, #3694, #9350 ) ;
#44883=ORIENTED_EDGE ( 'NONE', *, *, #60152, .T. ) ;
#44892=VECTOR ( 'NONE', #63866, 1000.000000000000000 ) ;
#44899=EDGE_CURVE ( 'NONE', #8098, #40022, #56305, .T. ) ;
#44905=AXIS2_PLACEMENT_3D ( 'NONE', #49510, #54819, #66457 ) ;
#44952=ORIENTED_EDGE ( 'NONE', *, *, #51097, .T. ) ;
#44971=CARTESIAN_POINT ( 'NONE',  ( 41.09999999999999432, -0.2000000000000000111, 0.000000000000000000 ) ) ;
#44987=ORIENTED_EDGE ( 'NONE', *, *, #28175, .T. ) ;
#45001=CARTESIAN_POINT ( 'NONE',  ( 46.39999999999999858, 33.00000000000000000, -2.750000000000000444 ) ) ;
#45017=EDGE_LOOP ( 'NONE', ( #8205, #24969, #25625, #253 ) ) ;
#45024=CARTESIAN_POINT ( 'NONE',  ( 25.57999999999999829, 0.000000000000000000, 0.000000000000000000 ) ) ;
#45025=CARTESIAN_POINT ( 'NONE',  ( 48.50000000000000000, 0.7500000000000000000, 3.418698582794335028 ) ) ;
#45041=DIRECTION ( 'NONE',  ( 0.000000000000000000, 0.000000000000000000, -1.000000000000000000 ) ) ;
#45044=DIRECTION ( 'NONE',  ( 1.000000000000000000, -0.000000000000000000, 0.000000000000000000 ) ) ;
#45050=AXIS2_PLACEMENT_3D ( 'NONE', #67754, #14719, #25693 ) ;
#45065=DIRECTION ( 'NONE',  ( 0.000000000000000000, 0.000000000000000000, 1.000000000000000000 ) ) ;
#45073=CYLINDRICAL_SURFACE ( 'NONE', #12336, 24.99999999998784972 ) ;
#45077=FACE_OUTER_BOUND ( 'NONE', #47224, .T. ) ;
#45084=LINE ( 'NONE', #34825, #33944 ) ;
#45087=DIRECTION ( 'NONE',  ( 0.000000000000000000, 0.000000000000000000, -1.000000000000000000 ) ) ;
#45089=AXIS2_PLACEMENT_3D ( 'NONE', #51284, #24420, #67560 ) ;
#45096=ORIENTED_EDGE ( 'NONE', *, *, #64441, .F. ) ;
#45104=DIRECTION ( 'NONE',  ( 1.000000000000000000, -0.000000000000000000, 0.000000000000000000 ) ) ;
#45112=CARTESIAN_POINT ( 'NONE',  ( 9.899999999999998579, -14.06939075806900874, 20.80000000000001137 ) ) ;
#45139=EDGE_CURVE ( 'NONE', #14789, #19943, #17944, .T. ) ;
#45140=DIRECTION ( 'NONE',  ( 0.000000000000000000, -0.1499999999999998002, -0.9886859966642594921 ) ) ;
#45165=CARTESIAN_POINT ( 'NONE',  ( 15.89999999999999680, -0.1999999999911430404, -8.864436962241481021E-12 ) ) ;
#45171=FILL_AREA_STYLE_COLOUR ( '', #559 ) ;
#45194=ORIENTED_EDGE ( 'NONE', *, *, #42402, .F. ) ;
#45201=VECTOR ( 'NONE', #11404, 1000.000000000000000 ) ;
#45213=DIRECTION ( 'NONE',  ( 0.000000000000000000, 1.000000000000000000, -0.000000000000000000 ) ) ;
#45214=DIRECTION ( 'NONE',  ( 0.000000000000000000, 0.000000000000000000, 1.000000000000000000 ) ) ;
#45222=CARTESIAN_POINT ( 'NONE',  ( 39.00000000000000000, 0.000000000000000000, 0.000000000000000000 ) ) ;
#45224=CARTESIAN_POINT ( 'NONE',  ( 49.00000000000000000, -0.2000000000089119934, -8.913009219568841313E-12 ) ) ;
#45226=PLANE ( 'NONE',  #34667 ) ;
#45234=DIRECTION ( 'NONE',  ( 0.000000000000000000, 0.000000000000000000, -1.000000000000000000 ) ) ;
#45235=ORIENTED_EDGE ( 'NONE', *, *, #19159, .T. ) ;
#45246=VECTOR ( 'NONE', #31032, 1000.000000000000000 ) ;
#45247=DIRECTION ( 'NONE',  ( -1.000000000000000000, 0.000000000000000000, 0.000000000000000000 ) ) ;
#45256=VERTEX_POINT ( 'NONE', #67788 ) ;
#45302=SURFACE_STYLE_FILL_AREA ( #61925 ) ;
#45318=ORIENTED_EDGE ( 'NONE', *, *, #22469, .T. ) ;
#45321=AXIS2_PLACEMENT_3D ( 'NONE', #46874, #3748, #25320 ) ;
#45324=LINE ( 'NONE', #23073, #29519 ) ;
#45328=EDGE_LOOP ( 'NONE', ( #41388, #37229, #13778, #2878, #19169, #43275, #52996, #40110 ) ) ;
#45339=EDGE_CURVE ( 'NONE', #29653, #32973, #2615, .T. ) ;
#45343=DIRECTION ( 'NONE',  ( 1.000000000000000000, 0.000000000000000000, 0.000000000000000000 ) ) ;
#45344=CIRCLE ( 'NONE', #11443, 24.99999999998789946 ) ;
#45347=CLOSED_SHELL ( 'NONE', ( #37571, #56585, #16852, #48899, #51633, #62184, #67302, #8842, #8714, #32774, #25481, #3740, #32070, #19414, #50484, #11218, #22078, #34910, #64908, #50689, #69004, #20021, #53405, #29641, #13829, #28575, #37270, #35198, #36460, #22270, #29859, #24718, #49528, #42925, #53588, #56846, #66742, #52988, #3703, #13493 ) ) ;
#45356=DIRECTION ( 'NONE',  ( -1.000000000000000000, 0.000000000000000000, 0.000000000000000000 ) ) ;
#45357=CARTESIAN_POINT ( 'NONE',  ( 8.900000000000002132, 21.00000000000000000, -18.00000000000000355 ) ) ;
#45360=AXIS2_PLACEMENT_3D ( 'NONE', #64413, #10312, #4663 ) ;
#45364=ORIENTED_EDGE ( 'NONE', *, *, #36928, .F. ) ;
#45378=LINE ( 'NONE', #56002, #29420 ) ;
#45379=ORIENTED_EDGE ( 'NONE', *, *, #53762, .F. ) ;
#45389=EDGE_CURVE ( 'NONE', #4520, #68247, #49287, .T. ) ;
#45403=EDGE_CURVE ( 'NONE', #62211, #38554, #41340, .T. ) ;
#45404=DIRECTION ( 'NONE',  ( 1.000000000000000000, -0.000000000000000000, -0.000000000000000000 ) ) ;
#45421=VERTEX_POINT ( 'NONE', #62008 ) ;
#45434=AXIS2_PLACEMENT_3D ( 'NONE', #35579, #13323, #56802 ) ;
#45438=CYLINDRICAL_SURFACE ( 'NONE', #63223, 24.99999999998784972 ) ;
#45444=CARTESIAN_POINT ( 'NONE',  ( 24.90000000000000213, 20.60000000000000142, -13.86939075806900057 ) ) ;
#45448=EDGE_CURVE ( 'NONE', #62779, #5488, #26289, .T. ) ;
#45457=DIRECTION ( 'NONE',  ( -1.000000000000000000, 0.000000000000000000, 0.000000000000000000 ) ) ;
#45467=EDGE_LOOP ( 'NONE', ( #42489, #63072, #24700, #17315, #53843, #8525, #48816, #30702 ) ) ;
#45479=FACE_OUTER_BOUND ( 'NONE', #25647, .T. ) ;
#45487=FACE_OUTER_BOUND ( 'NONE', #6683, .T. ) ;
#45527=ORIENTED_EDGE ( 'NONE', *, *, #43400, .F. ) ;
#45538=DIRECTION ( 'NONE',  ( 0.000000000000000000, 0.000000000000000000, -1.000000000000000000 ) ) ;
#45554=ORIENTED_EDGE ( 'NONE', *, *, #57435, .F. ) ;
#45559=DIRECTION ( 'NONE',  ( 0.000000000000000000, 0.000000000000000000, -1.000000000000000000 ) ) ;
#45603=ORIENTED_EDGE ( 'NONE', *, *, #20653, .T. ) ;
#45604=DIRECTION ( 'NONE',  ( 0.000000000000000000, 0.000000000000000000, -1.000000000000000000 ) ) ;
#45608=VECTOR ( 'NONE', #50317, 1000.000000000000000 ) ;
#45609=AXIS2_PLACEMENT_3D ( 'NONE', #69252, #20808, #9872 ) ;
#45620=DIRECTION ( 'NONE',  ( 0.000000000000000000, 0.000000000000000000, 1.000000000000000000 ) ) ;
#45630=ORIENTED_EDGE ( 'NONE', *, *, #60975, .F. ) ;
#45636=ORIENTED_EDGE ( 'NONE', *, *, #41431, .F. ) ;
#45640=( GEOMETRIC_REPRESENTATION_CONTEXT ( 3 ) GLOBAL_UNCERTAINTY_ASSIGNED_CONTEXT ( ( #37332 ) ) GLOBAL_UNIT_ASSIGNED_CONTEXT ( ( #67173, #29334, #18736 ) ) REPRESENTATION_CONTEXT ( 'NONE', 'WORKASPACE' ) );
#45641=EDGE_LOOP ( 'NONE', ( #8992, #40586, #33561, #7214 ) ) ;
#45645=CARTESIAN_POINT ( 'NONE',  ( 24.90000000000000213, -14.06939075806900874, 20.80000000000001137 ) ) ;
#45650=DIRECTION ( 'NONE',  ( 0.000000000000000000, 0.000000000000000000, -1.000000000000000000 ) ) ;
#45651=DIRECTION ( 'NONE',  ( -1.000000000000000000, 0.000000000000000000, 0.000000000000000000 ) ) ;
#45663=DIRECTION ( 'NONE',  ( -0.000000000000000000, -1.000000000000000000, 0.000000000000000000 ) ) ;
#45667=DIRECTION ( 'NONE',  ( -1.000000000000000000, 0.000000000000000000, 0.000000000000000000 ) ) ;
#45682=EDGE_CURVE ( 'NONE', #8950, #69402, #62278, .T. ) ;
#45683=SURFACE_SIDE_STYLE ('',( #40020 ) ) ;
#45703=CIRCLE ( 'NONE', #46872, 25.39999999999999858 ) ;
#45705=LINE ( 'NONE', #45357, #57570 ) ;
#45706=PLANE ( 'NONE',  #5248 ) ;
#45707=EDGE_CURVE ( 'NONE', #4332, #856, #24463, .T. ) ;
#45716=VERTEX_POINT ( 'NONE', #29749 ) ;
#45717=CARTESIAN_POINT ( 'NONE',  ( 9.899999999999998579, -21.00000000000000000, 13.86939075806900057 ) ) ;
#45722=EDGE_LOOP ( 'NONE', ( #42866, #11283, #35111, #25614 ) ) ;
#45732=VERTEX_POINT ( 'NONE', #19495 ) ;
#45738=LINE ( 'NONE', #35129, #65131 ) ;
#45761=DIRECTION ( 'NONE',  ( 0.000000000000000000, -1.000000000000000000, 0.000000000000000000 ) ) ;
#45763=EDGE_LOOP ( 'NONE', ( #11867, #31312, #42118, #24431 ) ) ;
#45766=CIRCLE ( 'NONE', #50261, 24.99999999998784972 ) ;
#45774=CARTESIAN_POINT ( 'NONE',  ( 41.09999999999999432, 20.60000000000000142, -13.86939075806900057 ) ) ;
#45787=EDGE_CURVE ( 'NONE', #60403, #42593, #4316, .T. ) ;
#45796=ORIENTED_EDGE ( 'NONE', *, *, #27692, .T. ) ;
#45806=CARTESIAN_POINT ( 'NONE',  ( 35.89999999999999858, -0.000000000000000000, 20.80000000000000426 ) ) ;
#45813=EDGE_LOOP ( 'NONE', ( #52796, #21887, #14462, #20227 ) ) ;
#45820=ORIENTED_EDGE ( 'NONE', *, *, #51267, .F. ) ;
#45827=CARTESIAN_POINT ( 'NONE',  ( 41.09999999999999432, -21.00000000000000000, 14.57806571531351914 ) ) ;
#45839=CARTESIAN_POINT ( 'NONE',  ( 39.90000000000000568, 0.000000000000000000, 3.447897592003593022E-15 ) ) ;
#45842=SURFACE_STYLE_FILL_AREA ( #29926 ) ;
#45856=EDGE_CURVE ( 'NONE', #25494, #62779, #43679, .T. ) ;
#45858=AXIS2_PLACEMENT_3D ( 'NONE', #3885, #57967, #68226 ) ;
#45859=VECTOR ( 'NONE', #66084, 1000.000000000000000 ) ;
#45863=AXIS2_PLACEMENT_3D ( 'NONE', #51109, #50754, #35180 ) ;
#45865=CARTESIAN_POINT ( 'NONE',  ( 34.89999999999999858, 20.60000000000000142, -13.86939075806900057 ) ) ;
#45866=EDGE_LOOP ( 'NONE', ( #59388, #40053 ) ) ;
#45869=ORIENTED_EDGE ( 'NONE', *, *, #46738, .F. ) ;
#45880=CARTESIAN_POINT ( 'NONE',  ( 40.90000000000000568, -21.00000000000000000, -16.96999999999999886 ) ) ;
#45895=ORIENTED_EDGE ( 'NONE', *, *, #21381, .F. ) ;
#45897=DIRECTION ( 'NONE',  ( 1.000000000000000000, -0.000000000000000000, 0.000000000000000000 ) ) ;
#45918=AXIS2_PLACEMENT_3D ( 'NONE', #22775, #53934, #32355 ) ;
#45921=VECTOR ( 'NONE', #67600, 1000.000000000000000 ) ;
#45925=VERTEX_POINT ( 'NONE', #28282 ) ;
#45946=LINE ( 'NONE', #50199, #13009 ) ;
#45950=DIRECTION ( 'NONE',  ( 0.000000000000000000, 0.000000000000000000, 1.000000000000000000 ) ) ;
#45976=DIRECTION ( 'NONE',  ( 0.000000000000000000, 0.000000000000000000, -1.000000000000000000 ) ) ;
#45980=ORIENTED_EDGE ( 'NONE', *, *, #60608, .T. ) ;
#45997=EDGE_CURVE ( 'NONE', #30310, #68810, #27945, .T. ) ;
#46001=EDGE_LOOP ( 'NONE', ( #4610, #14116, #43827, #36240, #65309, #5878 ) ) ;
#46011=PLANE ( 'NONE',  #27424 ) ;
#46022=CARTESIAN_POINT ( 'NONE',  ( 31.89999999999999858, 0.000000000000000000, 0.000000000000000000 ) ) ;
#46025=VECTOR ( 'NONE', #46586, 1000.000000000000000 ) ;
#46028=CARTESIAN_POINT ( 'NONE',  ( 39.00000000000000000, 16.96999999999999886, 21.00000000000000000 ) ) ;
#46036=DIRECTION ( 'NONE',  ( 1.000000000000000000, -0.000000000000000000, 0.000000000000000000 ) ) ;
#46040=CARTESIAN_POINT ( 'NONE',  ( 25.57999999999999829, 0.000000000000000000, 2.458500000000000796 ) ) ;
#46041=CARTESIAN_POINT ( 'NONE',  ( 49.00000000000000000, -21.00000000000000000, 13.86939075806900057 ) ) ;
#46052=MECHANICAL_DESIGN_GEOMETRIC_PRESENTATION_REPRESENTATION('',(#49448),#64159);
#46058=ADVANCED_FACE ( 'NONE', ( #66459, #67859 ), #45226, .T. ) ;
#46067=CARTESIAN_POINT ( 'NONE',  ( 35.89999999999999858, 0.000000000000000000, 0.000000000000000000 ) ) ;
#46090=ORIENTED_EDGE ( 'NONE', *, *, #42893, .T. ) ;
#46108=EDGE_LOOP ( 'NONE', ( #27650, #60588, #40758, #39374, #38491, #65535, #24703, #8049 ) ) ;
#46112=DIRECTION ( 'NONE',  ( 0.000000000000000000, 1.000000000000000000, -0.000000000000000000 ) ) ;
#46119=ORIENTED_EDGE ( 'NONE', *, *, #12286, .T. ) ;
#46128=ORIENTED_EDGE ( 'NONE', *, *, #16645, .T. ) ;
#46129=CARTESIAN_POINT ( 'NONE',  ( 24.90000000000000213, 20.60000000000000142, 13.86939075806900057 ) ) ;
#46132=CARTESIAN_POINT ( 'NONE',  ( 25.57999999999999829, 3.010794155703768650E-16, -2.458500000000000796 ) ) ;
#46133=CARTESIAN_POINT ( 'NONE',  ( 18.89999999999999858, 0.000000000000000000, 1.077467997501122647E-15 ) ) ;
#46143=CARTESIAN_POINT ( 'NONE',  ( 41.09999999999999432, 20.60000000000000142, 13.86939075806900057 ) ) ;
#46147=LINE ( 'NONE', #67716, #40916 ) ;
#46151=EDGE_CURVE ( 'NONE', #47575, #21656, #51602, .T. ) ;
#46154=VECTOR ( 'NONE', #68438, 1000.000000000000000 ) ;
#46159=DIRECTION ( 'NONE',  ( 0.000000000000000000, 1.000000000000000000, 0.000000000000000000 ) ) ;
#46160=DIRECTION ( 'NONE',  ( -1.000000000000000000, 0.000000000000000000, 0.000000000000000000 ) ) ;
#46180=VERTEX_POINT ( 'NONE', #14472 ) ;
#46184=CARTESIAN_POINT ( 'NONE',  ( 10.00000000000000000, -18.00000000000000355, 21.00000000000000000 ) ) ;
#46191=CARTESIAN_POINT ( 'NONE',  ( 23.90000000000000213, -21.00000000000000000, 13.86939075806900057 ) ) ;
#46200=VECTOR ( 'NONE', #56586, 1000.000000000000000 ) ;
#46201=EDGE_CURVE ( 'NONE', #44787, #33655, #47339, .T. ) ;
#46203=DIRECTION ( 'NONE',  ( 1.000000000000000000, -0.000000000000000000, 0.000000000000000000 ) ) ;
#46214=DIRECTION ( 'NONE',  ( -1.000000000000000000, 0.000000000000000000, 0.000000000000000000 ) ) ;
#46218=EDGE_CURVE ( 'NONE', #66965, #53158, #25078, .T. ) ;
#46228=DIRECTION ( 'NONE',  ( -0.7071067811865476838, 0.4999999999999997780, -0.4999999999999997780 ) ) ;
#46230=AXIS2_PLACEMENT_3D ( 'NONE', #28937, #7362, #66764 ) ;
#46238=ORIENTED_EDGE ( 'NONE', *, *, #20276, .F. ) ;
#46240=EDGE_CURVE ( 'NONE', #46180, #10693, #50471, .T. ) ;
#46257=LINE ( 'NONE', #8784, #37645 ) ;
#46259=EDGE_CURVE ( 'NONE', #30300, #17757, #48278, .T. ) ;
#46265=DIRECTION ( 'NONE',  ( 0.000000000000000000, 0.000000000000000000, 1.000000000000000000 ) ) ;
#46266=ORIENTED_EDGE ( 'NONE', *, *, #43131, .T. ) ;
#46269=DIRECTION ( 'NONE',  ( -1.000000000000000000, 0.000000000000000000, 0.000000000000000000 ) ) ;
#46276=SURFACE_STYLE_FILL_AREA ( #57242 ) ;
#46277=ORIENTED_EDGE ( 'NONE', *, *, #11202, .T. ) ;
#46288=CARTESIAN_POINT ( 'NONE',  ( 49.00000000000000000, -0.2000000000089119934, -8.913009219568841313E-12 ) ) ;
#46305=CARTESIAN_POINT ( 'NONE',  ( 20.90000000000000213, 20.60000000000000142, 13.86939075806900057 ) ) ;
#46306=EDGE_CURVE ( 'NONE', #58955, #1307, #14397, .T. ) ;
#46307=EDGE_CURVE ( 'NONE', #29826, #29082, #53935, .T. ) ;
#46329=DIRECTION ( 'NONE',  ( -1.000000000000000000, 0.000000000000000000, 0.000000000000000000 ) ) ;
#46330=CARTESIAN_POINT ( 'NONE',  ( 9.899999999999998579, -0.1999999999911795112, 8.826273045769999343E-12 ) ) ;
#46334=AXIS2_PLACEMENT_3D ( 'NONE', #29902, #3390, #30267 ) ;
#46336=FACE_OUTER_BOUND ( 'NONE', #12747, .T. ) ;
#46352=ORIENTED_EDGE ( 'NONE', *, *, #37248, .T. ) ;
#46359=CARTESIAN_POINT ( 'NONE',  ( 55.00000000000000000, 16.96999999999999886, -21.00000000000000000 ) ) ;
#46372=ORIENTED_EDGE ( 'NONE', *, *, #2533, .T. ) ;
#46381=AXIS2_PLACEMENT_3D ( 'NONE', #63617, #15175, #5269 ) ;
#46402=CARTESIAN_POINT ( 'NONE',  ( 41.09999999999999432, 20.60000000000000142, -13.86939075806900057 ) ) ;
#46431=ADVANCED_FACE ( 'NONE', ( #32127 ), #644, .F. ) ;
#46440=ORIENTED_EDGE ( 'NONE', *, *, #13277, .T. ) ;
#46458=VERTEX_POINT ( 'NONE', #24288 ) ;
#46461=AXIS2_PLACEMENT_3D ( 'NONE', #42809, #43153, #53433 ) ;
#46465=CARTESIAN_POINT ( 'NONE',  ( 40.90000000000000568, -0.2000000000089119934, -8.913009219568841313E-12 ) ) ;
#46484=DIRECTION ( 'NONE',  ( 1.000000000000000000, 0.000000000000000000, 0.000000000000000000 ) ) ;
#46492=ORIENTED_EDGE ( 'NONE', *, *, #20559, .T. ) ;
#46510=DIRECTION ( 'NONE',  ( -1.000000000000000000, 0.000000000000000000, 0.000000000000000000 ) ) ;
#46512=VERTEX_POINT ( 'NONE', #34528 ) ;
#46514=AXIS2_PLACEMENT_3D ( 'NONE', #67008, #34827, #51100 ) ;
#46515=EDGE_CURVE ( 'NONE', #26452, #19555, #4269, .T. ) ;
#46519=UNCERTAINTY_MEASURE_WITH_UNIT (LENGTH_MEASURE( 1.000000000000000082E-05 ), #57798, 'distance_accuracy_value', 'NONE');
#46525=EDGE_LOOP ( 'NONE', ( #8112, #59050, #69052, #52268 ) ) ;
#46527=AXIS2_PLACEMENT_3D ( 'NONE', #27189, #64324, #5282 ) ;
#46533=PLANE ( 'NONE',  #40296 ) ;
#46534=LINE ( 'NONE', #68109, #17794 ) ;
#46540=CARTESIAN_POINT ( 'NONE',  ( -6.661338147750939243E-15, 20.50000000000000000, -17.79289321881346808 ) ) ;
#46563=SURFACE_STYLE_USAGE ( .BOTH. , #24307 ) ;
#46572=LINE ( 'NONE', #63195, #54857 ) ;
#46578=EDGE_LOOP ( 'NONE', ( #58064, #47495, #37470, #47461 ) ) ;
#46583=ORIENTED_EDGE ( 'NONE', *, *, #10665, .T. ) ;
#46586=DIRECTION ( 'NONE',  ( -1.000000000000000000, 0.000000000000000000, 0.000000000000000000 ) ) ;
#46594=DIRECTION ( 'NONE',  ( 0.000000000000000000, 0.000000000000000000, -1.000000000000000000 ) ) ;
#46597=EDGE_LOOP ( 'NONE', ( #16620, #2323, #38348, #59675 ) ) ;
#46601=CARTESIAN_POINT ( 'NONE',  ( 40.90000000000000568, 21.00000000000000000, -16.96999999999999886 ) ) ;
#46647=LINE ( 'NONE', #8106, #34101 ) ;
#46650=DIRECTION ( 'NONE',  ( 0.000000000000000000, -0.7071067811865474617, 0.7071067811865474617 ) ) ;
#46655=CIRCLE ( 'NONE', #12764, 2.458500000000000796 ) ;
#46660=ORIENTED_EDGE ( 'NONE', *, *, #62092, .F. ) ;
#46662=ORIENTED_EDGE ( 'NONE', *, *, #62706, .F. ) ;
#46663=ORIENTED_EDGE ( 'NONE', *, *, #31439, .T. ) ;
#46665=CIRCLE ( 'NONE', #59094, 0.5000000000000000000 ) ;
#46667=LINE ( 'NONE', #25822, #61499 ) ;
#46668=CARTESIAN_POINT ( 'NONE',  ( 39.00000000000000000, -16.96999999999999886, 21.00000000000000000 ) ) ;
#46670=ORIENTED_EDGE ( 'NONE', *, *, #33124, .F. ) ;
#46677=AXIS2_PLACEMENT_3D ( 'NONE', #17198, #38770, #1292 ) ;
#46686=CIRCLE ( 'NONE', #61351, 24.99999999998784972 ) ;
#46687=ORIENTED_EDGE ( 'NONE', *, *, #54420, .T. ) ;
#46690=ORIENTED_EDGE ( 'NONE', *, *, #67848, .F. ) ;
#46693=DIRECTION ( 'NONE',  ( -1.000000000000000000, 0.000000000000000000, 0.000000000000000000 ) ) ;
#46701=DIRECTION ( 'NONE',  ( 0.000000000000000000, 0.000000000000000000, -1.000000000000000000 ) ) ;
#46706=DIRECTION ( 'NONE',  ( 0.000000000000000000, 0.000000000000000000, -1.000000000000000000 ) ) ;
#46715=CARTESIAN_POINT ( 'NONE',  ( 39.00000000000000000, 14.08845687959340331, 21.00000000000000000 ) ) ;
#46719=APPLICATION_CONTEXT ( 'automotive_design' ) ;
#46721=VERTEX_POINT ( 'NONE', #59946 ) ;
#46722=DIRECTION ( 'NONE',  ( 1.000000000000000000, -0.000000000000000000, 0.000000000000000000 ) ) ;
#46724=ORIENTED_EDGE ( 'NONE', *, *, #28354, .T. ) ;
#46725=CARTESIAN_POINT ( 'NONE',  ( 31.89999999999999858, 20.60000000000000142, 2.585923194002694273E-15 ) ) ;
#46726=AXIS2_PLACEMENT_3D ( 'NONE', #31807, #44123, #10571 ) ;
#46738=EDGE_CURVE ( 'NONE', #2257, #51399, #38724, .T. ) ;
#46743=ORIENTED_EDGE ( 'NONE', *, *, #10050, .T. ) ;
#46747=CARTESIAN_POINT ( 'NONE',  ( 9.900000000000000355, -18.00000000000000355, -21.00000000000000000 ) ) ;
#46750=CYLINDRICAL_SURFACE ( 'NONE', #56917, 24.99999999998789946 ) ;
#46751=LINE ( 'NONE', #20930, #32853 ) ;
#46754=FACE_OUTER_BOUND ( 'NONE', #21601, .T. ) ;
#46768=CARTESIAN_POINT ( 'NONE',  ( 49.00000000000000000, -0.1999999999911795112, 8.826273045769999343E-12 ) ) ;
#46770=ADVANCED_FACE ( 'NONE', ( #42991 ), #60286, .T. ) ;
#46771=VECTOR ( 'NONE', #64584, 1000.000000000000000 ) ;
#46776=ORIENTED_EDGE ( 'NONE', *, *, #43207, .T. ) ;
#46803=DIRECTION ( 'NONE',  ( 0.000000000000000000, 0.000000000000000000, -1.000000000000000000 ) ) ;
#46819=VECTOR ( 'NONE', #11675, 1000.000000000000000 ) ;
#46834=DIRECTION ( 'NONE',  ( 1.000000000000000000, 0.000000000000000000, 0.000000000000000000 ) ) ;
#46840=DIRECTION ( 'NONE',  ( 0.000000000000000000, 0.000000000000000000, -1.000000000000000000 ) ) ;
#46846=EDGE_LOOP ( 'NONE', ( #27485, #31617, #17640, #35079 ) ) ;
#46853=CARTESIAN_POINT ( 'NONE',  ( 12.90000000000000213, -21.00000000000001421, -13.86939075806900945 ) ) ;
#46863=VERTEX_POINT ( 'NONE', #66637 ) ;
#46864=EDGE_LOOP ( 'NONE', ( #69937, #28174, #35082, #19781, #878, #42001, #65459, #67450 ) ) ;
#46869=ORIENTED_EDGE ( 'NONE', *, *, #62848, .T. ) ;
#46872=AXIS2_PLACEMENT_3D ( 'NONE', #49861, #55176, #45234 ) ;
#46874=CARTESIAN_POINT ( 'NONE',  ( 39.90000000000000568, -0.2000000000089119934, -8.913009219568841313E-12 ) ) ;
#46880=( GEOMETRIC_REPRESENTATION_CONTEXT ( 3 ) GLOBAL_UNCERTAINTY_ASSIGNED_CONTEXT ( ( #26717 ) ) GLOBAL_UNIT_ASSIGNED_CONTEXT ( ( #40769, #13191, #40421 ) ) REPRESENTATION_CONTEXT ( 'NONE', 'WORKASPACE' ) );
#46883=DIRECTION ( 'NONE',  ( -0.7071067811865474617, 0.7071067811865474617, 0.000000000000000000 ) ) ;
#46889=SURFACE_SIDE_STYLE ('',( #45842 ) ) ;
#46890=ORIENTED_EDGE ( 'NONE', *, *, #17849, .T. ) ;
#46891=STYLED_ITEM ( 'NONE', ( #29320 ), #43848 ) ;
#46899=DIRECTION ( 'NONE',  ( 0.000000000000000000, 0.000000000000000000, -1.000000000000000000 ) ) ;
#46900=DIRECTION ( 'NONE',  ( 1.000000000000000000, -0.000000000000000000, 0.000000000000000000 ) ) ;
#46905=CARTESIAN_POINT ( 'NONE',  ( 13.90000000000000213, -21.00000000000001421, -13.86939075806900945 ) ) ;
#46908=CARTESIAN_POINT ( 'NONE',  ( 20.90000000000000213, 13.66939075806899240, 20.79999999999999361 ) ) ;
#46919=VECTOR ( 'NONE', #13996, 1000.000000000000000 ) ;
#46936=ORIENTED_EDGE ( 'NONE', *, *, #5858, .T. ) ;
#46941=CYLINDRICAL_SURFACE ( 'NONE', #47427, 24.99999999998784972 ) ;
#46945=EDGE_LOOP ( 'NONE', ( #5836, #10932 ) ) ;
#46953=VERTEX_POINT ( 'NONE', #2633 ) ;
#46969=EDGE_CURVE ( 'NONE', #14942, #21656, #56380, .T. ) ;
#46972=VECTOR ( 'NONE', #5471, 1000.000000000000000 ) ;
#46976=EDGE_CURVE ( 'NONE', #45256, #10779, #60642, .T. ) ;
#46979=VECTOR ( 'NONE', #10279, 1000.000000000000000 ) ;
#46984=FACE_OUTER_BOUND ( 'NONE', #3415, .T. ) ;
#46985=VERTEX_POINT ( 'NONE', #12193 ) ;
#46997=CARTESIAN_POINT ( 'NONE',  ( 27.90000000000000213, 0.000000000000000000, 2.458500000000000796 ) ) ;
#47018=CARTESIAN_POINT ( 'NONE',  ( 20.90000000000000213, -14.06939075806902117, -20.80000000000000426 ) ) ;
#47029=VERTEX_POINT ( 'NONE', #42215 ) ;
#47048=CARTESIAN_POINT ( 'NONE',  ( 9.900000000000000355, 21.00000000000000000, -18.00000000000000355 ) ) ;
#47050=EDGE_CURVE ( 'NONE', #22451, #50321, #48369, .T. ) ;
#47060=ORIENTED_EDGE ( 'NONE', *, *, #2012, .T. ) ;
#47072=PLANE ( 'NONE',  #40707 ) ;
#47079=DIRECTION ( 'NONE',  ( 0.000000000000000000, 0.000000000000000000, -1.000000000000000000 ) ) ;
#47087=ORIENTED_EDGE ( 'NONE', *, *, #46976, .T. ) ;
#47088=LINE ( 'NONE', #68660, #13457 ) ;
#47093=CARTESIAN_POINT ( 'NONE',  ( 36.90000000000000568, -0.1999999999911795112, 8.826273045769999343E-12 ) ) ;
#47100=CARTESIAN_POINT ( 'NONE',  ( 41.09999999999999432, 13.66939075806899950, 20.80000000000000426 ) ) ;
#47103=DIRECTION ( 'NONE',  ( 1.000000000000000000, -0.000000000000000000, 0.000000000000000000 ) ) ;
#47118=CARTESIAN_POINT ( 'NONE',  ( 49.00000000000000000, -0.1999999999911795112, 8.826273045769999343E-12 ) ) ;
#47119=ADVANCED_FACE ( 'NONE', ( #54237 ), #21704, .F. ) ;
#47120=DIRECTION ( 'NONE',  ( -1.000000000000000000, 0.000000000000000000, 0.000000000000000000 ) ) ;
#47129=VECTOR ( 'NONE', #52678, 1000.000000000000000 ) ;
#47139=AXIS2_PLACEMENT_3D ( 'NONE', #10463, #5172, #37689 ) ;
#47148=ORIENTED_EDGE ( 'NONE', *, *, #20268, .F. ) ;
#47158=EDGE_LOOP ( 'NONE', ( #45980, #32227, #55888, #32628 ) ) ;
#47163=ORIENTED_EDGE ( 'NONE', *, *, #3839, .F. ) ;
#47164=ADVANCED_FACE ( 'NONE', ( #47869 ), #37975, .F. ) ;
#47171=DIRECTION ( 'NONE',  ( 0.000000000000000000, 0.000000000000000000, -1.000000000000000000 ) ) ;
#47174=CARTESIAN_POINT ( 'NONE',  ( 34.89999999999999858, -14.06939075806900163, -20.80000000000000426 ) ) ;
#47186=CARTESIAN_POINT ( 'NONE',  ( 41.09999999999999432, -0.2000000000089119934, -8.913009219568841313E-12 ) ) ;
#47193=DIRECTION ( 'NONE',  ( 0.000000000000000000, 0.000000000000000000, 1.000000000000000000 ) ) ;
#47203=CARTESIAN_POINT ( 'NONE',  ( 21.90000000000000213, 0.000000000000000000, 1.508455196501571824E-15 ) ) ;
#47214=VECTOR ( 'NONE', #45065, 1000.000000000000000 ) ;
#47215=EDGE_CURVE ( 'NONE', #7152, #11562, #24684, .T. ) ;
#47218=CARTESIAN_POINT ( 'NONE',  ( 39.00000000000000000, 21.00000000000000000, -13.98999642601811999 ) ) ;
#47224=EDGE_LOOP ( 'NONE', ( #44597, #43468, #34069, #67722, #2207, #64628, #15276, #22285 ) ) ;
#47238=UNCERTAINTY_MEASURE_WITH_UNIT (LENGTH_MEASURE( 1.000000000000000082E-05 ), #41232, 'distance_accuracy_value', 'NONE');
#47245=CARTESIAN_POINT ( 'NONE',  ( 38.90000000000000568, 3.010794155703768650E-16, -2.458500000000000796 ) ) ;
#47246=EDGE_LOOP ( 'NONE', ( #68820, #50091, #26054, #49495, #426, #37163, #29702, #62787 ) ) ;
#47250=ADVANCED_FACE ( 'NONE', ( #55264 ), #44288, .T. ) ;
#47251=EDGE_CURVE ( 'NONE', #64694, #67710, #18111, .T. ) ;
#47253=FACE_OUTER_BOUND ( 'NONE', #3769, .T. ) ;
#47296=ORIENTED_EDGE ( 'NONE', *, *, #57472, .F. ) ;
#47307=ORIENTED_EDGE ( 'NONE', *, *, #69856, .T. ) ;
#47321=EDGE_CURVE ( 'NONE', #4210, #36995, #28074, .T. ) ;
#47324=EDGE_CURVE ( 'NONE', #47809, #10522, #55175, .T. ) ;
#47334=PLANE ( 'NONE',  #11699 ) ;
#47339=LINE ( 'NONE', #4569, #62955 ) ;
#47340=PLANE ( 'NONE',  #21566 ) ;
#47346=PRESENTATION_STYLE_ASSIGNMENT (( #52673 ) ) ;
#47353=LINE ( 'NONE', #15188, #4055 ) ;
#47357=ORIENTED_EDGE ( 'NONE', *, *, #26527, .F. ) ;
#47372=EDGE_CURVE ( 'NONE', #34850, #14942, #4374, .T. ) ;
#47374=CARTESIAN_POINT ( 'NONE',  ( 8.900000000000005684, -0.1999999999911430404, -8.864436962241481021E-12 ) ) ;
#47383=ORIENTED_EDGE ( 'NONE', *, *, #66898, .F. ) ;
#47391=DIRECTION ( 'NONE',  ( 0.000000000000000000, -1.000000000000000000, 0.000000000000000000 ) ) ;
#47410=DIRECTION ( 'NONE',  ( -1.000000000000000000, 0.000000000000000000, 0.000000000000000000 ) ) ;
#47414=DIRECTION ( 'NONE',  ( 0.000000000000000000, 0.000000000000000000, -1.000000000000000000 ) ) ;
#47419=DIRECTION ( 'NONE',  ( 0.000000000000000000, -1.000000000000000000, 0.000000000000000000 ) ) ;
#47427=AXIS2_PLACEMENT_3D ( 'NONE', #68522, #26089, #20079 ) ;
#47432=CARTESIAN_POINT ( 'NONE',  ( 55.00000000000000000, -21.00000000000000000, 16.96999999999999886 ) ) ;
#47447=ORIENTED_EDGE ( 'NONE', *, *, #13703, .T. ) ;
#47461=ORIENTED_EDGE ( 'NONE', *, *, #67756, .F. ) ;
#47464=EDGE_CURVE ( 'NONE', #45716, #7560, #8196, .T. ) ;
#47467=DIRECTION ( 'NONE',  ( -1.000000000000000000, 0.000000000000000000, 0.000000000000000000 ) ) ;
#47477=CIRCLE ( 'NONE', #30513, 2.458500000000000796 ) ;
#47482=LINE ( 'NONE', #58803, #2664 ) ;
#47484=VERTEX_POINT ( 'NONE', #47702 ) ;
#47487=CIRCLE ( 'NONE', #6835, 24.99999999998784972 ) ;
#47492=EDGE_LOOP ( 'NONE', ( #36279, #33233, #22083, #40423 ) ) ;
#47495=ORIENTED_EDGE ( 'NONE', *, *, #29111, .T. ) ;
#47497=CIRCLE ( 'NONE', #12437, 24.99999999998789946 ) ;
#47511=ADVANCED_FACE ( 'NONE', ( #26486 ), #21526, .F. ) ;
#47513=FACE_OUTER_BOUND ( 'NONE', #57578, .T. ) ;
#47518=CARTESIAN_POINT ( 'NONE',  ( 49.00000000000000000, 13.66939075806899950, 20.80000000000000426 ) ) ;
#47524=CARTESIAN_POINT ( 'NONE',  ( 12.90000000000000213, 20.60000000000000142, -13.86939075806900057 ) ) ;
#47528=EDGE_CURVE ( 'NONE', #9916, #35535, #66027, .T. ) ;
#47530=SURFACE_SIDE_STYLE ('',( #59189 ) ) ;
#47535=CARTESIAN_POINT ( 'NONE',  ( 38.90000000000000568, 20.60000000000000142, -13.86939075806900057 ) ) ;
#47546=LINE ( 'NONE', #64177, #37960 ) ;
#47550=CARTESIAN_POINT ( 'NONE',  ( 10.00000000000000000, 21.00000000000000000, -18.00000000000000355 ) ) ;
#47553=DIRECTION ( 'NONE',  ( 1.000000000000000000, -0.000000000000000000, 0.000000000000000000 ) ) ;
#47554=ORIENTED_EDGE ( 'NONE', *, *, #203, .F. ) ;
#47555=VECTOR ( 'NONE', #49966, 1000.000000000000000 ) ;
#47559=CARTESIAN_POINT ( 'NONE',  ( 46.39999999999999858, 33.00000000000000000, 0.7500000000000000000 ) ) ;
#47575=VERTEX_POINT ( 'NONE', #48750 ) ;
#47578=VECTOR ( 'NONE', #16739, 1000.000000000000000 ) ;
#47582=DIRECTION ( 'NONE',  ( 0.000000000000000000, -0.1875000000000000000, -0.9822646028438569710 ) ) ;
#47594=PLANE ( 'NONE',  #64311 ) ;
#47599=DIRECTION ( 'NONE',  ( -1.000000000000000000, 0.000000000000000000, 0.000000000000000000 ) ) ;
#47611=CARTESIAN_POINT ( 'NONE',  ( 23.90000000000000213, 20.60000000000000142, 13.86939075806899702 ) ) ;
#47614=ORIENTED_EDGE ( 'NONE', *, *, #10480, .F. ) ;
#47618=DIRECTION ( 'NONE',  ( -1.000000000000000000, 0.000000000000000000, 0.000000000000000000 ) ) ;
#47619=VERTEX_POINT ( 'NONE', #16218 ) ;
#47636=DIRECTION ( 'NONE',  ( -1.000000000000000000, 0.000000000000000000, 0.000000000000000000 ) ) ;
#47637=CARTESIAN_POINT ( 'NONE',  ( 41.09999999999999432, -0.2000000000089119934, 8.909539772616881237E-12 ) ) ;
#47640=CLOSED_SHELL ( 'NONE', ( #17859, #57149, #33231, #4282, #34885, #33761, #20855, #36560, #18101, #17726, #48222, #63603, #52285, #33565, #54005, #49348, #13591, #11472, #4168, #31026, #50055 ) ) ;
#47645=EDGE_LOOP ( 'NONE', ( #32153, #46776, #3309, #62578, #44598, #49719, #42417, #44546 ) ) ;
#47647=CARTESIAN_POINT ( 'NONE',  ( 39.90000000000000568, -21.00000000000000000, -16.96999999999999886 ) ) ;
#47652=CARTESIAN_POINT ( 'NONE',  ( 27.90000000000000213, -21.00000000000000000, 13.86939075806900057 ) ) ;
#47664=DIRECTION ( 'NONE',  ( 0.000000000000000000, 0.000000000000000000, -1.000000000000000000 ) ) ;
#47665=DIRECTION ( 'NONE',  ( -0.000000000000000000, -1.000000000000000000, 0.000000000000000000 ) ) ;
#47669=ADVANCED_FACE ( 'NONE', ( #43427, #27524 ), #2035, .T. ) ;
#47683=SURFACE_SIDE_STYLE ('',( #10204 ) ) ;
#47685=CARTESIAN_POINT ( 'NONE',  ( 39.90000000000000568, 0.000000000000000000, 3.447897592003593022E-15 ) ) ;
#47688=FACE_OUTER_BOUND ( 'NONE', #17211, .T. ) ;
#47690=DIRECTION ( 'NONE',  ( -1.000000000000000000, 0.000000000000000000, 0.000000000000000000 ) ) ;
#47699=ORIENTED_EDGE ( 'NONE', *, *, #57556, .F. ) ;
#47700=DIRECTION ( 'NONE',  ( 1.000000000000000000, 0.000000000000000000, 0.000000000000000000 ) ) ;
#47702=CARTESIAN_POINT ( 'NONE',  ( 0.000000000000000000, 17.79289321881345032, -20.50000000000000000 ) ) ;
#47706=ORIENTED_EDGE ( 'NONE', *, *, #27157, .F. ) ;
#47710=DIRECTION ( 'NONE',  ( 0.000000000000000000, 0.000000000000000000, -1.000000000000000000 ) ) ;
#47711=CARTESIAN_POINT ( 'NONE',  ( 16.89999999999999858, -21.00000000000001421, -13.86939075806900945 ) ) ;
#47723=VECTOR ( 'NONE', #7605, 1000.000000000000000 ) ;
#47724=EDGE_CURVE ( 'NONE', #16791, #13851, #56324, .T. ) ;
#47742=ORIENTED_EDGE ( 'NONE', *, *, #6484, .F. ) ;
#47747=EDGE_LOOP ( 'NONE', ( #31820, #6668, #64984, #69964, #55075, #54350, #3372, #6749 ) ) ;
#47766=PLANE ( 'NONE',  #67319 ) ;
#47768=DIRECTION ( 'NONE',  ( 0.000000000000000000, 0.000000000000000000, -1.000000000000000000 ) ) ;
#47785=ORIENTED_EDGE ( 'NONE', *, *, #27267, .F. ) ;
#47793=EDGE_LOOP ( 'NONE', ( #65227, #18788, #19037, #40931 ) ) ;
#47798=DIRECTION ( 'NONE',  ( 0.000000000000000000, 1.000000000000000000, -0.000000000000000000 ) ) ;
#47800=AXIS2_PLACEMENT_3D ( 'NONE', #44252, #7108, #806 ) ;
#47801=ADVANCED_FACE ( 'NONE', ( #13333 ), #56467, .T. ) ;
#47802=DIRECTION ( 'NONE',  ( 0.000000000000000000, 0.000000000000000000, 1.000000000000000000 ) ) ;
#47803=MECHANICAL_DESIGN_GEOMETRIC_PRESENTATION_REPRESENTATION('',(#54585),#66971);
#47807=ORIENTED_EDGE ( 'NONE', *, *, #63507, .F. ) ;
#47809=VERTEX_POINT ( 'NONE', #28890 ) ;
#47811=CARTESIAN_POINT ( 'NONE',  ( 26.90000000000000213, 20.60000000000000142, 13.86939075806900057 ) ) ;
#47814=CARTESIAN_POINT ( 'NONE',  ( 49.00000000000000000, -21.00000000000000000, 13.86939075806900057 ) ) ;
#47828=ORIENTED_EDGE ( 'NONE', *, *, #56547, .T. ) ;
#47835=ORIENTED_EDGE ( 'NONE', *, *, #45448, .T. ) ;
#47837=DIRECTION ( 'NONE',  ( 0.000000000000000000, 1.000000000000000000, -0.000000000000000000 ) ) ;
#47852=COLOUR_RGB ( '', 0.66274510, 0.83137255, 0.94901961) ;
#47856=CARTESIAN_POINT ( 'NONE',  ( 37.90000000000000568, -0.1999999999911430404, -8.864436962241481021E-12 ) ) ;
#47858=AXIS2_PLACEMENT_3D ( 'NONE', #53009, #9874, #41677 ) ;
#47861=ADVANCED_FACE ( 'NONE', ( #37028 ), #10482, .T. ) ;
#47869=FACE_OUTER_BOUND ( 'NONE', #24789, .T. ) ;
#47875=DIRECTION ( 'NONE',  ( 0.000000000000000000, 1.000000000000000000, 0.000000000000000000 ) ) ;
#47902=DIRECTION ( 'NONE',  ( 0.000000000000000000, -1.000000000000000000, 0.000000000000000000 ) ) ;
#47906=AXIS2_PLACEMENT_3D ( 'NONE', #12654, #55474, #23283 ) ;
#47914=ORIENTED_EDGE ( 'NONE', *, *, #40714, .F. ) ;
#47947=CARTESIAN_POINT ( 'NONE',  ( 48.50000000000000000, 0.7500000000000000000, -3.418698582794335028 ) ) ;
#47959=ORIENTED_EDGE ( 'NONE', *, *, #50073, .T. ) ;
#47964=AXIS2_PLACEMENT_3D ( 'NONE', #67073, #39499, #61403 ) ;
#47967=DIRECTION ( 'NONE',  ( 1.000000000000000000, -0.000000000000000000, 0.000000000000000000 ) ) ;
#47972=DIRECTION ( 'NONE',  ( 0.000000000000000000, 0.000000000000000000, -1.000000000000000000 ) ) ;
#47976=DIRECTION ( 'NONE',  ( 0.000000000000000000, 0.000000000000000000, -1.000000000000000000 ) ) ;
#47980=EDGE_CURVE ( 'NONE', #22897, #29653, #59819, .T. ) ;
#47982=CYLINDRICAL_SURFACE ( 'NONE', #16894, 24.99999999998784972 ) ;
#47997=CYLINDRICAL_SURFACE ( 'NONE', #50050, 24.99999999998784972 ) ;
#48002=ORIENTED_EDGE ( 'NONE', *, *, #66898, .T. ) ;
#48013=VECTOR ( 'NONE', #12832, 1000.000000000000000 ) ;
#48021=ORIENTED_EDGE ( 'NONE', *, *, #203, .T. ) ;
#48027=DIRECTION ( 'NONE',  ( -1.000000000000000000, 0.000000000000000000, 0.000000000000000000 ) ) ;
#48029=ORIENTED_EDGE ( 'NONE', *, *, #16372, .T. ) ;
#48035=DIRECTION ( 'NONE',  ( 0.000000000000000000, 0.000000000000000000, -1.000000000000000000 ) ) ;
#48051=PRESENTATION_STYLE_ASSIGNMENT (( #49446 ) ) ;
#48052=DIRECTION ( 'NONE',  ( 0.000000000000000000, 1.000000000000000000, 0.000000000000000000 ) ) ;
#48064=DIRECTION ( 'NONE',  ( 0.000000000000000000, 0.000000000000000000, 1.000000000000000000 ) ) ;
#48077=ADVANCED_FACE ( 'NONE', ( #43000, #64579 ), #10825, .F. ) ;
#48085=DIRECTION ( 'NONE',  ( 0.6785983445458448893, -0.2810846377148217834, 0.6785983445458485530 ) ) ;
#48090=DIRECTION ( 'NONE',  ( 0.000000000000000000, 0.000000000000000000, 1.000000000000000000 ) ) ;
#48102=AXIS2_PLACEMENT_3D ( 'NONE', #32062, #53638, #5540 ) ;
#48107=VERTEX_POINT ( 'NONE', #46129 ) ;
#48114=ORIENTED_EDGE ( 'NONE', *, *, #42666, .T. ) ;
#48116=CARTESIAN_POINT ( 'NONE',  ( 9.900000000000000355, -18.00000000000000355, -21.00000000000000000 ) ) ;
#48118=CARTESIAN_POINT ( 'NONE',  ( 0.5000000000000000000, -21.00000000000000000, 18.00000000000000355 ) ) ;
#48120=ADVANCED_FACE ( 'NONE', ( #2641 ), #45073, .T. ) ;
#48121=ADVANCED_FACE ( 'NONE', ( #67696, #1593 ), #62379, .F. ) ;
#48122=LINE ( 'NONE', #10626, #18802 ) ;
#48127=VECTOR ( 'NONE', #4231, 1000.000000000000000 ) ;
#48136=CARTESIAN_POINT ( 'NONE',  ( 37.90000000000000568, -0.000000000000000000, -20.80000000000000071 ) ) ;
#48146=CIRCLE ( 'NONE', #26646, 0.5000000000000000000 ) ;
#48148=CARTESIAN_POINT ( 'NONE',  ( 41.09999999999999432, -0.1999999999911430404, -8.864436962241481021E-12 ) ) ;
#48149=PLANE ( 'NONE',  #1209 ) ;
#48151=FACE_OUTER_BOUND ( 'NONE', #22393, .T. ) ;
#48153=VECTOR ( 'NONE', #27683, 1000.000000000000000 ) ;
#48174=ORIENTED_EDGE ( 'NONE', *, *, #21777, .F. ) ;
#48180=FACE_OUTER_BOUND ( 'NONE', #32180, .T. ) ;
#48188=FACE_OUTER_BOUND ( 'NONE', #7544, .T. ) ;
#48195=ORIENTED_EDGE ( 'NONE', *, *, #21305, .F. ) ;
#48201=ORIENTED_EDGE ( 'NONE', *, *, #10469, .F. ) ;
#48217=VECTOR ( 'NONE', #36110, 1000.000000000000000 ) ;
#48222=ADVANCED_FACE ( 'NONE', ( #14317 ), #8994, .T. ) ;
#48235=EDGE_CURVE ( 'NONE', #54092, #5641, #35878, .T. ) ;
#48246=DIRECTION ( 'NONE',  ( 0.000000000000000000, 0.000000000000000000, -1.000000000000000000 ) ) ;
#48250=LINE ( 'NONE', #33371, #20436 ) ;
#48256=AXIS2_PLACEMENT_3D ( 'NONE', #6547, #44345, #49342 ) ;
#48267=CARTESIAN_POINT ( 'NONE',  ( 10.00000000000000000, 18.00000000000000355, 21.00000000000000000 ) ) ;
#48275=ADVANCED_FACE ( 'NONE', ( #19958 ), #36568, .F. ) ;
#48278=CIRCLE ( 'NONE', #21168, 0.5000000000000000000 ) ;
#48281=CARTESIAN_POINT ( 'NONE',  ( 0.5000000000000000000, -21.00000000000000000, -18.00000000000000355 ) ) ;
#48285=VERTEX_POINT ( 'NONE', #62739 ) ;
#48293=ORIENTED_EDGE ( 'NONE', *, *, #22070, .T. ) ;
#48296=AXIS2_PLACEMENT_3D ( 'NONE', #28529, #50099, #1653 ) ;
#48300=VECTOR ( 'NONE', #47798, 1000.000000000000000 ) ;
#48306=VECTOR ( 'NONE', #60891, 1000.000000000000000 ) ;
#48313=DIRECTION ( 'NONE',  ( 0.000000000000000000, 0.000000000000000000, -1.000000000000000000 ) ) ;
#48319=CARTESIAN_POINT ( 'NONE',  ( 39.90000000000000568, -0.2000000000089119934, 8.909539772616881237E-12 ) ) ;
#48331=DIRECTION ( 'NONE',  ( -1.000000000000000000, 0.000000000000000000, 0.000000000000000000 ) ) ;
#48334=CARTESIAN_POINT ( 'NONE',  ( 49.00000000000000000, -0.2000000000089119934, -8.913009219568841313E-12 ) ) ;
#48335=EDGE_CURVE ( 'NONE', #43945, #4916, #3335, .T. ) ;
#48354=ORIENTED_EDGE ( 'NONE', *, *, #63498, .T. ) ;
#48358=AXIS2_PLACEMENT_3D ( 'NONE', #58885, #32012, #31670 ) ;
#48368=ORIENTED_EDGE ( 'NONE', *, *, #64770, .T. ) ;
#48369=CIRCLE ( 'NONE', #11113, 24.99999999998784972 ) ;
#48383=CARTESIAN_POINT ( 'NONE',  ( 39.90000000000000568, -21.00000000000000000, 13.86939075806900057 ) ) ;
#48385=ORIENTED_EDGE ( 'NONE', *, *, #69730, .F. ) ;
#48390=DIRECTION ( 'NONE',  ( 0.000000000000000000, 0.000000000000000000, -1.000000000000000000 ) ) ;
#48416=CARTESIAN_POINT ( 'NONE',  ( 31.89999999999999858, 13.66939075806899240, 20.79999999999999361 ) ) ;
#48441=CARTESIAN_POINT ( 'NONE',  ( 41.09999999999999432, -21.00000000000000000, -13.86939075806900057 ) ) ;
#48464=AXIS2_PLACEMENT_3D ( 'NONE', #8344, #7993, #40173 ) ;
#48472=EDGE_CURVE ( 'NONE', #69700, #15393, #66228, .T. ) ;
#48474=AXIS2_PLACEMENT_3D ( 'NONE', #67603, #40005, #29753 ) ;
#48479=DIRECTION ( 'NONE',  ( 1.000000000000000000, -0.000000000000000000, 0.000000000000000000 ) ) ;
#48490=CARTESIAN_POINT ( 'NONE',  ( 39.00000000000000000, -0.2000000000000000111, 0.000000000000000000 ) ) ;
#48502=VERTEX_POINT ( 'NONE', #60906 ) ;
#48516=VERTEX_POINT ( 'NONE', #23783 ) ;
#48533=SHAPE_REPRESENTATION_RELATIONSHIP ( 'NONE' , 'NONE' ,  #33595, #19156 ) ;
#48552=CARTESIAN_POINT ( 'NONE',  ( 25.57999999999999829, 3.010794155703768650E-16, -2.458500000000000796 ) ) ;
#48573=CARTESIAN_POINT ( 'NONE',  ( 9.900000000000000355, 0.000000000000000000, 2.154935995002245639E-16 ) ) ;
#48609=DIRECTION ( 'NONE',  ( 0.000000000000000000, 1.000000000000000000, 0.000000000000000000 ) ) ;
#48620=AXIS2_PLACEMENT_3D ( 'NONE', #60459, #33253, #743 ) ;
#48635=EDGE_LOOP ( 'NONE', ( #69512, #61858, #69251, #52615 ) ) ;
#48643=AXIS2_PLACEMENT_3D ( 'NONE', #68287, #67590, #45650 ) ;
#48660=PLANE ( 'NONE',  #36172 ) ;
#48665=EDGE_LOOP ( 'NONE', ( #13734, #2668, #42253, #45527 ) ) ;
#48712=ORIENTED_EDGE ( 'NONE', *, *, #44868, .F. ) ;
#48726=CARTESIAN_POINT ( 'NONE',  ( 26.90000000000000213, 20.60000000000000142, -13.86939075806900057 ) ) ;
#48737=CARTESIAN_POINT ( 'NONE',  ( 35.89999999999999858, 20.60000000000000142, 3.016910393003143647E-15 ) ) ;
#48746=ORIENTED_EDGE ( 'NONE', *, *, #24114, .T. ) ;
#48750=CARTESIAN_POINT ( 'NONE',  ( 13.90000000000000213, -14.06939075806900874, 20.80000000000001137 ) ) ;
#48768=FACE_OUTER_BOUND ( 'NONE', #36092, .T. ) ;
#48775=DIRECTION ( 'NONE',  ( 0.000000000000000000, 0.2142857142857142738, 0.9767710236555245951 ) ) ;
#48790=LINE ( 'NONE', #48441, #53632 ) ;
#48791=CARTESIAN_POINT ( 'NONE',  ( 10.90000000000000036, 20.60000000000000142, -13.86939075806900057 ) ) ;
#48815=DIRECTION ( 'NONE',  ( 0.000000000000000000, 0.000000000000000000, -1.000000000000000000 ) ) ;
#48816=ORIENTED_EDGE ( 'NONE', *, *, #2901, .F. ) ;
#48829=LINE ( 'NONE', #31178, #57668 ) ;
#48841=CARTESIAN_POINT ( 'NONE',  ( 27.00000000000000000, 3.010794155703768650E-16, 2.458500000000000796 ) ) ;
#48844=PLANE ( 'NONE',  #29564 ) ;
#48861=FACE_OUTER_BOUND ( 'NONE', #52531, .T. ) ;
#48893=EDGE_LOOP ( 'NONE', ( #7528, #34076, #65580, #7432 ) ) ;
#48899=ADVANCED_FACE ( 'NONE', ( #12721 ), #49540, .T. ) ;
#48907=DIRECTION ( 'NONE',  ( 1.000000000000000000, -0.000000000000000000, 0.000000000000000000 ) ) ;
#48908=ORIENTED_EDGE ( 'NONE', *, *, #28082, .T. ) ;
#48909=ORIENTED_EDGE ( 'NONE', *, *, #36727, .T. ) ;
#48914=CARTESIAN_POINT ( 'NONE',  ( 49.00000000000000000, -21.00000000000000000, 13.86939075806900057 ) ) ;
#48926=CARTESIAN_POINT ( 'NONE',  ( 27.00000000000000000, 3.010794155703768650E-16, 2.458500000000000796 ) ) ;
#48934=VERTEX_POINT ( 'NONE', #38924 ) ;
#48949=ORIENTED_EDGE ( 'NONE', *, *, #66531, .T. ) ;
#48972=ORIENTED_EDGE ( 'NONE', *, *, #5151, .F. ) ;
#48975=CARTESIAN_POINT ( 'NONE',  ( 41.09999999999999432, 20.60000000000000142, 13.86939075806900057 ) ) ;
#49008=DIRECTION ( 'NONE',  ( 0.000000000000000000, -1.000000000000000000, 0.000000000000000000 ) ) ;
#49011=VECTOR ( 'NONE', #9892, 1000.000000000000000 ) ;
#49012=AXIS2_PLACEMENT_3D ( 'NONE', #65237, #33041, #10772 ) ;
#49033=AXIS2_PLACEMENT_3D ( 'NONE', #15304, #42519, #31920 ) ;
#49036=DIRECTION ( 'NONE',  ( 1.000000000000000000, -0.000000000000000000, 0.000000000000000000 ) ) ;
#49037=ORIENTED_EDGE ( 'NONE', *, *, #29576, .T. ) ;
#49042=DIRECTION ( 'NONE',  ( 0.000000000000000000, 0.000000000000000000, -1.000000000000000000 ) ) ;
#49050=CARTESIAN_POINT ( 'NONE',  ( 10.90000000000000036, -0.2000000000089119934, -8.913009219568841313E-12 ) ) ;
#49055=LINE ( 'NONE', #38451, #61543 ) ;
#49060=EDGE_LOOP ( 'NONE', ( #10371, #61236, #17784, #59328 ) ) ;
#49061=EDGE_LOOP ( 'NONE', ( #66603, #32720, #4163, #29754 ) ) ;
#49085=DIRECTION ( 'NONE',  ( 0.000000000000000000, -1.000000000000000000, 0.000000000000000000 ) ) ;
#49086=ORIENTED_EDGE ( 'NONE', *, *, #66004, .F. ) ;
#49090=EDGE_CURVE ( 'NONE', #1707, #65063, #51629, .T. ) ;
#49110=ORIENTED_EDGE ( 'NONE', *, *, #52076, .T. ) ;
#49121=EDGE_CURVE ( 'NONE', #61094, #69579, #19782, .T. ) ;
#49130=CIRCLE ( 'NONE', #53685, 24.99999999998784972 ) ;
#49138=ORIENTED_EDGE ( 'NONE', *, *, #22821, .F. ) ;
#49154=AXIS2_PLACEMENT_3D ( 'NONE', #55107, #55784, #39178 ) ;
#49177=DIRECTION ( 'NONE',  ( -1.000000000000000000, 0.000000000000000000, 0.000000000000000000 ) ) ;
#49197=ORIENTED_EDGE ( 'NONE', *, *, #35938, .F. ) ;
#49198=EDGE_CURVE ( 'NONE', #64226, #33306, #7996, .T. ) ;
#49217=AXIS2_PLACEMENT_3D ( 'NONE', #51666, #57664, #63322 ) ;
#49219=CARTESIAN_POINT ( 'NONE',  ( 39.00000000000000000, -16.96999999999999886, -21.00000000000000000 ) ) ;
#49225=VECTOR ( 'NONE', #66750, 1000.000000000000000 ) ;
#49227=CARTESIAN_POINT ( 'NONE',  ( 33.89999999999999858, -21.00000000000000000, 13.86939075806900057 ) ) ;
#49244=CARTESIAN_POINT ( 'NONE',  ( 18.89999999999999858, 20.60000000000000142, -13.86939075806900057 ) ) ;
#49250=EDGE_LOOP ( 'NONE', ( #23192, #69321, #69095, #62484 ) ) ;
#49251=CARTESIAN_POINT ( 'NONE',  ( 20.90000000000000213, 13.66939075806899950, 20.80000000000000426 ) ) ;
#49252=COLOUR_RGB ( '', 0.31764706, 0.68627451, 0.89019608) ;
#49272=LINE ( 'NONE', #15349, #67119 ) ;
#49279=CARTESIAN_POINT ( 'NONE',  ( 8.900000000000002132, 0.000000000000000000, 0.000000000000000000 ) ) ;
#49280=ADVANCED_FACE ( 'NONE', ( #3756 ), #47594, .T. ) ;
#49287=CIRCLE ( 'NONE', #33473, 5.000000000000000000 ) ;
#49296=ORIENTED_EDGE ( 'NONE', *, *, #10773, .T. ) ;
#49319=ADVANCED_FACE ( 'NONE', ( #19655 ), #20371, .F. ) ;
#49342=DIRECTION ( 'NONE',  ( 0.000000000000000000, 0.000000000000000000, 1.000000000000000000 ) ) ;
#49348=ADVANCED_FACE ( 'NONE', ( #47253 ), #3068, .F. ) ;
#49351=VECTOR ( 'NONE', #24386, 1000.000000000000000 ) ;
#49354=EDGE_CURVE ( 'NONE', #29693, #68454, #14580, .T. ) ;
#49355=FACE_OUTER_BOUND ( 'NONE', #13388, .T. ) ;
#49359=EDGE_CURVE ( 'NONE', #21251, #32793, #30981, .T. ) ;
#49365=EDGE_CURVE ( 'NONE', #43945, #40050, #10458, .T. ) ;
#49388=DIRECTION ( 'NONE',  ( 0.000000000000000000, -0.7071067811865475727, -0.7071067811865475727 ) ) ;
#49395=VERTEX_POINT ( 'NONE', #50279 ) ;
#49402=AXIS2_PLACEMENT_3D ( 'NONE', #30564, #67693, #12879 ) ;
#49416=VECTOR ( 'NONE', #5727, 1000.000000000000000 ) ;
#49417=VECTOR ( 'NONE', #22027, 1000.000000000000000 ) ;
#49421=ORIENTED_EDGE ( 'NONE', *, *, #20903, .T. ) ;
#49428=ORIENTED_EDGE ( 'NONE', *, *, #22130, .F. ) ;
#49432=PRESENTATION_STYLE_ASSIGNMENT (( #54731 ) ) ;
#49439=PLANE ( 'NONE',  #64669 ) ;
#49440=EDGE_CURVE ( 'NONE', #41070, #58001, #69955, .T. ) ;
#49446=SURFACE_STYLE_USAGE ( .BOTH. , #42393 ) ;
#49448=STYLED_ITEM ( 'NONE', ( #63447 ), #20943 ) ;
#49455=ORIENTED_EDGE ( 'NONE', *, *, #44090, .T. ) ;
#49469=DIRECTION ( 'NONE',  ( -1.000000000000000000, 0.000000000000000000, 0.000000000000000000 ) ) ;
#49495=ORIENTED_EDGE ( 'NONE', *, *, #31082, .F. ) ;
#49498=ORIENTED_EDGE ( 'NONE', *, *, #59672, .T. ) ;
#49503=AXIS2_PLACEMENT_3D ( 'NONE', #51897, #14764, #46228 ) ;
#49505=CARTESIAN_POINT ( 'NONE',  ( 19.90000000000000213, -0.2000000000089119934, -8.913009219568841313E-12 ) ) ;
#49510=CARTESIAN_POINT ( 'NONE',  ( 10.00000000000000000, -21.00000000000000000, -18.00000000000000355 ) ) ;
#49513=CARTESIAN_POINT ( 'NONE',  ( 39.00000000000000000, 21.00000000000000000, -16.96999999999999886 ) ) ;
#49528=ADVANCED_FACE ( 'NONE', ( #55247 ), #66200, .F. ) ;
#49540=CYLINDRICAL_SURFACE ( 'NONE', #13573, 0.5000000000000000000 ) ;
#49543=FACE_BOUND ( 'NONE', #10580, .T. ) ;
#49547=CARTESIAN_POINT ( 'NONE',  ( 38.90000000000000568, -14.06939075806902117, -20.80000000000000426 ) ) ;
#49557=AXIS2_PLACEMENT_3D ( 'NONE', #1936, #60965, #38718 ) ;
#49563=EDGE_LOOP ( 'NONE', ( #61223, #11383, #10547, #22688 ) ) ;
#49565=ORIENTED_EDGE ( 'NONE', *, *, #34637, .F. ) ;
#49570=CARTESIAN_POINT ( 'NONE',  ( 40.90000000000000568, 20.60000000000000142, -13.86939075806900057 ) ) ;
#49576=FACE_BOUND ( 'NONE', #38544, .T. ) ;
#49602=PLANE ( 'NONE',  #11966 ) ;
#49608=ORIENTED_EDGE ( 'NONE', *, *, #60935, .F. ) ;
#49609=ORIENTED_EDGE ( 'NONE', *, *, #55339, .F. ) ;
#49610=AXIS2_PLACEMENT_3D ( 'NONE', #1841, #53264, #49931 ) ;
#49611=DIRECTION ( 'NONE',  ( 1.000000000000000000, -0.000000000000000000, 0.000000000000000000 ) ) ;
#49615=AXIS2_PLACEMENT_3D ( 'NONE', #36218, #30231, #47193 ) ;
#49628=DIRECTION ( 'NONE',  ( 0.000000000000000000, -1.000000000000000000, 0.000000000000000000 ) ) ;
#49649=VERTEX_POINT ( 'NONE', #47535 ) ;
#49651=AXIS2_PLACEMENT_3D ( 'NONE', #46288, #40981, #24731 ) ;
#49660=EDGE_CURVE ( 'NONE', #18694, #32607, #33841, .T. ) ;
#49662=VERTEX_POINT ( 'NONE', #17702 ) ;
#49665=CARTESIAN_POINT ( 'NONE',  ( 14.89999999999999680, -21.00000000000000000, 13.86939075806900057 ) ) ;
#49676=DIRECTION ( 'NONE',  ( -1.000000000000000000, 0.000000000000000000, 0.000000000000000000 ) ) ;
#49686=DIRECTION ( 'NONE',  ( 0.000000000000000000, -1.000000000000000000, 0.000000000000000000 ) ) ;
#49687=LINE ( 'NONE', #1258, #29774 ) ;
#49692=FILL_AREA_STYLE_COLOUR ( '', #68306 ) ;
#49695=EDGE_CURVE ( 'NONE', #32276, #4210, #55872, .T. ) ;
#49702=CARTESIAN_POINT ( 'NONE',  ( 41.09999999999999432, 21.00000000000000000, 13.98999642601811999 ) ) ;
#49710=CIRCLE ( 'NONE', #55371, 2.458500000000000796 ) ;
#49719=ORIENTED_EDGE ( 'NONE', *, *, #57219, .T. ) ;
#49734=LINE ( 'NONE', #44080, #6259 ) ;
#49746=CYLINDRICAL_SURFACE ( 'NONE', #31167, 24.99999999998794920 ) ;
#49764=DIRECTION ( 'NONE',  ( 0.000000000000000000, 0.000000000000000000, -1.000000000000000000 ) ) ;
#49772=CARTESIAN_POINT ( 'NONE',  ( 23.90000000000000213, 13.66939075806899240, 20.79999999999999361 ) ) ;
#49781=CARTESIAN_POINT ( 'NONE',  ( 31.89999999999999858, -0.2000000000089119934, 8.909539772616881237E-12 ) ) ;
#49788=DIRECTION ( 'NONE',  ( 1.000000000000000000, 0.000000000000000000, 0.000000000000000000 ) ) ;
#49789=DIRECTION ( 'NONE',  ( 0.000000000000000000, 0.000000000000000000, 1.000000000000000000 ) ) ;
#49792=CIRCLE ( 'NONE', #31744, 24.99999999998784972 ) ;
#49794=MECHANICAL_DESIGN_GEOMETRIC_PRESENTATION_REPRESENTATION('',(#10287),#17090);
#49796=CARTESIAN_POINT ( 'NONE',  ( 39.00000000000000000, 16.96999999999999886, -21.00000000000000000 ) ) ;
#49808=CIRCLE ( 'NONE', #64474, 24.99999999998784972 ) ;
#49820=ORIENTED_EDGE ( 'NONE', *, *, #21733, .F. ) ;
#49827=EDGE_CURVE ( 'NONE', #54853, #34859, #31615, .T. ) ;
#49842=CIRCLE ( 'NONE', #64554, 3.500000000000000000 ) ;
#49852=LINE ( 'NONE', #56799, #7558 ) ;
#49854=CLOSED_SHELL ( 'NONE', ( #16032, #29384, #3406, #14375, #43359, #28700, #6852, #18534, #41736, #54355 ) ) ;
#49861=CARTESIAN_POINT ( 'NONE',  ( 40.90000000000000568, -0.2000000000000000111, 0.000000000000000000 ) ) ;
#49868=VERTEX_POINT ( 'NONE', #67541 ) ;
#49877=DIRECTION ( 'NONE',  ( 1.000000000000000000, -0.000000000000000000, -0.000000000000000000 ) ) ;
#49884=DIRECTION ( 'NONE',  ( -0.000000000000000000, -1.000000000000000000, 0.000000000000000000 ) ) ;
#49886=DIRECTION ( 'NONE',  ( 0.000000000000000000, 0.000000000000000000, -1.000000000000000000 ) ) ;
#49889=AXIS2_PLACEMENT_3D ( 'NONE', #68653, #14905, #62277 ) ;
#49899=VERTEX_POINT ( 'NONE', #56570 ) ;
#49905=CIRCLE ( 'NONE', #19415, 2.458500000000000796 ) ;
#49913=ORIENTED_EDGE ( 'NONE', *, *, #11187, .F. ) ;
#49922=VERTEX_POINT ( 'NONE', #62558 ) ;
#49924=CYLINDRICAL_SURFACE ( 'NONE', #6883, 24.99999999998784972 ) ;
#49928=DIRECTION ( 'NONE',  ( 0.000000000000000000, 0.000000000000000000, 1.000000000000000000 ) ) ;
#49931=DIRECTION ( 'NONE',  ( 0.000000000000000000, 0.000000000000000000, -1.000000000000000000 ) ) ;
#49933=LINE ( 'NONE', #65519, #5675 ) ;
#49934=AXIS2_PLACEMENT_3D ( 'NONE', #23578, #6287, #6965 ) ;
#49953=ORIENTED_EDGE ( 'NONE', *, *, #14980, .T. ) ;
#49956=EDGE_CURVE ( 'NONE', #64055, #8098, #30404, .T. ) ;
#49957=EDGE_LOOP ( 'NONE', ( #53929, #39090, #43713, #18649 ) ) ;
#49964=FACE_OUTER_BOUND ( 'NONE', #34616, .T. ) ;
#49966=DIRECTION ( 'NONE',  ( -1.000000000000000000, 0.000000000000000000, 0.000000000000000000 ) ) ;
#49976=CIRCLE ( 'NONE', #54502, 24.99999999998784972 ) ;
#49983=CARTESIAN_POINT ( 'NONE',  ( 48.99818295588534767, 0.7500000000000000000, 3.928729023727064451 ) ) ;
#50002=EDGE_LOOP ( 'NONE', ( #21897, #20453, #26613, #65111 ) ) ;
#50012=FACE_OUTER_BOUND ( 'NONE', #14640, .T. ) ;
#50013=DIRECTION ( 'NONE',  ( -1.000000000000000000, 0.000000000000000000, 0.000000000000000000 ) ) ;
#50015=ORIENTED_EDGE ( 'NONE', *, *, #6943, .F. ) ;
#50027=VERTEX_POINT ( 'NONE', #4249 ) ;
#50035=DIRECTION ( 'NONE',  ( 0.000000000000000000, 0.000000000000000000, -1.000000000000000000 ) ) ;
#50037=FACE_OUTER_BOUND ( 'NONE', #32453, .T. ) ;
#50040=DIRECTION ( 'NONE',  ( 1.000000000000000000, -0.000000000000000000, 0.000000000000000000 ) ) ;
#50046=ADVANCED_FACE ( 'NONE', ( #9539 ), #37464, .F. ) ;
#50049=EDGE_LOOP ( 'NONE', ( #47614, #39847, #23193, #31950 ) ) ;
#50050=AXIS2_PLACEMENT_3D ( 'NONE', #21129, #24062, #45620 ) ;
#50055=ADVANCED_FACE ( 'NONE', ( #4590, #69282 ), #20835, .T. ) ;
#50068=CARTESIAN_POINT ( 'NONE',  ( 9.899999999999998579, 21.00000000000000355, -13.98999642601812354 ) ) ;
#50069=DIRECTION ( 'NONE',  ( 0.000000000000000000, 0.000000000000000000, -1.000000000000000000 ) ) ;
#50073=EDGE_CURVE ( 'NONE', #53577, #29958, #59369, .T. ) ;
#50076=FACE_OUTER_BOUND ( 'NONE', #38507, .T. ) ;
#50080=ORIENTED_EDGE ( 'NONE', *, *, #50694, .T. ) ;
#50083=DIRECTION ( 'NONE',  ( 0.000000000000000000, -0.7071067811865474617, -0.7071067811865474617 ) ) ;
#50084=ADVANCED_FACE ( 'NONE', ( #44819 ), #673, .F. ) ;
#50091=ORIENTED_EDGE ( 'NONE', *, *, #11433, .F. ) ;
#50098=CARTESIAN_POINT ( 'NONE',  ( 46.39999999999999858, 21.00000000000000000, -0.7500000000000000000 ) ) ;
#50099=DIRECTION ( 'NONE',  ( -1.000000000000000000, 0.000000000000000000, 0.000000000000000000 ) ) ;
#50100=LINE ( 'NONE', #44786, #19588 ) ;
#50106=AXIS2_PLACEMENT_3D ( 'NONE', #47685, #25421, #6202 ) ;
#50111=AXIS2_PLACEMENT_3D ( 'NONE', #60526, #6773, #24081 ) ;
#50121=EDGE_CURVE ( 'NONE', #60080, #10676, #58760, .T. ) ;
#50125=EDGE_CURVE ( 'NONE', #17228, #5931, #22920, .T. ) ;
#50138=ORIENTED_EDGE ( 'NONE', *, *, #67340, .F. ) ;
#50144=CARTESIAN_POINT ( 'NONE',  ( 9.900000000000000355, -14.48845687959340012, 21.00000000000000000 ) ) ;
#50150=CARTESIAN_POINT ( 'NONE',  ( 39.90000000000000568, 0.000000000000000000, 3.447897592003593022E-15 ) ) ;
#50156=DIRECTION ( 'NONE',  ( 0.000000000000000000, 0.000000000000000000, 1.000000000000000000 ) ) ;
#50158=CARTESIAN_POINT ( 'NONE',  ( 41.09999999999999432, -14.06939075806900163, 20.80000000000000426 ) ) ;
#50165=( NAMED_UNIT ( * ) PLANE_ANGLE_UNIT ( ) SI_UNIT ( $, .RADIAN. ) );
#50166=CIRCLE ( 'NONE', #18512, 24.99999999998784972 ) ;
#50181=FACE_OUTER_BOUND ( 'NONE', #12766, .T. ) ;
#50194=CARTESIAN_POINT ( 'NONE',  ( 35.89999999999999858, -21.00000000000000000, 13.86939075806900057 ) ) ;
#50195=DIRECTION ( 'NONE',  ( -1.000000000000000000, 0.000000000000000000, 0.000000000000000000 ) ) ;
#50199=CARTESIAN_POINT ( 'NONE',  ( 41.09999999999999432, 14.08845687959340331, -21.00000000000000000 ) ) ;
#50209=AXIS2_PLACEMENT_3D ( 'NONE', #10940, #59727, #44829 ) ;
#50220=ADVANCED_FACE ( 'NONE', ( #59713 ), #17950, .F. ) ;
#50242=CARTESIAN_POINT ( 'NONE',  ( 47.00000000000000000, 0.000000000000000000, 0.000000000000000000 ) ) ;
#50260=EDGE_CURVE ( 'NONE', #13113, #27714, #50485, .T. ) ;
#50261=AXIS2_PLACEMENT_3D ( 'NONE', #49050, #17207, #6258 ) ;
#50263=CARTESIAN_POINT ( 'NONE',  ( 47.00000000000000000, -0.7500000000000000000, 3.418698582794335028 ) ) ;
#50270=VERTEX_POINT ( 'NONE', #34900 ) ;
#50279=CARTESIAN_POINT ( 'NONE',  ( 36.90000000000000568, 20.60000000000000142, 13.86939075806900057 ) ) ;
#50296=AXIS2_PLACEMENT_3D ( 'NONE', #4155, #38079, #63893 ) ;
#50317=DIRECTION ( 'NONE',  ( -1.000000000000000000, 0.000000000000000000, 0.000000000000000000 ) ) ;
#50320=DIRECTION ( 'NONE',  ( 0.000000000000000000, 0.000000000000000000, -1.000000000000000000 ) ) ;
#50321=VERTEX_POINT ( 'NONE', #51538 ) ;
#50326=CARTESIAN_POINT ( 'NONE',  ( 25.57999999999999829, 0.000000000000000000, 5.250000000000000000 ) ) ;
#50333=LINE ( 'NONE', #23469, #48013 ) ;
#50337=ORIENTED_EDGE ( 'NONE', *, *, #282, .T. ) ;
#50342=DIRECTION ( 'NONE',  ( 0.000000000000000000, 0.000000000000000000, 1.000000000000000000 ) ) ;
#50351=CARTESIAN_POINT ( 'NONE',  ( 34.89999999999999858, 13.66939075806899950, 20.80000000000000426 ) ) ;
#50363=CIRCLE ( 'NONE', #59413, 24.99999999998794920 ) ;
#50371=CARTESIAN_POINT ( 'NONE',  ( 41.09999999999999432, 13.66939075806899950, 20.80000000000000426 ) ) ;
#50374=COLOUR_RGB ( '', 0.40784314, 0.44705882, 0.49803922) ;
#50376=FACE_OUTER_BOUND ( 'NONE', #46945, .T. ) ;
#50377=CARTESIAN_POINT ( 'NONE',  ( 13.90000000000000213, 20.60000000000000142, -13.86939075806900057 ) ) ;
#50380=CARTESIAN_POINT ( 'NONE',  ( 39.00000000000000000, 14.08845687959340331, -21.00000000000000000 ) ) ;
#50388=ADVANCED_FACE ( 'NONE', ( #9815 ), #30667, .F. ) ;
#50395=PLANE ( 'NONE',  #40658 ) ;
#50408=ORIENTED_EDGE ( 'NONE', *, *, #41596, .F. ) ;
#50410=VECTOR ( 'NONE', #50574, 1000.000000000000000 ) ;
#50415=VECTOR ( 'NONE', #2885, 1000.000000000000000 ) ;
#50416=VECTOR ( 'NONE', #52006, 1000.000000000000000 ) ;
#50419=VERTEX_POINT ( 'NONE', #10148 ) ;
#50421=CARTESIAN_POINT ( 'NONE',  ( 27.90000000000000213, -21.00000000000000000, 13.86939075806900057 ) ) ;
#50426=DIRECTION ( 'NONE',  ( 0.000000000000000000, 0.000000000000000000, 1.000000000000000000 ) ) ;
#50428=EDGE_LOOP ( 'NONE', ( #62130, #15568, #48949, #44502 ) ) ;
#50431=CARTESIAN_POINT ( 'NONE',  ( 49.00000000000000000, -0.2000000000089119934, 8.909539772616881237E-12 ) ) ;
#50445=STYLED_ITEM ( 'NONE', ( #35396 ), #19195 ) ;
#50446=DIRECTION ( 'NONE',  ( 0.000000000000000000, 1.000000000000000000, 0.000000000000000000 ) ) ;
#50448=VECTOR ( 'NONE', #59347, 1000.000000000000000 ) ;
#50457=CARTESIAN_POINT ( 'NONE',  ( 41.09999999999999432, -21.00000000000000000, -13.86939075806900057 ) ) ;
#50463=DIRECTION ( 'NONE',  ( 1.000000000000000000, -0.000000000000000000, -0.000000000000000000 ) ) ;
#50470=LINE ( 'NONE', #38815, #24313 ) ;
#50471=CIRCLE ( 'NONE', #27923, 24.99999999998784972 ) ;
#50474=DIRECTION ( 'NONE',  ( 1.000000000000000000, -0.000000000000000000, 0.000000000000000000 ) ) ;
#50477=DIRECTION ( 'NONE',  ( 0.000000000000000000, -0.7071067811865474617, -0.7071067811865474617 ) ) ;
#50484=ADVANCED_FACE ( 'NONE', ( #41972 ), #15467, .T. ) ;
#50485=LINE ( 'NONE', #40214, #68898 ) ;
#50495=PLANE ( 'NONE',  #20899 ) ;
#50499=DIRECTION ( 'NONE',  ( -1.000000000000000000, 0.000000000000000000, 0.000000000000000000 ) ) ;
#50517=DIRECTION ( 'NONE',  ( 0.000000000000000000, -1.000000000000000000, 0.000000000000000000 ) ) ;
#50540=DIRECTION ( 'NONE',  ( 0.000000000000000000, 0.000000000000000000, -1.000000000000000000 ) ) ;
#50562=LINE ( 'NONE', #6049, #46819 ) ;
#50574=DIRECTION ( 'NONE',  ( -0.000000000000000000, -1.000000000000000000, 0.000000000000000000 ) ) ;
#50586=PLANE ( 'NONE',  #69409 ) ;
#50588=CARTESIAN_POINT ( 'NONE',  ( 49.00000000000000000, 13.66939075806899950, 20.80000000000000426 ) ) ;
#50597=DIRECTION ( 'NONE',  ( -1.000000000000000000, 0.000000000000000000, 0.000000000000000000 ) ) ;
#50599=CARTESIAN_POINT ( 'NONE',  ( 33.89999999999999858, -0.1999999999911795112, 8.826273045769999343E-12 ) ) ;
#50615=CYLINDRICAL_SURFACE ( 'NONE', #13038, 2.458500000000000796 ) ;
#50617=EDGE_LOOP ( 'NONE', ( #45364, #29300, #13700, #64304 ) ) ;
#50618=DIRECTION ( 'NONE',  ( 0.000000000000000000, 1.000000000000000000, 0.000000000000000000 ) ) ;
#50625=DIRECTION ( 'NONE',  ( -1.000000000000000000, 0.000000000000000000, 0.000000000000000000 ) ) ;
#50633=LINE ( 'NONE', #40002, #41797 ) ;
#50653=EDGE_CURVE ( 'NONE', #46863, #49899, #50741, .T. ) ;
#50662=ORIENTED_EDGE ( 'NONE', *, *, #52563, .F. ) ;
#50665=VERTEX_POINT ( 'NONE', #35521 ) ;
#50667=AXIS2_PLACEMENT_3D ( 'NONE', #18451, #24118, #40016 ) ;
#50669=LINE ( 'NONE', #1888, #4537 ) ;
#50683=VERTEX_POINT ( 'NONE', #40836 ) ;
#50686=ORIENTED_EDGE ( 'NONE', *, *, #31104, .F. ) ;
#50689=ADVANCED_FACE ( 'NONE', ( #34465 ), #8301, .T. ) ;
#50690=ORIENTED_EDGE ( 'NONE', *, *, #48235, .F. ) ;
#50692=EDGE_LOOP ( 'NONE', ( #58020, #39713, #64111, #23659 ) ) ;
#50693=CARTESIAN_POINT ( 'NONE',  ( 7.900000000000000355, 18.00000000000000355, -21.00000000000000000 ) ) ;
#50694=EDGE_CURVE ( 'NONE', #62756, #8699, #51096, .T. ) ;
#50701=EDGE_CURVE ( 'NONE', #45421, #54092, #45084, .T. ) ;
#50731=EDGE_CURVE ( 'NONE', #5641, #33487, #2652, .T. ) ;
#50740=PRESENTATION_STYLE_ASSIGNMENT (( #30242 ) ) ;
#50741=LINE ( 'NONE', #56747, #4605 ) ;
#50750=AXIS2_PLACEMENT_3D ( 'NONE', #34973, #66804, #2458 ) ;
#50754=DIRECTION ( 'NONE',  ( 0.000000000000000000, 0.000000000000000000, -1.000000000000000000 ) ) ;
#50766=LINE ( 'NONE', #2681, #21461 ) ;
#50781=EDGE_LOOP ( 'NONE', ( #35271, #33501, #12316, #8439 ) ) ;
#50790=DIRECTION ( 'NONE',  ( 1.000000000000000000, -0.000000000000000000, 0.000000000000000000 ) ) ;
#50799=AXIS2_PLACEMENT_3D ( 'NONE', #15198, #31471, #52688 ) ;
#50812=ORIENTED_EDGE ( 'NONE', *, *, #56202, .F. ) ;
#50821=DIRECTION ( 'NONE',  ( 1.000000000000000000, 0.000000000000000000, 0.000000000000000000 ) ) ;
#50832=CARTESIAN_POINT ( 'NONE',  ( 39.00000000000000000, 21.00000000000000000, 16.96999999999999886 ) ) ;
#50837=ORIENTED_EDGE ( 'NONE', *, *, #20405, .F. ) ;
#50840=LINE ( 'NONE', #67480, #46025 ) ;
#50844=CIRCLE ( 'NONE', #27151, 24.99999999998794920 ) ;
#50868=EDGE_LOOP ( 'NONE', ( #67909, #57382, #30397, #27746 ) ) ;
#50873=ORIENTED_EDGE ( 'NONE', *, *, #679, .T. ) ;
#50878=CARTESIAN_POINT ( 'NONE',  ( 41.09999999999999432, -21.00000000000000000, 13.86939075806900057 ) ) ;
#50894=VECTOR ( 'NONE', #28617, 1000.000000000000000 ) ;
#50902=ORIENTED_EDGE ( 'NONE', *, *, #5439, .F. ) ;
#50903=VECTOR ( 'NONE', #69115, 1000.000000000000000 ) ;
#50911=EDGE_CURVE ( 'NONE', #56111, #68694, #25992, .T. ) ;
#50916=ADVANCED_FACE ( 'NONE', ( #53224 ), #69464, .F. ) ;
#50921=EDGE_CURVE ( 'NONE', #37725, #31770, #48250, .T. ) ;
#50923=FACE_OUTER_BOUND ( 'NONE', #61329, .T. ) ;
#50929=FACE_OUTER_BOUND ( 'NONE', #53313, .T. ) ;
#50954=ORIENTED_EDGE ( 'NONE', *, *, #57793, .T. ) ;
#50958=ORIENTED_EDGE ( 'NONE', *, *, #39356, .F. ) ;
#50960=AXIS2_PLACEMENT_3D ( 'NONE', #24604, #19630, #9027 ) ;
#50970=DIRECTION ( 'NONE',  ( 0.000000000000000000, 0.000000000000000000, 1.000000000000000000 ) ) ;
#50973=AXIS2_PLACEMENT_3D ( 'NONE', #61231, #12795, #33684 ) ;
#50981=DIRECTION ( 'NONE',  ( 0.000000000000000000, 0.000000000000000000, 1.000000000000000000 ) ) ;
#50992=LINE ( 'NONE', #2550, #18443 ) ;
#50996=CARTESIAN_POINT ( 'NONE',  ( 55.00000000000000000, 21.00000000000000000, 16.96999999999999886 ) ) ;
#50998=AXIS2_PLACEMENT_3D ( 'NONE', #19746, #68905, #42027 ) ;
#51016=ORIENTED_EDGE ( 'NONE', *, *, #28175, .F. ) ;
#51017=CARTESIAN_POINT ( 'NONE',  ( 12.90000000000000213, -21.00000000000000000, 13.86939075806900057 ) ) ;
#51023=DIRECTION ( 'NONE',  ( 0.000000000000000000, 0.000000000000000000, 1.000000000000000000 ) ) ;
#51024=CARTESIAN_POINT ( 'NONE',  ( 22.90000000000000213, 13.66939075806899950, 20.80000000000000426 ) ) ;
#51026=SURFACE_STYLE_USAGE ( .BOTH. , #7877 ) ;
#51033=DIRECTION ( 'NONE',  ( 0.000000000000000000, 0.7071067811865474617, 0.7071067811865474617 ) ) ;
#51034=CYLINDRICAL_SURFACE ( 'NONE', #20789, 2.458500000000000796 ) ;
#51037=EDGE_LOOP ( 'NONE', ( #25117, #48908, #26420, #61905 ) ) ;
#51038=ORIENTED_EDGE ( 'NONE', *, *, #13381, .F. ) ;
#51042=ORIENTED_EDGE ( 'NONE', *, *, #54556, .T. ) ;
#51052=FACE_OUTER_BOUND ( 'NONE', #18027, .T. ) ;
#51060=ORIENTED_EDGE ( 'NONE', *, *, #44844, .T. ) ;
#51068=AXIS2_PLACEMENT_3D ( 'NONE', #64671, #16230, #37807 ) ;
#51070=ORIENTED_EDGE ( 'NONE', *, *, #60045, .F. ) ;
#51077=PLANE ( 'NONE',  #16426 ) ;
#51093=CARTESIAN_POINT ( 'NONE',  ( 49.00000000000000000, -14.06939075806900163, -20.80000000000000426 ) ) ;
#51096=LINE ( 'NONE', #8665, #41835 ) ;
#51097=EDGE_CURVE ( 'NONE', #57808, #35535, #66580, .T. ) ;
#51099=VERTEX_POINT ( 'NONE', #23451 ) ;
#51100=DIRECTION ( 'NONE',  ( 0.000000000000000000, 0.000000000000000000, 1.000000000000000000 ) ) ;
#51109=CARTESIAN_POINT ( 'NONE',  ( 49.00000000000000000, 13.66939075806899950, 20.80000000000000426 ) ) ;
#51112=DIRECTION ( 'NONE',  ( 0.000000000000000000, 0.000000000000000000, 1.000000000000000000 ) ) ;
#51115=CARTESIAN_POINT ( 'NONE',  ( 9.899999999999998579, -21.00000000000001421, -13.86939075806900945 ) ) ;
#51121=FACE_OUTER_BOUND ( 'NONE', #22094, .T. ) ;
#51133=ORIENTED_EDGE ( 'NONE', *, *, #4756, .F. ) ;
#51148=AXIS2_PLACEMENT_3D ( 'NONE', #35633, #8779, #30346 ) ;
#51150=CARTESIAN_POINT ( 'NONE',  ( 30.90000000000000213, -0.1999999999911430404, -8.864436962241481021E-12 ) ) ;
#51151=CARTESIAN_POINT ( 'NONE',  ( 40.90000000000000568, -21.00000000000000000, 13.86939075806900057 ) ) ;
#51154=EDGE_LOOP ( 'NONE', ( #54118, #17286, #39371, #51016 ) ) ;
#51157=( LENGTH_UNIT ( ) NAMED_UNIT ( * ) SI_UNIT ( .MILLI., .METRE. ) );
#51164=DIRECTION ( 'NONE',  ( -1.000000000000000000, 0.000000000000000000, 0.000000000000000000 ) ) ;
#51168=CARTESIAN_POINT ( 'NONE',  ( 0.000000000000000000, -20.50000000000000000, 17.79289321881345032 ) ) ;
#51173=LINE ( 'NONE', #23261, #18544 ) ;
#51181=ADVANCED_FACE ( 'NONE', ( #49964 ), #61967, .F. ) ;
#51194=ORIENTED_EDGE ( 'NONE', *, *, #66090, .T. ) ;
#51196=DIRECTION ( 'NONE',  ( 1.000000000000000000, -0.000000000000000000, 0.000000000000000000 ) ) ;
#51200=DIRECTION ( 'NONE',  ( 0.000000000000000000, 0.000000000000000000, -1.000000000000000000 ) ) ;
#51220=DIRECTION ( 'NONE',  ( -1.000000000000000000, 0.000000000000000000, 0.000000000000000000 ) ) ;
#51224=DIRECTION ( 'NONE',  ( 0.000000000000000000, 0.000000000000000000, -1.000000000000000000 ) ) ;
#51229=ORIENTED_EDGE ( 'NONE', *, *, #27017, .T. ) ;
#51234=ORIENTED_EDGE ( 'NONE', *, *, #64233, .T. ) ;
#51235=DIRECTION ( 'NONE',  ( -1.000000000000000000, 0.000000000000000000, 0.000000000000000000 ) ) ;
#51248=VECTOR ( 'NONE', #59194, 1000.000000000000000 ) ;
#51252=DIRECTION ( 'NONE',  ( 0.000000000000000000, 0.000000000000000000, -1.000000000000000000 ) ) ;
#51260=LINE ( 'NONE', #68594, #65758 ) ;
#51264=EDGE_CURVE ( 'NONE', #21251, #62304, #46751, .T. ) ;
#51267=EDGE_CURVE ( 'NONE', #58100, #51627, #42152, .T. ) ;
#51282=ORIENTED_EDGE ( 'NONE', *, *, #38661, .T. ) ;
#51284=CARTESIAN_POINT ( 'NONE',  ( 39.00000000000000000, 0.000000000000000000, 0.000000000000000000 ) ) ;
#51304=CARTESIAN_POINT ( 'NONE',  ( 35.89999999999999858, 0.000000000000000000, 0.000000000000000000 ) ) ;
#51306=CIRCLE ( 'NONE', #36684, 25.39999999999999858 ) ;
#51308=ORIENTED_EDGE ( 'NONE', *, *, #7555, .T. ) ;
#51320=CARTESIAN_POINT ( 'NONE',  ( 34.89999999999999858, 20.60000000000000142, -13.86939075806900057 ) ) ;
#51324=LINE ( 'NONE', #55937, #45921 ) ;
#51326=VECTOR ( 'NONE', #55306, 1000.000000000000000 ) ;
#51330=CARTESIAN_POINT ( 'NONE',  ( 41.09999999999999432, 20.60000000000000142, 13.86939075806900057 ) ) ;
#51331=DIRECTION ( 'NONE',  ( 0.000000000000000000, 0.000000000000000000, -1.000000000000000000 ) ) ;
#51333=CARTESIAN_POINT ( 'NONE',  ( 40.90000000000000568, -0.1999999999911430404, -8.864436962241481021E-12 ) ) ;
#51351=ORIENTED_EDGE ( 'NONE', *, *, #32159, .F. ) ;
#51368=CARTESIAN_POINT ( 'NONE',  ( 11.90000000000000036, -14.06939075806902117, -20.80000000000000426 ) ) ;
#51374=VERTEX_POINT ( 'NONE', #49547 ) ;
#51394=EDGE_CURVE ( 'NONE', #55707, #9246, #32936, .T. ) ;
#51399=VERTEX_POINT ( 'NONE', #784 ) ;
#51426=VECTOR ( 'NONE', #9479, 1000.000000000000000 ) ;
#51434=CARTESIAN_POINT ( 'NONE',  ( 41.09999999999999432, -14.06939075806900163, 20.80000000000000426 ) ) ;
#51444=CARTESIAN_POINT ( 'NONE',  ( 47.00000000000000000, -0.7500000000000000000, 3.418698582794334584 ) ) ;
#51449=( LENGTH_UNIT ( ) NAMED_UNIT ( * ) SI_UNIT ( .MILLI., .METRE. ) );
#51453=FACE_OUTER_BOUND ( 'NONE', #69648, .T. ) ;
#51456=DIRECTION ( 'NONE',  ( 0.000000000000000000, 0.000000000000000000, 1.000000000000000000 ) ) ;
#51466=CYLINDRICAL_SURFACE ( 'NONE', #40776, 2.458500000000000796 ) ;
#51484=CIRCLE ( 'NONE', #18774, 4.000000000000000000 ) ;
#51486=LINE ( 'NONE', #45827, #40541 ) ;
#51487=ORIENTED_EDGE ( 'NONE', *, *, #11487, .T. ) ;
#51490=VECTOR ( 'NONE', #47710, 1000.000000000000000 ) ;
#51495=VERTEX_POINT ( 'NONE', #66833 ) ;
#51503=DIRECTION ( 'NONE',  ( 1.000000000000000000, 0.000000000000000000, 0.000000000000000000 ) ) ;
#51514=CIRCLE ( 'NONE', #68432, 24.99999999998789946 ) ;
#51523=DIRECTION ( 'NONE',  ( 0.000000000000000000, 0.000000000000000000, -1.000000000000000000 ) ) ;
#51527=CIRCLE ( 'NONE', #21053, 24.99999999998794920 ) ;
#51529=ORIENTED_EDGE ( 'NONE', *, *, #14356, .T. ) ;
#51538=CARTESIAN_POINT ( 'NONE',  ( 22.90000000000000213, -14.06939075806902117, -20.80000000000000426 ) ) ;
#51562=DIRECTION ( 'NONE',  ( 0.000000000000000000, 0.000000000000000000, 1.000000000000000000 ) ) ;
#51563=DIRECTION ( 'NONE',  ( 0.000000000000000000, -1.000000000000000000, 0.000000000000000000 ) ) ;
#51568=ORIENTED_EDGE ( 'NONE', *, *, #3204, .F. ) ;
#51570=AXIS2_PLACEMENT_3D ( 'NONE', #54478, #33585, #6033 ) ;
#51572=DIRECTION ( 'NONE',  ( 0.000000000000000000, 0.000000000000000000, 1.000000000000000000 ) ) ;
#51574=ORIENTED_EDGE ( 'NONE', *, *, #4025, .T. ) ;
#51577=AXIS2_PLACEMENT_3D ( 'NONE', #36358, #15156, #46265 ) ;
#51586=FACE_OUTER_BOUND ( 'NONE', #52082, .T. ) ;
#51587=DIRECTION ( 'NONE',  ( 1.000000000000000000, -0.000000000000000000, 0.000000000000000000 ) ) ;
#51588=EDGE_CURVE ( 'NONE', #69402, #43890, #59996, .T. ) ;
#51594=CARTESIAN_POINT ( 'NONE',  ( 41.09999999999999432, 20.60000000000000142, -13.86939075806900057 ) ) ;
#51602=LINE ( 'NONE', #39574, #52781 ) ;
#51616=CARTESIAN_POINT ( 'NONE',  ( 40.90000000000000568, 0.000000000000000000, 0.000000000000000000 ) ) ;
#51627=VERTEX_POINT ( 'NONE', #34661 ) ;
#51629=LINE ( 'NONE', #3193, #1173 ) ;
#51631=PLANE ( 'NONE',  #41984 ) ;
#51633=ADVANCED_FACE ( 'NONE', ( #17359 ), #38931, .T. ) ;
#51634=EDGE_CURVE ( 'NONE', #66814, #16172, #45344, .T. ) ;
#51645=ORIENTED_EDGE ( 'NONE', *, *, #4944, .F. ) ;
#51650=CARTESIAN_POINT ( 'NONE',  ( 41.09999999999999432, -14.06939075806901940, -20.80000000000000426 ) ) ;
#51666=CARTESIAN_POINT ( 'NONE',  ( 10.90000000000000036, -0.1999999999911430404, -8.864436962241481021E-12 ) ) ;
#51676=CIRCLE ( 'NONE', #3118, 24.99999999998784972 ) ;
#51678=EDGE_CURVE ( 'NONE', #58634, #856, #41981, .T. ) ;
#51712=DIRECTION ( 'NONE',  ( 0.000000000000000000, 0.000000000000000000, -1.000000000000000000 ) ) ;
#51716=AXIS2_PLACEMENT_3D ( 'NONE', #8907, #63722, #57353 ) ;
#51717=VERTEX_POINT ( 'NONE', #54002 ) ;
#51720=FACE_OUTER_BOUND ( 'NONE', #61770, .T. ) ;
#51727=ORIENTED_EDGE ( 'NONE', *, *, #42479, .T. ) ;
#51729=PLANE ( 'NONE',  #34841 ) ;
#51730=LINE ( 'NONE', #67989, #13977 ) ;
#51742=EDGE_CURVE ( 'NONE', #65063, #42085, #4749, .T. ) ;
#51745=AXIS2_PLACEMENT_3D ( 'NONE', #49279, #43614, #69441 ) ;
#51750=LINE ( 'NONE', #53170, #1188 ) ;
#51754=EDGE_CURVE ( 'NONE', #40990, #1707, #38615, .T. ) ;
#51764=EDGE_CURVE ( 'NONE', #31019, #19555, #26423, .T. ) ;
#51765=CARTESIAN_POINT ( 'NONE',  ( 17.89999999999999858, 20.60000000000000142, 13.86939075806899702 ) ) ;
#51785=EDGE_CURVE ( 'NONE', #19388, #17980, #61190, .T. ) ;
#51803=VERTEX_POINT ( 'NONE', #5554 ) ;
#51807=FACE_OUTER_BOUND ( 'NONE', #2408, .T. ) ;
#51823=FACE_OUTER_BOUND ( 'NONE', #47158, .T. ) ;
#51833=VERTEX_POINT ( 'NONE', #17531 ) ;
#51848=ORIENTED_EDGE ( 'NONE', *, *, #21271, .T. ) ;
#51861=CARTESIAN_POINT ( 'NONE',  ( 34.89999999999999858, -21.00000000000000000, 13.86939075806900057 ) ) ;
#51863=CARTESIAN_POINT ( 'NONE',  ( 12.90000000000000213, 20.60000000000000142, -13.86939075806900057 ) ) ;
#51883=DIRECTION ( 'NONE',  ( 1.000000000000000000, -0.000000000000000000, 0.000000000000000000 ) ) ;
#51884=AXIS2_PLACEMENT_3D ( 'NONE', #46184, #41228, #25325 ) ;
#51895=ORIENTED_EDGE ( 'NONE', *, *, #27573, .T. ) ;
#51897=CARTESIAN_POINT ( 'NONE',  ( 0.5000000000000000000, -18.00000000000000355, 21.00000000000000000 ) ) ;
#51903=EDGE_CURVE ( 'NONE', #30310, #34997, #32765, .T. ) ;
#51906=ORIENTED_EDGE ( 'NONE', *, *, #30157, .F. ) ;
#51914=LINE ( 'NONE', #47652, #31575 ) ;
#51938=EDGE_CURVE ( 'NONE', #30889, #7937, #34833, .T. ) ;
#51947=VERTEX_POINT ( 'NONE', #41192 ) ;
#51961=DIRECTION ( 'NONE',  ( 0.000000000000000000, 0.000000000000000000, -1.000000000000000000 ) ) ;
#51969=CARTESIAN_POINT ( 'NONE',  ( 41.09999999999999432, -21.00000000000000000, 13.86939075806900057 ) ) ;
#51970=DIRECTION ( 'NONE',  ( 1.000000000000000000, 0.000000000000000000, 0.000000000000000000 ) ) ;
#51983=ADVANCED_FACE ( 'NONE', ( #2322 ), #39785, .F. ) ;
#51987=CARTESIAN_POINT ( 'NONE',  ( 49.00000000000000000, 13.66939075806899950, 20.80000000000000426 ) ) ;
#52000=LINE ( 'NONE', #51650, #23004 ) ;
#52006=DIRECTION ( 'NONE',  ( -1.000000000000000000, 0.000000000000000000, 0.000000000000000000 ) ) ;
#52008=DIRECTION ( 'NONE',  ( 0.000000000000000000, -0.2142857142857146346, -0.9767710236555243730 ) ) ;
#52035=DIRECTION ( 'NONE',  ( 0.000000000000000000, 0.000000000000000000, 1.000000000000000000 ) ) ;
#52047=CARTESIAN_POINT ( 'NONE',  ( 27.90000000000000213, -0.2000000000089119934, 8.909539772616881237E-12 ) ) ;
#52048=DIRECTION ( 'NONE',  ( 1.000000000000000000, -0.000000000000000000, 0.000000000000000000 ) ) ;
#52062=LINE ( 'NONE', #19526, #9411 ) ;
#52064=DIRECTION ( 'NONE',  ( 0.000000000000000000, 0.000000000000000000, 1.000000000000000000 ) ) ;
#52065=DIRECTION ( 'NONE',  ( 0.000000000000000000, 0.000000000000000000, -1.000000000000000000 ) ) ;
#52068=EDGE_CURVE ( 'NONE', #38301, #37330, #32006, .T. ) ;
#52076=EDGE_CURVE ( 'NONE', #31863, #21068, #43141, .T. ) ;
#52079=AXIS2_PLACEMENT_3D ( 'NONE', #58932, #52948, #69191 ) ;
#52082=EDGE_LOOP ( 'NONE', ( #46352, #13293, #44341, #54949 ) ) ;
#52084=ORIENTED_EDGE ( 'NONE', *, *, #57550, .F. ) ;
#52090=EDGE_CURVE ( 'NONE', #62485, #4332, #1352, .T. ) ;
#52101=FACE_OUTER_BOUND ( 'NONE', #51154, .T. ) ;
#52105=CARTESIAN_POINT ( 'NONE',  ( 36.90000000000000568, 13.66939075806899950, 20.80000000000000426 ) ) ;
#52111=CARTESIAN_POINT ( 'NONE',  ( 31.89999999999999858, -21.00000000000000000, 13.86939075806900057 ) ) ;
#52124=( GEOMETRIC_REPRESENTATION_CONTEXT ( 3 ) GLOBAL_UNCERTAINTY_ASSIGNED_CONTEXT ( ( #57832 ) ) GLOBAL_UNIT_ASSIGNED_CONTEXT ( ( #8524, #67937, #64052 ) ) REPRESENTATION_CONTEXT ( 'NONE', 'WORKASPACE' ) );
#52131=CLOSED_SHELL ( 'NONE', ( #69926, #23140, #36098, #43867, #23690, #55191, #4235, #60772, #32034, #14666, #13547, #21167, #55976, #772 ) ) ;
#52138=EDGE_LOOP ( 'NONE', ( #40895, #40183, #17270, #3666, #8166, #61971, #65071, #22669 ) ) ;
#52141=CARTESIAN_POINT ( 'NONE',  ( 27.00000000000000000, 0.000000000000000000, 0.000000000000000000 ) ) ;
#52159=CARTESIAN_POINT ( 'NONE',  ( 41.09999999999999432, -14.48845687959340012, 21.00000000000000000 ) ) ;
#52163=EDGE_CURVE ( 'NONE', #3626, #38637, #42947, .T. ) ;
#52164=VERTEX_POINT ( 'NONE', #4443 ) ;
#52169=DIRECTION ( 'NONE',  ( 0.000000000000000000, 0.000000000000000000, -1.000000000000000000 ) ) ;
#52173=CARTESIAN_POINT ( 'NONE',  ( 37.90000000000000568, -0.1999999999911795112, 8.826273045769999343E-12 ) ) ;
#52183=DIRECTION ( 'NONE',  ( -1.000000000000000000, 0.000000000000000000, 0.000000000000000000 ) ) ;
#52185=ORIENTED_EDGE ( 'NONE', *, *, #25409, .T. ) ;
#52190=ORIENTED_EDGE ( 'NONE', *, *, #11666, .F. ) ;
#52212=PRESENTATION_STYLE_ASSIGNMENT (( #35228 ) ) ;
#52228=EDGE_CURVE ( 'NONE', #5488, #50027, #44319, .T. ) ;
#52268=ORIENTED_EDGE ( 'NONE', *, *, #59334, .F. ) ;
#52272=EDGE_LOOP ( 'NONE', ( #66718, #28228, #2954, #53265 ) ) ;
#52278=CARTESIAN_POINT ( 'NONE',  ( 24.90000000000000213, -21.00000000000000000, 13.86939075806900057 ) ) ;
#52285=ADVANCED_FACE ( 'NONE', ( #27040 ), #6837, .F. ) ;
#52289=CARTESIAN_POINT ( 'NONE',  ( 17.89999999999999858, 20.60000000000000142, -13.86939075806900057 ) ) ;
#52294=AXIS2_PLACEMENT_3D ( 'NONE', #55189, #44556, #11688 ) ;
#52320=DIRECTION ( 'NONE',  ( 1.000000000000000000, -0.000000000000000000, 0.000000000000000000 ) ) ;
#52328=ORIENTED_EDGE ( 'NONE', *, *, #9846, .F. ) ;
#52335=DIRECTION ( 'NONE',  ( 0.000000000000000000, 0.7071067811865474617, -0.7071067811865474617 ) ) ;
#52344=DIRECTION ( 'NONE',  ( 1.000000000000000000, -0.000000000000000000, 0.000000000000000000 ) ) ;
#52345=CARTESIAN_POINT ( 'NONE',  ( 33.89999999999999858, -0.2000000000089119934, -8.913009219568841313E-12 ) ) ;
#52347=AXIS2_PLACEMENT_3D ( 'NONE', #44750, #19289, #66679 ) ;
#52352=DIRECTION ( 'NONE',  ( 1.000000000000000000, -0.000000000000000000, 0.000000000000000000 ) ) ;
#52371=CARTESIAN_POINT ( 'NONE',  ( 55.00000000000000000, 0.000000000000000000, 0.000000000000000000 ) ) ;
#52393=LINE ( 'NONE', #9968, #61564 ) ;
#52398=DIRECTION ( 'NONE',  ( 0.000000000000000000, 0.000000000000000000, -1.000000000000000000 ) ) ;
#52403=ORIENTED_EDGE ( 'NONE', *, *, #50121, .T. ) ;
#52407=DIRECTION ( 'NONE',  ( 0.000000000000000000, 0.000000000000000000, -1.000000000000000000 ) ) ;
#52421=B_SPLINE_CURVE_WITH_KNOTS ( 'NONE', 3,
 ( #45025, #49983, #1546, #39377 ),
 .UNSPECIFIED., .F., .F.,
 ( 4, 4 ),
 ( 4.336808689942017736E-19, 0.002138888851505100618 ),
 .UNSPECIFIED. ) ;
#52443=ORIENTED_EDGE ( 'NONE', *, *, #21024, .T. ) ;
#52472=CARTESIAN_POINT ( 'NONE',  ( 46.39999999999999858, 21.00000000000000000, -0.7500000000000000000 ) ) ;
#52473=DIRECTION ( 'NONE',  ( 0.000000000000000000, 1.000000000000000000, 0.000000000000000000 ) ) ;
#52474=DIRECTION ( 'NONE',  ( 0.000000000000000000, 0.000000000000000000, 1.000000000000000000 ) ) ;
#52480=DIRECTION ( 'NONE',  ( -1.000000000000000000, 0.000000000000000000, 0.000000000000000000 ) ) ;
#52481=FILL_AREA_STYLE ('',( #15350 ) ) ;
#52483=ORIENTED_EDGE ( 'NONE', *, *, #30341, .T. ) ;
#52491=CARTESIAN_POINT ( 'NONE',  ( 49.00000000000000000, -14.06939075806900163, -20.80000000000000426 ) ) ;
#52502=CARTESIAN_POINT ( 'NONE',  ( 47.00000000000000000, 0.7500000000000000000, -3.418698582794335028 ) ) ;
#52504=LINE ( 'NONE', #21016, #35704 ) ;
#52506=( NAMED_UNIT ( * ) PLANE_ANGLE_UNIT ( ) SI_UNIT ( $, .RADIAN. ) );
#52508=ORIENTED_EDGE ( 'NONE', *, *, #4980, .F. ) ;
#52511=( GEOMETRIC_REPRESENTATION_CONTEXT ( 3 ) GLOBAL_UNCERTAINTY_ASSIGNED_CONTEXT ( ( #16803 ) ) GLOBAL_UNIT_ASSIGNED_CONTEXT ( ( #34449, #39418, #28129 ) ) REPRESENTATION_CONTEXT ( 'NONE', 'WORKASPACE' ) );
#52512=LINE ( 'NONE', #15384, #29336 ) ;
#52529=PLANE ( 'NONE',  #17928 ) ;
#52531=EDGE_LOOP ( 'NONE', ( #59720, #12078, #57671, #57730 ) ) ;
#52540=AXIS2_PLACEMENT_3D ( 'NONE', #62122, #46214, #14754 ) ;
#52563=EDGE_CURVE ( 'NONE', #25374, #13215, #56935, .T. ) ;
#52572=ADVANCED_FACE ( 'NONE', ( #36510, #58081 ), #15657, .T. ) ;
#52589=AXIS2_PLACEMENT_3D ( 'NONE', #65717, #66047, #22246 ) ;
#52593=AXIS2_PLACEMENT_3D ( 'NONE', #35964, #29599, #35240 ) ;
#52599=VECTOR ( 'NONE', #65499, 1000.000000000000000 ) ;
#52600=EDGE_LOOP ( 'NONE', ( #25764, #44227 ) ) ;
#52605=AXIS2_PLACEMENT_3D ( 'NONE', #19361, #50499, #40581 ) ;
#52612=EDGE_LOOP ( 'NONE', ( #57921, #30546, #38751, #32651 ) ) ;
#52615=ORIENTED_EDGE ( 'NONE', *, *, #4732, .F. ) ;
#52616=DIRECTION ( 'NONE',  ( 0.000000000000000000, 0.000000000000000000, -1.000000000000000000 ) ) ;
#52621=AXIS2_PLACEMENT_3D ( 'NONE', #35676, #62914, #56892 ) ;
#52622=DIRECTION ( 'NONE',  ( -1.000000000000000000, 0.000000000000000000, 0.000000000000000000 ) ) ;
#52627=ORIENTED_EDGE ( 'NONE', *, *, #495, .F. ) ;
#52633=DIRECTION ( 'NONE',  ( -1.000000000000000000, 0.000000000000000000, 0.000000000000000000 ) ) ;
#52643=ADVANCED_FACE ( 'NONE', ( #25211 ), #35809, .F. ) ;
#52644=EDGE_LOOP ( 'NONE', ( #55699, #58260, #34760 ) ) ;
#52646=DIRECTION ( 'NONE',  ( 1.000000000000000000, -0.000000000000000000, 0.000000000000000000 ) ) ;
#52668=LINE ( 'NONE', #37097, #61254 ) ;
#52673=SURFACE_STYLE_USAGE ( .BOTH. , #31094 ) ;
#52676=ORIENTED_EDGE ( 'NONE', *, *, #68215, .F. ) ;
#52678=DIRECTION ( 'NONE',  ( 0.000000000000000000, 1.000000000000000000, 0.000000000000000000 ) ) ;
#52679=PLANE ( 'NONE',  #46527 ) ;
#52686=CARTESIAN_POINT ( 'NONE',  ( 46.39999999999999858, 21.00000000000000000, 1.750000000000000222 ) ) ;
#52688=DIRECTION ( 'NONE',  ( 0.000000000000000000, 0.000000000000000000, -1.000000000000000000 ) ) ;
#52700=VECTOR ( 'NONE', #57673, 1000.000000000000000 ) ;
#52701=DIRECTION ( 'NONE',  ( 0.000000000000000000, 0.000000000000000000, -1.000000000000000000 ) ) ;
#52709=VECTOR ( 'NONE', #49788, 1000.000000000000000 ) ;
#52711=CARTESIAN_POINT ( 'NONE',  ( 9.899999999999998579, -0.2000000000089119934, -8.913009219568841313E-12 ) ) ;
#52718=AXIS2_PLACEMENT_3D ( 'NONE', #66685, #23550, #29551 ) ;
#52726=CIRCLE ( 'NONE', #69620, 24.99999999998789946 ) ;
#52741=CARTESIAN_POINT ( 'NONE',  ( 8.900000000000002132, 18.00000000000000355, 21.00000000000000000 ) ) ;
#52742=DIRECTION ( 'NONE',  ( 0.000000000000000000, 0.000000000000000000, -1.000000000000000000 ) ) ;
#52744=EDGE_CURVE ( 'NONE', #15490, #59745, #27646, .T. ) ;
#52746=CARTESIAN_POINT ( 'NONE',  ( 39.90000000000000568, 21.00000000000000000, -13.98999642601811999 ) ) ;
#52747=CIRCLE ( 'NONE', #30101, 25.40000000000000213 ) ;
#52776=DIRECTION ( 'NONE',  ( 0.000000000000000000, 0.5547756303226741847, -0.8320000000000477014 ) ) ;
#52781=VECTOR ( 'NONE', #34264, 1000.000000000000000 ) ;
#52787=ORIENTED_EDGE ( 'NONE', *, *, #60453, .T. ) ;
#52788=CARTESIAN_POINT ( 'NONE',  ( 27.90000000000000213, 20.60000000000000142, 13.86939075806899702 ) ) ;
#52790=CYLINDRICAL_SURFACE ( 'NONE', #64950, 5.250000000000000000 ) ;
#52796=ORIENTED_EDGE ( 'NONE', *, *, #2801, .T. ) ;
#52809=ORIENTED_EDGE ( 'NONE', *, *, #59334, .T. ) ;
#52816=AXIS2_PLACEMENT_3D ( 'NONE', #5806, #6500, #11101 ) ;
#52817=AXIS2_PLACEMENT_3D ( 'NONE', #9683, #14288, #31946 ) ;
#52818=DIRECTION ( 'NONE',  ( 0.000000000000000000, 0.000000000000000000, -1.000000000000000000 ) ) ;
#52828=ORIENTED_EDGE ( 'NONE', *, *, #31819, .F. ) ;
#52831=CARTESIAN_POINT ( 'NONE',  ( 15.89999999999999680, -14.06939075806900874, 20.80000000000001137 ) ) ;
#52836=CARTESIAN_POINT ( 'NONE',  ( 0.000000000000000000, 17.79289321881345032, 20.50000000000000000 ) ) ;
#52843=DIRECTION ( 'NONE',  ( 0.000000000000000000, 0.000000000000000000, -1.000000000000000000 ) ) ;
#52849=CARTESIAN_POINT ( 'NONE',  ( 39.90000000000000568, 0.000000000000000000, 0.000000000000000000 ) ) ;
#52851=VECTOR ( 'NONE', #37978, 1000.000000000000000 ) ;
#52855=DIRECTION ( 'NONE',  ( 1.000000000000000000, -0.000000000000000000, 0.000000000000000000 ) ) ;
#52856=ORIENTED_EDGE ( 'NONE', *, *, #62259, .F. ) ;
#52857=CARTESIAN_POINT ( 'NONE',  ( 20.90000000000000213, 20.60000000000000142, -13.86939075806900057 ) ) ;
#52859=AXIS2_PLACEMENT_3D ( 'NONE', #20579, #14936, #42144 ) ;
#52872=LINE ( 'NONE', #20660, #38503 ) ;
#52909=UNCERTAINTY_MEASURE_WITH_UNIT (LENGTH_MEASURE( 1.000000000000000082E-05 ), #33960, 'distance_accuracy_value', 'NONE');
#52925=CARTESIAN_POINT ( 'NONE',  ( 25.90000000000000213, -0.2000000000089119934, -8.913009219568841313E-12 ) ) ;
#52932=CARTESIAN_POINT ( 'NONE',  ( 39.90000000000000568, -21.00000000000000000, 13.86939075806900057 ) ) ;
#52942=DIRECTION ( 'NONE',  ( -1.000000000000000000, 0.000000000000000000, 0.000000000000000000 ) ) ;
#52948=DIRECTION ( 'NONE',  ( 0.000000000000000000, -1.000000000000000000, 0.000000000000000000 ) ) ;
#52980=CARTESIAN_POINT ( 'NONE',  ( 25.90000000000000213, -14.06939075806900874, 20.80000000000001137 ) ) ;
#52988=ADVANCED_FACE ( 'NONE', ( #57649 ), #57298, .F. ) ;
#52992=CARTESIAN_POINT ( 'NONE',  ( 10.00000000000000000, -18.00000000000000355, -21.00000000000000000 ) ) ;
#52995=CARTESIAN_POINT ( 'NONE',  ( 34.89999999999999858, 0.000000000000000000, 2.458500000000000796 ) ) ;
#52996=ORIENTED_EDGE ( 'NONE', *, *, #57344, .F. ) ;
#53000=CARTESIAN_POINT ( 'NONE',  ( 41.09999999999999432, 20.60000000000000142, -13.86939075806900057 ) ) ;
#53005=SURFACE_STYLE_USAGE ( .BOTH. , #47683 ) ;
#53006=EDGE_LOOP ( 'NONE', ( #19258, #52483 ) ) ;
#53009=CARTESIAN_POINT ( 'NONE',  ( 0.5000000000000000000, 21.00000000000000000, 18.00000000000000355 ) ) ;
#53022=LINE ( 'NONE', #15182, #8506 ) ;
#53047=CARTESIAN_POINT ( 'NONE',  ( 47.00000000000000000, 0.000000000000000000, 5.000000000000000000 ) ) ;
#53072=VECTOR ( 'NONE', #23354, 1000.000000000000114 ) ;
#53089=VECTOR ( 'NONE', #52183, 1000.000000000000000 ) ;
#53092=FILL_AREA_STYLE_COLOUR ( '', #39685 ) ;
#53100=EDGE_CURVE ( 'NONE', #67710, #1557, #5998, .T. ) ;
#53101=CARTESIAN_POINT ( 'NONE',  ( 49.00000000000000000, -14.06939075806900163, -20.80000000000000426 ) ) ;
#53102=CARTESIAN_POINT ( 'NONE',  ( 12.90000000000000213, 0.000000000000000000, 4.309871990004491277E-16 ) ) ;
#53109=ORIENTED_EDGE ( 'NONE', *, *, #38200, .F. ) ;
#53118=DIRECTION ( 'NONE',  ( 0.000000000000000000, 0.000000000000000000, -1.000000000000000000 ) ) ;
#53122=EDGE_CURVE ( 'NONE', #69832, #33868, #48790, .T. ) ;
#53128=VERTEX_POINT ( 'NONE', #21234 ) ;
#53130=VERTEX_POINT ( 'NONE', #43124 ) ;
#53154=DIRECTION ( 'NONE',  ( 1.000000000000000000, -0.000000000000000000, 0.000000000000000000 ) ) ;
#53156=ORIENTED_EDGE ( 'NONE', *, *, #48335, .F. ) ;
#53157=VERTEX_POINT ( 'NONE', #1381 ) ;
#53158=VERTEX_POINT ( 'NONE', #33891 ) ;
#53166=ORIENTED_EDGE ( 'NONE', *, *, #2012, .F. ) ;
#53170=CARTESIAN_POINT ( 'NONE',  ( 10.00000000000000000, 21.00000000000000000, 18.00000000000000355 ) ) ;
#53189=PLANE ( 'NONE',  #68493 ) ;
#53205=ADVANCED_FACE ( 'NONE', ( #55816 ), #39208, .T. ) ;
#53218=DIRECTION ( 'NONE',  ( 0.000000000000000000, 0.000000000000000000, -1.000000000000000000 ) ) ;
#53224=FACE_OUTER_BOUND ( 'NONE', #42179, .T. ) ;
#53226=DIRECTION ( 'NONE',  ( 0.000000000000000000, 0.000000000000000000, -1.000000000000000000 ) ) ;
#53228=VECTOR ( 'NONE', #54607, 1000.000000000000000 ) ;
#53234=DIRECTION ( 'NONE',  ( -1.000000000000000000, 0.000000000000000000, 0.000000000000000000 ) ) ;
#53248=ORIENTED_EDGE ( 'NONE', *, *, #26258, .T. ) ;
#53250=ORIENTED_EDGE ( 'NONE', *, *, #10275, .F. ) ;
#53262=CLOSED_SHELL ( 'NONE', ( #59036, #32368, #30993, #17199, #30473, #50084, #61229, #34566, #2089, #48121, #1709, #52572 ) ) ;
#53264=DIRECTION ( 'NONE',  ( -1.000000000000000000, 0.000000000000000000, 0.000000000000000000 ) ) ;
#53265=ORIENTED_EDGE ( 'NONE', *, *, #60198, .F. ) ;
#53270=FACE_OUTER_BOUND ( 'NONE', #65701, .T. ) ;
#53276=CARTESIAN_POINT ( 'NONE',  ( 9.899999999999998579, 21.00000000000000355, 13.98999642601812354 ) ) ;
#53283=CARTESIAN_POINT ( 'NONE',  ( 40.90000000000000568, -21.00000000000000000, -14.57806571531351914 ) ) ;
#53287=ADVANCED_FACE ( 'NONE', ( #29987 ), #68530, .F. ) ;
#53293=ORIENTED_EDGE ( 'NONE', *, *, #18023, .T. ) ;
#53295=LINE ( 'NONE', #10832, #39638 ) ;
#53308=DIRECTION ( 'NONE',  ( 0.000000000000000000, 0.000000000000000000, -1.000000000000000000 ) ) ;
#53313=EDGE_LOOP ( 'NONE', ( #45554, #7965, #10979, #38851 ) ) ;
#53322=ORIENTED_EDGE ( 'NONE', *, *, #37308, .T. ) ;
#53333=VERTEX_POINT ( 'NONE', #41999 ) ;
#53349=EDGE_CURVE ( 'NONE', #4233, #34215, #51914, .T. ) ;
#53350=( LENGTH_UNIT ( ) NAMED_UNIT ( * ) SI_UNIT ( .MILLI., .METRE. ) );
#53352=( NAMED_UNIT ( * ) PLANE_ANGLE_UNIT ( ) SI_UNIT ( $, .RADIAN. ) );
#53355=CARTESIAN_POINT ( 'NONE',  ( 36.90000000000000568, -0.2000000000089119934, 8.909539772616881237E-12 ) ) ;
#53372=CARTESIAN_POINT ( 'NONE',  ( 49.00000000000000000, 13.66939075806899950, 20.80000000000000426 ) ) ;
#53375=ORIENTED_EDGE ( 'NONE', *, *, #66956, .F. ) ;
#53390=VERTEX_POINT ( 'NONE', #12161 ) ;
#53398=CARTESIAN_POINT ( 'NONE',  ( 0.000000000000000000, -20.50000000000000000, -17.79289321881345032 ) ) ;
#53403=CARTESIAN_POINT ( 'NONE',  ( 39.00000000000000000, 0.000000000000000000, 0.000000000000000000 ) ) ;
#53405=ADVANCED_FACE ( 'NONE', ( #43040 ), #16528, .F. ) ;
#53433=DIRECTION ( 'NONE',  ( 0.000000000000000000, 0.000000000000000000, 1.000000000000000000 ) ) ;
#53444=VECTOR ( 'NONE', #55226, 1000.000000000000000 ) ;
#53445=ORIENTED_EDGE ( 'NONE', *, *, #66967, .F. ) ;
#53454=VECTOR ( 'NONE', #17291, 1000.000000000000000 ) ;
#53467=CIRCLE ( 'NONE', #22953, 2.458500000000000796 ) ;
#53468=ORIENTED_EDGE ( 'NONE', *, *, #27267, .T. ) ;
#53474=CARTESIAN_POINT ( 'NONE',  ( 22.90000000000000213, 13.66939075806899240, 20.79999999999999361 ) ) ;
#53478=VECTOR ( 'NONE', #63875, 1000.000000000000000 ) ;
#53485=DIRECTION ( 'NONE',  ( -1.000000000000000000, 0.000000000000000000, 0.000000000000000000 ) ) ;
#53501=ORIENTED_EDGE ( 'NONE', *, *, #39704, .T. ) ;
#53502=ORIENTED_EDGE ( 'NONE', *, *, #23067, .T. ) ;
#53506=ORIENTED_EDGE ( 'NONE', *, *, #23725, .F. ) ;
#53517=CIRCLE ( 'NONE', #34238, 5.250000000000000000 ) ;
#53521=CARTESIAN_POINT ( 'NONE',  ( 39.90000000000000568, 21.00000000000000000, 16.96999999999999886 ) ) ;
#53525=CARTESIAN_POINT ( 'NONE',  ( 27.90000000000000213, 20.60000000000000142, 2.154935995002245293E-15 ) ) ;
#53529=CARTESIAN_POINT ( 'NONE',  ( 49.00000000000000000, 20.60000000000000142, -13.86939075806900057 ) ) ;
#53532=ORIENTED_EDGE ( 'NONE', *, *, #50911, .T. ) ;
#53557=CARTESIAN_POINT ( 'NONE',  ( 38.90000000000000568, -14.06939075806900163, -20.80000000000000426 ) ) ;
#53571=DIRECTION ( 'NONE',  ( 0.000000000000000000, 0.000000000000000000, -1.000000000000000000 ) ) ;
#53575=ADVANCED_FACE ( 'NONE', ( #56026 ), #65593, .F. ) ;
#53577=VERTEX_POINT ( 'NONE', #12183 ) ;
#53588=ADVANCED_FACE ( 'NONE', ( #13232 ), #6877, .F. ) ;
#53593=UNCERTAINTY_MEASURE_WITH_UNIT (LENGTH_MEASURE( 1.000000000000000082E-05 ), #26311, 'distance_accuracy_value', 'NONE');
#53598=CARTESIAN_POINT ( 'NONE',  ( 27.90000000000000213, -0.2000000000089119934, -8.913009219568841313E-12 ) ) ;
#53606=DIRECTION ( 'NONE',  ( 1.000000000000000000, 0.000000000000000000, 0.000000000000000000 ) ) ;
#53618=DIRECTION ( 'NONE',  ( 0.000000000000000000, 0.000000000000000000, -1.000000000000000000 ) ) ;
#53622=DIRECTION ( 'NONE',  ( 0.000000000000000000, 0.000000000000000000, -1.000000000000000000 ) ) ;
#53632=VECTOR ( 'NONE', #16624, 1000.000000000000000 ) ;
#53638=DIRECTION ( 'NONE',  ( 0.000000000000000000, -1.000000000000000000, 0.000000000000000000 ) ) ;
#53647=AXIS2_PLACEMENT_3D ( 'NONE', #21893, #17274, #43457 ) ;
#53649=DIRECTION ( 'NONE',  ( 1.000000000000000000, -0.000000000000000000, 0.000000000000000000 ) ) ;
#53652=DIRECTION ( 'NONE',  ( 0.000000000000000000, 0.000000000000000000, -1.000000000000000000 ) ) ;
#53653=VERTEX_POINT ( 'NONE', #24196 ) ;
#53654=ORIENTED_EDGE ( 'NONE', *, *, #31436, .T. ) ;
#53658=EDGE_CURVE ( 'NONE', #62865, #34324, #68382, .T. ) ;
#53685=AXIS2_PLACEMENT_3D ( 'NONE', #57850, #8720, #19319 ) ;
#53686=DIRECTION ( 'NONE',  ( 0.000000000000000000, 0.000000000000000000, 1.000000000000000000 ) ) ;
#53713=( LENGTH_UNIT ( ) NAMED_UNIT ( * ) SI_UNIT ( .MILLI., .METRE. ) );
#53723=ORIENTED_EDGE ( 'NONE', *, *, #15597, .F. ) ;
#53733=DIRECTION ( 'NONE',  ( 1.000000000000000000, -0.000000000000000000, 0.000000000000000000 ) ) ;
#53739=DIRECTION ( 'NONE',  ( 0.000000000000000000, 0.000000000000000000, -1.000000000000000000 ) ) ;
#53740=ORIENTED_EDGE ( 'NONE', *, *, #30285, .T. ) ;
#53741=EDGE_LOOP ( 'NONE', ( #549, #63688, #6863, #1192 ) ) ;
#53749=STYLED_ITEM ( 'NONE', ( #41590 ), #19540 ) ;
#53759=ADVANCED_FACE ( 'NONE', ( #4040 ), #30553, .T. ) ;
#53762=EDGE_CURVE ( 'NONE', #21321, #55707, #59872, .T. ) ;
#53789=DIRECTION ( 'NONE',  ( 0.000000000000000000, -1.000000000000000000, 0.000000000000000000 ) ) ;
#53797=VERTEX_POINT ( 'NONE', #32990 ) ;
#53800=LINE ( 'NONE', #32584, #21074 ) ;
#53809=DIRECTION ( 'NONE',  ( 0.000000000000000000, 1.000000000000000000, -0.000000000000000000 ) ) ;
#53814=AXIS2_PLACEMENT_3D ( 'NONE', #15021, #27027, #15725 ) ;
#53823=ORIENTED_EDGE ( 'NONE', *, *, #29764, .T. ) ;
#53829=DIRECTION ( 'NONE',  ( 1.000000000000000000, -0.000000000000000000, 0.000000000000000000 ) ) ;
#53834=VERTEX_POINT ( 'NONE', #58832 ) ;
#53839=CARTESIAN_POINT ( 'NONE',  ( 23.90000000000000213, -0.1999999999911430404, -8.864436962241481021E-12 ) ) ;
#53843=ORIENTED_EDGE ( 'NONE', *, *, #65547, .F. ) ;
#53854=ORIENTED_EDGE ( 'NONE', *, *, #63433, .F. ) ;
#53861=ADVANCED_FACE ( 'NONE', ( #20633 ), #21344, .F. ) ;
#53869=ADVANCED_FACE ( 'NONE', ( #37613 ), #59863, .T. ) ;
#53877=ORIENTED_EDGE ( 'NONE', *, *, #50653, .F. ) ;
#53881=DIRECTION ( 'NONE',  ( 0.000000000000000000, 0.000000000000000000, -1.000000000000000000 ) ) ;
#53889=ORIENTED_EDGE ( 'NONE', *, *, #29573, .T. ) ;
#53897=CARTESIAN_POINT ( 'NONE',  ( 21.90000000000000213, -14.06939075806902117, -20.80000000000000426 ) ) ;
#53911=DIRECTION ( 'NONE',  ( 0.000000000000000000, 1.000000000000000000, 0.000000000000000000 ) ) ;
#53915=LINE ( 'NONE', #59892, #53228 ) ;
#53923=ORIENTED_EDGE ( 'NONE', *, *, #6514, .F. ) ;
#53929=ORIENTED_EDGE ( 'NONE', *, *, #31439, .F. ) ;
#53930=EDGE_CURVE ( 'NONE', #40969, #9904, #30490, .T. ) ;
#53931=EDGE_LOOP ( 'NONE', ( #27974, #18327, #6879, #17097 ) ) ;
#53934=DIRECTION ( 'NONE',  ( 0.000000000000000000, 0.000000000000000000, 1.000000000000000000 ) ) ;
#53935=CIRCLE ( 'NONE', #23427, 0.5000000000000000000 ) ;
#53936=EDGE_CURVE ( 'NONE', #57134, #53130, #38424, .T. ) ;
#53938=ORIENTED_EDGE ( 'NONE', *, *, #68959, .F. ) ;
#53940=ORIENTED_EDGE ( 'NONE', *, *, #30204, .T. ) ;
#53944=CARTESIAN_POINT ( 'NONE',  ( 41.09999999999999432, 20.60000000000000142, -13.86939075806900057 ) ) ;
#53958=EDGE_LOOP ( 'NONE', ( #32937, #30272, #24775, #35067 ) ) ;
#53959=AXIS2_PLACEMENT_3D ( 'NONE', #5391, #64766, #43884 ) ;
#53977=VECTOR ( 'NONE', #49686, 1000.000000000000000 ) ;
#53978=ORIENTED_EDGE ( 'NONE', *, *, #6413, .T. ) ;
#53985=PLANE ( 'NONE',  #24214 ) ;
#53991=EDGE_CURVE ( 'NONE', #13299, #29909, #49933, .T. ) ;
#53999=ORIENTED_EDGE ( 'NONE', *, *, #6473, .T. ) ;
#54002=CARTESIAN_POINT ( 'NONE',  ( 24.90000000000000213, -21.00000000000001421, -13.86939075806900945 ) ) ;
#54003=ADVANCED_FACE ( 'NONE', ( #17409, #60545 ), #65852, .F. ) ;
#54005=ADVANCED_FACE ( 'NONE', ( #13142, #12435 ), #38644, .T. ) ;
#54008=ORIENTED_EDGE ( 'NONE', *, *, #62092, .T. ) ;
#54021=EDGE_CURVE ( 'NONE', #26524, #69579, #50633, .T. ) ;
#54039=CYLINDRICAL_SURFACE ( 'NONE', #60607, 25.39999999999999858 ) ;
#54050=DIRECTION ( 'NONE',  ( 0.000000000000000000, 0.000000000000000000, -1.000000000000000000 ) ) ;
#54051=DIRECTION ( 'NONE',  ( -0.000000000000000000, -1.000000000000000000, 0.000000000000000000 ) ) ;
#54052=CARTESIAN_POINT ( 'NONE',  ( 41.09999999999999432, -14.06939075806900163, 20.80000000000000426 ) ) ;
#54069=ADVANCED_FACE ( 'NONE', ( #62630 ), #40722, .F. ) ;
#54092=VERTEX_POINT ( 'NONE', #19150 ) ;
#54095=PLANE ( 'NONE',  #42603 ) ;
#54107=DIRECTION ( 'NONE',  ( 1.000000000000000000, 0.000000000000000000, 0.000000000000000000 ) ) ;
#54114=VERTEX_POINT ( 'NONE', #8891 ) ;
#54118=ORIENTED_EDGE ( 'NONE', *, *, #44426, .F. ) ;
#54127=DIRECTION ( 'NONE',  ( 0.000000000000000000, 0.000000000000000000, -1.000000000000000000 ) ) ;
#54133=DIRECTION ( 'NONE',  ( 0.000000000000000000, -1.000000000000000000, 0.000000000000000000 ) ) ;
#54144=EDGE_CURVE ( 'NONE', #51803, #6097, #13624, .T. ) ;
#54147=DIRECTION ( 'NONE',  ( -1.000000000000000000, 0.000000000000000000, 0.000000000000000000 ) ) ;
#54153=EDGE_CURVE ( 'NONE', #66814, #57287, #30463, .T. ) ;
#54156=EDGE_LOOP ( 'NONE', ( #67760, #18404, #69711, #66430 ) ) ;
#54162=EDGE_CURVE ( 'NONE', #32793, #35449, #19849, .T. ) ;
#54163=VECTOR ( 'NONE', #44222, 1000.000000000000114 ) ;
#54168=ORIENTED_EDGE ( 'NONE', *, *, #35522, .F. ) ;
#54193=EDGE_LOOP ( 'NONE', ( #67500, #42196, #66676, #43399 ) ) ;
#54196=ADVANCED_FACE ( 'NONE', ( #4653 ), #36467, .F. ) ;
#54197=CARTESIAN_POINT ( 'NONE',  ( 49.00000000000000000, 20.60000000000000142, -13.86939075806900057 ) ) ;
#54216=DIRECTION ( 'NONE',  ( 0.000000000000000000, 0.7071067811865474617, -0.7071067811865474617 ) ) ;
#54224=AXIS2_PLACEMENT_3D ( 'NONE', #34200, #61075, #22242 ) ;
#54230=VERTEX_POINT ( 'NONE', #26214 ) ;
#54236=AXIS2_PLACEMENT_3D ( 'NONE', #50431, #46510, #29195 ) ;
#54237=FACE_OUTER_BOUND ( 'NONE', #3260, .T. ) ;
#54239=CARTESIAN_POINT ( 'NONE',  ( 25.90000000000000213, -0.1999999999911795112, 8.826273045769999343E-12 ) ) ;
#54253=DIRECTION ( 'NONE',  ( 0.000000000000000000, 0.000000000000000000, -1.000000000000000000 ) ) ;
#54278=AXIS2_PLACEMENT_3D ( 'NONE', #61933, #13847, #19498 ) ;
#54286=DIRECTION ( 'NONE',  ( -1.000000000000000000, 0.000000000000000000, 0.000000000000000000 ) ) ;
#54300=CARTESIAN_POINT ( 'NONE',  ( 2.664535259100375697E-15, -20.50000000000000355, -17.79289321881343611 ) ) ;
#54304=DIRECTION ( 'NONE',  ( 1.000000000000000000, 0.000000000000000000, 0.000000000000000000 ) ) ;
#54310=AXIS2_PLACEMENT_3D ( 'NONE', #26768, #48331, #37038 ) ;
#54319=EDGE_CURVE ( 'NONE', #10593, #46953, #26563, .T. ) ;
#54330=EDGE_CURVE ( 'NONE', #60107, #57546, #64400, .T. ) ;
#54333=DIRECTION ( 'NONE',  ( 1.000000000000000000, 0.000000000000000000, 0.000000000000000000 ) ) ;
#54345=FACE_BOUND ( 'NONE', #25216, .T. ) ;
#54350=ORIENTED_EDGE ( 'NONE', *, *, #27442, .T. ) ;
#54355=ADVANCED_FACE ( 'NONE', ( #2110 ), #39241, .T. ) ;
#54359=DIRECTION ( 'NONE',  ( 0.000000000000000000, 0.000000000000000000, -1.000000000000000000 ) ) ;
#54389=DIRECTION ( 'NONE',  ( 0.000000000000000000, -0.7071067811865474617, 0.7071067811865474617 ) ) ;
#54392=DIRECTION ( 'NONE',  ( 0.000000000000000000, -1.000000000000000000, 0.000000000000000000 ) ) ;
#54402=DIRECTION ( 'NONE',  ( 0.000000000000000000, 0.000000000000000000, -1.000000000000000000 ) ) ;
#54408=CARTESIAN_POINT ( 'NONE',  ( 36.90000000000000568, 0.000000000000000000, 0.000000000000000000 ) ) ;
#54417=CLOSED_SHELL ( 'NONE', ( #31116, #30691, #11070, #32387, #35201, #6721, #39726, #5459, #17820, #55259 ) ) ;
#54419=DIRECTION ( 'NONE',  ( 0.000000000000000000, -1.000000000000000000, 0.000000000000000000 ) ) ;
#54420=EDGE_CURVE ( 'NONE', #40026, #61739, #38228, .T. ) ;
#54421=DIRECTION ( 'NONE',  ( 0.000000000000000000, 0.000000000000000000, 1.000000000000000000 ) ) ;
#54426=CYLINDRICAL_SURFACE ( 'NONE', #35594, 24.99999999998789946 ) ;
#54427=ORIENTED_EDGE ( 'NONE', *, *, #9965, .F. ) ;
#54440=CYLINDRICAL_SURFACE ( 'NONE', #33219, 3.500000000000000000 ) ;
#54441=AXIS2_PLACEMENT_3D ( 'NONE', #25240, #4723, #15330 ) ;
#54450=AXIS2_PLACEMENT_3D ( 'NONE', #60041, #16919, #44121 ) ;
#54459=EDGE_CURVE ( 'NONE', #47029, #50321, #40634, .T. ) ;
#54478=CARTESIAN_POINT ( 'NONE',  ( 47.00000000000000000, 0.000000000000000000, 0.000000000000000000 ) ) ;
#54481=AXIS2_PLACEMENT_3D ( 'NONE', #53372, #26148, #63628 ) ;
#54493=LINE ( 'NONE', #6046, #14191 ) ;
#54502=AXIS2_PLACEMENT_3D ( 'NONE', #15792, #36661, #31381 ) ;
#54517=CARTESIAN_POINT ( 'NONE',  ( 29.89999999999999858, 13.66939075806899240, -20.79999999999999361 ) ) ;
#54525=VECTOR ( 'NONE', #1532, 1000.000000000000000 ) ;
#54529=( LENGTH_UNIT ( ) NAMED_UNIT ( * ) SI_UNIT ( .MILLI., .METRE. ) );
#54547=CARTESIAN_POINT ( 'NONE',  ( 23.90000000000000213, -21.00000000000000000, 13.86939075806900057 ) ) ;
#54556=EDGE_CURVE ( 'NONE', #20722, #21068, #56204, .T. ) ;
#54564=ORIENTED_EDGE ( 'NONE', *, *, #37164, .F. ) ;
#54585=STYLED_ITEM ( 'NONE', ( #14466 ), #42921 ) ;
#54590=EDGE_LOOP ( 'NONE', ( #43244, #66769 ) ) ;
#54592=DIRECTION ( 'NONE',  ( 0.000000000000000000, 0.2142857142857145514, 0.9767710236555243730 ) ) ;
#54607=DIRECTION ( 'NONE',  ( 0.000000000000000000, 1.000000000000000000, 0.000000000000000000 ) ) ;
#54608=ORIENTED_EDGE ( 'NONE', *, *, #65195, .T. ) ;
#54612=EDGE_LOOP ( 'NONE', ( #66766, #69831, #45630, #39703 ) ) ;
#54616=ORIENTED_EDGE ( 'NONE', *, *, #56804, .F. ) ;
#54619=DIRECTION ( 'NONE',  ( -1.000000000000000000, 0.000000000000000000, 0.000000000000000000 ) ) ;
#54625=VERTEX_POINT ( 'NONE', #42732 ) ;
#54631=AXIS2_PLACEMENT_3D ( 'NONE', #9666, #31240, #52818 ) ;
#54637=VECTOR ( 'NONE', #17053, 1000.000000000000000 ) ;
#54638=ADVANCED_FACE ( 'NONE', ( #9515 ), #47340, .F. ) ;
#54640=DIRECTION ( 'NONE',  ( -1.000000000000000000, -0.000000000000000000, -0.000000000000000000 ) ) ;
#54643=CARTESIAN_POINT ( 'NONE',  ( 55.00000000000000000, -21.00000000000000000, 16.96999999999999886 ) ) ;
#54655=DIRECTION ( 'NONE',  ( 0.000000000000000000, 0.000000000000000000, -1.000000000000000000 ) ) ;
#54659=CARTESIAN_POINT ( 'NONE',  ( 39.00000000000000000, 21.00000000000000000, -13.98999642601811999 ) ) ;
#54660=CARTESIAN_POINT ( 'NONE',  ( 9.900000000000000355, 18.00000000000000355, 21.00000000000000000 ) ) ;
#54666=DIRECTION ( 'NONE',  ( 1.000000000000000000, 0.000000000000000000, 0.000000000000000000 ) ) ;
#54673=ORIENTED_EDGE ( 'NONE', *, *, #34412, .T. ) ;
#54680=CARTESIAN_POINT ( 'NONE',  ( 0.5000000000000000000, -18.00000000000000355, 21.00000000000000000 ) ) ;
#54682=EDGE_LOOP ( 'NONE', ( #15189, #30868, #15183, #60295, #58698, #68279, #46670, #1296 ) ) ;
#54685=DIRECTION ( 'NONE',  ( 0.000000000000000000, 0.000000000000000000, -1.000000000000000000 ) ) ;
#54692=ORIENTED_EDGE ( 'NONE', *, *, #29497, .F. ) ;
#54711=EDGE_CURVE ( 'NONE', #41932, #32778, #37367, .T. ) ;
#54719=ORIENTED_EDGE ( 'NONE', *, *, #21271, .F. ) ;
#54724=DIRECTION ( 'NONE',  ( 0.000000000000000000, 0.000000000000000000, -1.000000000000000000 ) ) ;
#54729=DIRECTION ( 'NONE',  ( 0.000000000000000000, 0.000000000000000000, -1.000000000000000000 ) ) ;
#54731=SURFACE_STYLE_USAGE ( .BOTH. , #55758 ) ;
#54751=LINE ( 'NONE', #28900, #33829 ) ;
#54755=DIRECTION ( 'NONE',  ( 0.000000000000000000, 0.000000000000000000, 1.000000000000000000 ) ) ;
#54763=CARTESIAN_POINT ( 'NONE',  ( 39.00000000000000000, -21.00000000000000000, -14.57806571531351914 ) ) ;
#54764=LINE ( 'NONE', #49796, #28828 ) ;
#54765=ORIENTED_EDGE ( 'NONE', *, *, #21305, .T. ) ;
#54769=CYLINDRICAL_SURFACE ( 'NONE', #50209, 24.99999999998784972 ) ;
#54784=MECHANICAL_DESIGN_GEOMETRIC_PRESENTATION_REPRESENTATION('',(#5126),#10765);
#54786=CARTESIAN_POINT ( 'NONE',  ( 30.90000000000000213, 20.60000000000000142, -13.86939075806900057 ) ) ;
#54788=ORIENTED_EDGE ( 'NONE', *, *, #63507, .T. ) ;
#54789=ORIENTED_EDGE ( 'NONE', *, *, #44863, .T. ) ;
#54794=LINE ( 'NONE', #44505, #62670 ) ;
#54802=EDGE_LOOP ( 'NONE', ( #26338, #49498, #67104, #32943 ) ) ;
#54819=DIRECTION ( 'NONE',  ( 0.000000000000000000, 0.7071067811865475727, 0.7071067811865475727 ) ) ;
#54843=LINE ( 'NONE', #6401, #17981 ) ;
#54852=ADVANCED_FACE ( 'NONE', ( #39160 ), #60721, .F. ) ;
#54853=VERTEX_POINT ( 'NONE', #63088 ) ;
#54857=VECTOR ( 'NONE', #31393, 1000.000000000000000 ) ;
#54863=ORIENTED_EDGE ( 'NONE', *, *, #26, .F. ) ;
#54867=AXIS2_PLACEMENT_3D ( 'NONE', #22791, #18169, #17835 ) ;
#54869=VECTOR ( 'NONE', #29041, 1000.000000000000000 ) ;
#54879=LINE ( 'NONE', #1129, #19881 ) ;
#54882=ORIENTED_EDGE ( 'NONE', *, *, #20690, .T. ) ;
#54885=VERTEX_POINT ( 'NONE', #47524 ) ;
#54891=EDGE_CURVE ( 'NONE', #55138, #53577, #56577, .T. ) ;
#54894=DIRECTION ( 'NONE',  ( 0.000000000000000000, 0.000000000000000000, 1.000000000000000000 ) ) ;
#54905=CARTESIAN_POINT ( 'NONE',  ( 48.83285635894858245, -0.7500000000000019984, -3.758896888126563862 ) ) ;
#54906=ORIENTED_EDGE ( 'NONE', *, *, #45139, .T. ) ;
#54926=VECTOR ( 'NONE', #5678, 1000.000000000000000 ) ;
#54927=CARTESIAN_POINT ( 'NONE',  ( 25.90000000000000213, 20.60000000000000142, -13.86939075806900057 ) ) ;
#54928=FACE_OUTER_BOUND ( 'NONE', #35839, .T. ) ;
#54929=CARTESIAN_POINT ( 'NONE',  ( 49.00000000000000000, -5.000000000000000000, 0.000000000000000000 ) ) ;
#54930=DIRECTION ( 'NONE',  ( 1.000000000000000000, -0.000000000000000000, 0.000000000000000000 ) ) ;
#54931=AXIS2_PLACEMENT_3D ( 'NONE', #30552, #36197, #52474 ) ;
#54933=VECTOR ( 'NONE', #50156, 1000.000000000000000 ) ;
#54934=DIRECTION ( 'NONE',  ( 1.000000000000000000, -0.000000000000000000, 0.000000000000000000 ) ) ;
#54939=CARTESIAN_POINT ( 'NONE',  ( 29.89999999999999858, -21.00000000000001421, -13.86939075806900945 ) ) ;
#54944=CARTESIAN_POINT ( 'NONE',  ( 8.900000000000005684, -0.2000000000089119934, 8.909539772616881237E-12 ) ) ;
#54949=ORIENTED_EDGE ( 'NONE', *, *, #16243, .F. ) ;
#54952=LINE ( 'NONE', #32673, #711 ) ;
#54955=DIRECTION ( 'NONE',  ( 0.000000000000000000, 0.000000000000000000, -1.000000000000000000 ) ) ;
#54961=CARTESIAN_POINT ( 'NONE',  ( 8.900000000000005684, -21.00000000000000000, 18.00000000000000355 ) ) ;
#54964=DIRECTION ( 'NONE',  ( -1.000000000000000000, 0.000000000000000000, 0.000000000000000000 ) ) ;
#54970=CIRCLE ( 'NONE', #51570, 5.000000000000000000 ) ;
#54988=VERTEX_POINT ( 'NONE', #69091 ) ;
#54996=VECTOR ( 'NONE', #47419, 1000.000000000000000 ) ;
#54997=CARTESIAN_POINT ( 'NONE',  ( 28.90000000000000213, 20.60000000000000142, 13.86939075806900057 ) ) ;
#55002=CARTESIAN_POINT ( 'NONE',  ( 10.00000000000000000, -14.48845687959340012, -21.00000000000000000 ) ) ;
#55023=( GEOMETRIC_REPRESENTATION_CONTEXT ( 3 ) GLOBAL_UNCERTAINTY_ASSIGNED_CONTEXT ( ( #6187 ) ) GLOBAL_UNIT_ASSIGNED_CONTEXT ( ( #12318, #50165, #44855 ) ) REPRESENTATION_CONTEXT ( 'NONE', 'WORKASPACE' ) );
#55030=DIRECTION ( 'NONE',  ( 0.000000000000000000, 0.000000000000000000, -1.000000000000000000 ) ) ;
#55032=FACE_OUTER_BOUND ( 'NONE', #27382, .T. ) ;
#55040=EDGE_CURVE ( 'NONE', #61720, #40050, #21703, .T. ) ;
#55058=ORIENTED_EDGE ( 'NONE', *, *, #63855, .T. ) ;
#55060=CARTESIAN_POINT ( 'NONE',  ( 13.90000000000000036, 0.000000000000000000, 6.464807985006735683E-16 ) ) ;
#55066=AXIS2_PLACEMENT_3D ( 'NONE', #35573, #20376, #13664 ) ;
#55068=CARTESIAN_POINT ( 'NONE',  ( 36.90000000000000568, -21.00000000000000000, 13.86939075806900057 ) ) ;
#55075=ORIENTED_EDGE ( 'NONE', *, *, #67010, .T. ) ;
#55085=LINE ( 'NONE', #23925, #30222 ) ;
#55086=( NAMED_UNIT ( * ) SI_UNIT ( $, .STERADIAN. ) SOLID_ANGLE_UNIT ( ) );
#55094=ORIENTED_EDGE ( 'NONE', *, *, #58327, .T. ) ;
#55099=DIRECTION ( 'NONE',  ( -1.000000000000000000, 0.000000000000000000, 0.000000000000000000 ) ) ;
#55107=CARTESIAN_POINT ( 'NONE',  ( 20.90000000000000213, -0.2000000000089119934, 8.909539772616881237E-12 ) ) ;
#55108=CARTESIAN_POINT ( 'NONE',  ( 38.90000000000000568, -14.06939075806900874, 20.80000000000001137 ) ) ;
#55138=VERTEX_POINT ( 'NONE', #65862 ) ;
#55143=CARTESIAN_POINT ( 'NONE',  ( 30.90000000000000213, 0.000000000000000000, 2.458500000000000796 ) ) ;
#55154=ORIENTED_EDGE ( 'NONE', *, *, #15016, .F. ) ;
#55175=CIRCLE ( 'NONE', #15666, 24.99999999998794920 ) ;
#55176=DIRECTION ( 'NONE',  ( 1.000000000000000000, -0.000000000000000000, 0.000000000000000000 ) ) ;
#55184=CARTESIAN_POINT ( 'NONE',  ( 9.900000000000000355, 0.000000000000000000, 2.154935995002245639E-16 ) ) ;
#55189=CARTESIAN_POINT ( 'NONE',  ( 40.90000000000000568, 0.000000000000000000, 3.447897592003593022E-15 ) ) ;
#55191=ADVANCED_FACE ( 'NONE', ( #56298 ), #38989, .T. ) ;
#55192=CARTESIAN_POINT ( 'NONE',  ( 46.39999999999999858, 21.00000000000000000, -0.7500000000000000000 ) ) ;
#55198=ADVANCED_FACE ( 'NONE', ( #7146 ), #61581, .F. ) ;
#55201=ORIENTED_EDGE ( 'NONE', *, *, #62265, .T. ) ;
#55216=EDGE_LOOP ( 'NONE', ( #36082, #40342, #14709, #18005 ) ) ;
#55226=DIRECTION ( 'NONE',  ( -1.000000000000000000, 0.000000000000000000, 0.000000000000000000 ) ) ;
#55227=EDGE_CURVE ( 'NONE', #23509, #24837, #22733, .T. ) ;
#55239=EDGE_CURVE ( 'NONE', #2916, #12117, #45324, .T. ) ;
#55241=DIRECTION ( 'NONE',  ( -1.000000000000000000, 0.000000000000000000, 0.000000000000000000 ) ) ;
#55247=FACE_OUTER_BOUND ( 'NONE', #44692, .T. ) ;
#55250=DIRECTION ( 'NONE',  ( 1.000000000000000000, 0.000000000000000000, 0.000000000000000000 ) ) ;
#55259=ADVANCED_FACE ( 'NONE', ( #24116 ), #29418, .T. ) ;
#55264=FACE_OUTER_BOUND ( 'NONE', #41848, .T. ) ;
#55288=DIRECTION ( 'NONE',  ( 0.000000000000000000, 0.000000000000000000, -1.000000000000000000 ) ) ;
#55289=EDGE_CURVE ( 'NONE', #39379, #20422, #2899, .T. ) ;
#55298=LINE ( 'NONE', #50326, #66904 ) ;
#55305=ORIENTED_EDGE ( 'NONE', *, *, #4548, .T. ) ;
#55306=DIRECTION ( 'NONE',  ( 1.000000000000000000, 0.000000000000000000, 0.000000000000000000 ) ) ;
#55308=AXIS2_PLACEMENT_3D ( 'NONE', #38755, #49388, #21804 ) ;
#55315=VECTOR ( 'NONE', #26838, 1000.000000000000000 ) ;
#55317=ORIENTED_EDGE ( 'NONE', *, *, #49440, .F. ) ;
#55339=EDGE_CURVE ( 'NONE', #4916, #43945, #43107, .T. ) ;
#55343=CARTESIAN_POINT ( 'NONE',  ( 14.89999999999999680, 13.66939075806899950, 20.80000000000000426 ) ) ;
#55344=AXIS2_PLACEMENT_3D ( 'NONE', #60697, #18595, #55399 ) ;
#55361=AXIS2_PLACEMENT_3D ( 'NONE', #8732, #13680, #61772 ) ;
#55371=AXIS2_PLACEMENT_3D ( 'NONE', #62347, #19225, #13916 ) ;
#55382=VERTEX_POINT ( 'NONE', #69353 ) ;
#55388=DIRECTION ( 'NONE',  ( 0.000000000000000000, 0.000000000000000000, 1.000000000000000000 ) ) ;
#55393=CARTESIAN_POINT ( 'NONE',  ( 0.5000000000000000000, 21.00000000000000000, -18.00000000000000355 ) ) ;
#55394=CARTESIAN_POINT ( 'NONE',  ( 8.900000000000002132, 18.00000000000000355, 21.00000000000000000 ) ) ;
#55399=DIRECTION ( 'NONE',  ( 0.000000000000000000, 0.000000000000000000, 1.000000000000000000 ) ) ;
#55409=CIRCLE ( 'NONE', #2303, 5.000000000000000000 ) ;
#55413=ADVANCED_FACE ( 'NONE', ( #58754 ), #48844, .F. ) ;
#55418=ADVANCED_FACE ( 'NONE', ( #31540 ), #21624, .F. ) ;
#55423=SURFACE_STYLE_FILL_AREA ( #6282 ) ;
#55424=VERTEX_POINT ( 'NONE', #10651 ) ;
#55425=VERTEX_POINT ( 'NONE', #5006 ) ;
#55435=CARTESIAN_POINT ( 'NONE',  ( 19.90000000000000213, -0.1999999999911430404, -8.864436962241481021E-12 ) ) ;
#55464=DIRECTION ( 'NONE',  ( 0.000000000000000000, 0.000000000000000000, 1.000000000000000000 ) ) ;
#55474=DIRECTION ( 'NONE',  ( 1.000000000000000000, -0.000000000000000000, 0.000000000000000000 ) ) ;
#55486=VERTEX_POINT ( 'NONE', #5375 ) ;
#55504=CARTESIAN_POINT ( 'NONE',  ( 41.09999999999999432, -21.00000000000000000, 13.86939075806900057 ) ) ;
#55508=ORIENTED_EDGE ( 'NONE', *, *, #51754, .T. ) ;
#55509=PLANE ( 'NONE',  #44905 ) ;
#55541=DIRECTION ( 'NONE',  ( 1.000000000000000000, -0.000000000000000000, 0.000000000000000000 ) ) ;
#55543=PRESENTATION_STYLE_ASSIGNMENT (( #12383 ) ) ;
#55549=ORIENTED_EDGE ( 'NONE', *, *, #15636, .T. ) ;
#55554=( NAMED_UNIT ( * ) SI_UNIT ( $, .STERADIAN. ) SOLID_ANGLE_UNIT ( ) );
#55573=FACE_OUTER_BOUND ( 'NONE', #54682, .T. ) ;
#55615=ORIENTED_EDGE ( 'NONE', *, *, #50694, .F. ) ;
#55616=VERTEX_POINT ( 'NONE', #11678 ) ;
#55617=AXIS2_PLACEMENT_3D ( 'NONE', #60988, #54666, #23167 ) ;
#55620=ORIENTED_EDGE ( 'NONE', *, *, #12947, .T. ) ;
#55657=B_SPLINE_CURVE_WITH_KNOTS ( 'NONE', 3,
 ( #33325, #54905, #6458, #6779 ),
 .UNSPECIFIED., .F., .F.,
 ( 4, 4 ),
 ( 0.0009978974790779693294, 0.7140570275647658560 ),
 .UNSPECIFIED. ) ;
#55659=CARTESIAN_POINT ( 'NONE',  ( 41.09999999999999432, -14.06939075806900163, 20.80000000000000426 ) ) ;
#55680=LINE ( 'NONE', #62369, #31192 ) ;
#55681=ORIENTED_EDGE ( 'NONE', *, *, #11737, .F. ) ;
#55687=DIRECTION ( 'NONE',  ( 0.000000000000000000, 0.2142857142857145514, 0.9767710236555243730 ) ) ;
#55689=VECTOR ( 'NONE', #14450, 1000.000000000000000 ) ;
#55699=ORIENTED_EDGE ( 'NONE', *, *, #49695, .F. ) ;
#55707=VERTEX_POINT ( 'NONE', #35682 ) ;
#55710=CIRCLE ( 'NONE', #46677, 24.99999999998789946 ) ;
#55722=COLOUR_RGB ( '', 0.72549020, 0.75294118, 0.79215686) ;
#55731=ORIENTED_EDGE ( 'NONE', *, *, #2084, .F. ) ;
#55733=EDGE_LOOP ( 'NONE', ( #25359, #22551, #55914, #57545 ) ) ;
#55740=EDGE_CURVE ( 'NONE', #42432, #60403, #40644, .T. ) ;
#55743=DIRECTION ( 'NONE',  ( 0.000000000000000000, -1.000000000000000000, 0.000000000000000000 ) ) ;
#55744=ORIENTED_EDGE ( 'NONE', *, *, #3518, .F. ) ;
#55745=EDGE_CURVE ( 'NONE', #12180, #42535, #46647, .T. ) ;
#55750=DIRECTION ( 'NONE',  ( 0.000000000000000000, 0.000000000000000000, 1.000000000000000000 ) ) ;
#55754=ADVANCED_FACE ( 'NONE', ( #36040 ), #57611, .F. ) ;
#55758=SURFACE_SIDE_STYLE ('',( #55423 ) ) ;
#55764=AXIS2_PLACEMENT_3D ( 'NONE', #45222, #61478, #35662 ) ;
#55768=VECTOR ( 'NONE', #51712, 1000.000000000000000 ) ;
#55775=CARTESIAN_POINT ( 'NONE',  ( 49.00000000000000000, -0.2000000000089119934, -8.913009219568841313E-12 ) ) ;
#55780=CARTESIAN_POINT ( 'NONE',  ( 39.00000000000000000, -16.96999999999999886, 21.00000000000000000 ) ) ;
#55784=DIRECTION ( 'NONE',  ( 1.000000000000000000, -0.000000000000000000, 0.000000000000000000 ) ) ;
#55789=ADVANCED_FACE ( 'NONE', ( #65017, #10921 ), #52679, .F. ) ;
#55790=LINE ( 'NONE', #18295, #67016 ) ;
#55794=AXIS2_PLACEMENT_3D ( 'NONE', #54944, #16759, #60220 ) ;
#55816=FACE_OUTER_BOUND ( 'NONE', #9181, .T. ) ;
#55819=ORIENTED_EDGE ( 'NONE', *, *, #50125, .F. ) ;
#55820=CARTESIAN_POINT ( 'NONE',  ( 46.39999999999999858, 33.00000000000000000, -0.7500000000000000000 ) ) ;
#55821=ORIENTED_EDGE ( 'NONE', *, *, #29506, .T. ) ;
#55832=DIRECTION ( 'NONE',  ( 0.000000000000000000, -1.000000000000000000, 0.000000000000000000 ) ) ;
#55835=CARTESIAN_POINT ( 'NONE',  ( 47.00000000000000000, 6.123233995736766282E-16, -5.000000000000000000 ) ) ;
#55836=CARTESIAN_POINT ( 'NONE',  ( 17.89999999999999858, -0.1999999999911795112, 8.826273045769999343E-12 ) ) ;
#55838=ADVANCED_FACE ( 'NONE', ( #31103 ), #32139, .F. ) ;
#55866=CARTESIAN_POINT ( 'NONE',  ( 49.00000000000000000, -0.1999999999911430404, -8.864436962241481021E-12 ) ) ;
#55872=LINE ( 'NONE', #33617, #53072 ) ;
#55888=ORIENTED_EDGE ( 'NONE', *, *, #8156, .T. ) ;
#55899=CARTESIAN_POINT ( 'NONE',  ( 55.00000000000000000, 0.000000000000000000, 5.250000000000000000 ) ) ;
#55904=ORIENTED_EDGE ( 'NONE', *, *, #18023, .F. ) ;
#55906=LINE ( 'NONE', #66515, #29862 ) ;
#55911=AXIS2_PLACEMENT_3D ( 'NONE', #24067, #67912, #3564 ) ;
#55913=ORIENTED_EDGE ( 'NONE', *, *, #9376, .T. ) ;
#55914=ORIENTED_EDGE ( 'NONE', *, *, #420, .T. ) ;
#55922=AXIS2_PLACEMENT_3D ( 'NONE', #46768, #69760, #63402 ) ;
#55927=FACE_OUTER_BOUND ( 'NONE', #53958, .T. ) ;
#55937=CARTESIAN_POINT ( 'NONE',  ( 41.09999999999999432, 20.60000000000000142, 13.86939075806900057 ) ) ;
#55944=ORIENTED_EDGE ( 'NONE', *, *, #4214, .F. ) ;
#55946=PLANE ( 'NONE',  #13129 ) ;
#55948=DIRECTION ( 'NONE',  ( -1.000000000000000000, 0.000000000000000000, 0.000000000000000000 ) ) ;
#55949=CARTESIAN_POINT ( 'NONE',  ( 34.89999999999999858, -0.1999999999911795112, 8.826273045769999343E-12 ) ) ;
#55976=ADVANCED_FACE ( 'NONE', ( #33520 ), #38488, .F. ) ;
#55985=AXIS2_PLACEMENT_3D ( 'NONE', #55435, #17590, #23585 ) ;
#56000=AXIS2_PLACEMENT_3D ( 'NONE', #58570, #10118, #25329 ) ;
#56002=CARTESIAN_POINT ( 'NONE',  ( 21.90000000000000213, 20.60000000000000142, -13.86939075806900057 ) ) ;
#56005=ORIENTED_EDGE ( 'NONE', *, *, #34029, .T. ) ;
#56007=VECTOR ( 'NONE', #68414, 1000.000000000000000 ) ;
#56009=DIRECTION ( 'NONE',  ( 0.000000000000000000, -1.000000000000000000, 0.000000000000000000 ) ) ;
#56011=DIRECTION ( 'NONE',  ( 0.000000000000000000, -1.000000000000000000, 0.000000000000000000 ) ) ;
#56012=VECTOR ( 'NONE', #2520, 1000.000000000000000 ) ;
#56015=DIRECTION ( 'NONE',  ( 0.000000000000000000, 0.000000000000000000, 1.000000000000000000 ) ) ;
#56025=EDGE_CURVE ( 'NONE', #17228, #61430, #57843, .T. ) ;
#56026=FACE_OUTER_BOUND ( 'NONE', #7963, .T. ) ;
#56031=DIRECTION ( 'NONE',  ( -1.000000000000000000, 0.000000000000000000, 0.000000000000000000 ) ) ;
#56035=EDGE_CURVE ( 'NONE', #2764, #62836, #2514, .T. ) ;
#56038=EDGE_LOOP ( 'NONE', ( #53740, #61735, #5764, #17350 ) ) ;
#56039=EDGE_CURVE ( 'NONE', #56183, #15490, #39754, .T. ) ;
#56041=CARTESIAN_POINT ( 'NONE',  ( 36.90000000000000568, -14.06939075806900874, 20.80000000000001137 ) ) ;
#56047=LINE ( 'NONE', #62037, #37596 ) ;
#56048=EDGE_LOOP ( 'NONE', ( #61092, #40777, #23474, #34483 ) ) ;
#56056=CARTESIAN_POINT ( 'NONE',  ( 39.00000000000000000, 16.96999999999999886, -21.00000000000000000 ) ) ;
#56065=ORIENTED_EDGE ( 'NONE', *, *, #25802, .F. ) ;
#56074=EDGE_LOOP ( 'NONE', ( #31333, #22328, #30563 ) ) ;
#56083=ORIENTED_EDGE ( 'NONE', *, *, #23486, .F. ) ;
#56097=MECHANICAL_DESIGN_GEOMETRIC_PRESENTATION_REPRESENTATION('',(#50445),#65162);
#56111=VERTEX_POINT ( 'NONE', #23942 ) ;
#56117=EDGE_CURVE ( 'NONE', #60377, #60100, #26260, .T. ) ;
#56132=DIRECTION ( 'NONE',  ( -1.000000000000000000, 0.000000000000000000, 0.000000000000000000 ) ) ;
#56133=ORIENTED_EDGE ( 'NONE', *, *, #49354, .T. ) ;
#56147=DIRECTION ( 'NONE',  ( 0.000000000000000000, 0.000000000000000000, -1.000000000000000000 ) ) ;
#56155=CARTESIAN_POINT ( 'NONE',  ( 39.00000000000000000, 16.96999999999999886, 21.00000000000000000 ) ) ;
#56165=AXIS2_PLACEMENT_3D ( 'NONE', #15371, #59197, #43273 ) ;
#56166=PLANE ( 'NONE',  #32698 ) ;
#56171=DIRECTION ( 'NONE',  ( 1.000000000000000000, -0.000000000000000000, 0.000000000000000000 ) ) ;
#56175=DIRECTION ( 'NONE',  ( -0.000000000000000000, -1.000000000000000000, 0.000000000000000000 ) ) ;
#56183=VERTEX_POINT ( 'NONE', #67779 ) ;
#56190=DIRECTION ( 'NONE',  ( 0.000000000000000000, 0.000000000000000000, -1.000000000000000000 ) ) ;
#56195=CARTESIAN_POINT ( 'NONE',  ( 10.90000000000000036, -0.1999999999911795112, 8.826273045769999343E-12 ) ) ;
#56202=EDGE_CURVE ( 'NONE', #32122, #53390, #31717, .T. ) ;
#56204=LINE ( 'NONE', #20470, #10265 ) ;
#56206=EDGE_CURVE ( 'NONE', #57523, #17475, #26753, .T. ) ;
#56211=SURFACE_SIDE_STYLE ('',( #60807 ) ) ;
#56222=DIRECTION ( 'NONE',  ( 0.000000000000000000, -1.000000000000000000, 0.000000000000000000 ) ) ;
#56224=EDGE_CURVE ( 'NONE', #68694, #7560, #43001, .T. ) ;
#56225=CARTESIAN_POINT ( 'NONE',  ( 9.900000000000000355, 21.00000000000000000, -18.00000000000000355 ) ) ;
#56246=CARTESIAN_POINT ( 'NONE',  ( 36.90000000000000568, -0.2000000000089119934, -8.913009219568841313E-12 ) ) ;
#56261=VERTEX_POINT ( 'NONE', #37366 ) ;
#56262=ORIENTED_EDGE ( 'NONE', *, *, #56206, .T. ) ;
#56273=CARTESIAN_POINT ( 'NONE',  ( 40.90000000000000568, 21.00000000000000000, 13.98999642601811999 ) ) ;
#56274=DIRECTION ( 'NONE',  ( -1.000000000000000000, 0.000000000000000000, 0.000000000000000000 ) ) ;
#56280=DIRECTION ( 'NONE',  ( 0.000000000000000000, 1.000000000000000000, 0.000000000000000000 ) ) ;
#56296=ADVANCED_FACE ( 'NONE', ( #37029, #26402 ), #9435, .F. ) ;
#56298=FACE_OUTER_BOUND ( 'NONE', #19851, .T. ) ;
#56299=DIRECTION ( 'NONE',  ( 0.000000000000000000, 0.000000000000000000, -1.000000000000000000 ) ) ;
#56305=LINE ( 'NONE', #50996, #27771 ) ;
#56313=CARTESIAN_POINT ( 'NONE',  ( 41.09999999999999432, 13.66939075806899950, 20.80000000000000426 ) ) ;
#56320=VERTEX_POINT ( 'NONE', #25717 ) ;
#56324=CIRCLE ( 'NONE', #1026, 24.99999999998794920 ) ;
#56343=DIRECTION ( 'NONE',  ( 0.000000000000000000, 0.000000000000000000, -1.000000000000000000 ) ) ;
#56347=DIRECTION ( 'NONE',  ( 0.000000000000000000, 1.000000000000000000, -0.000000000000000000 ) ) ;
#56358=DIRECTION ( 'NONE',  ( -1.000000000000000000, 0.000000000000000000, 0.000000000000000000 ) ) ;
#56359=CYLINDRICAL_SURFACE ( 'NONE', #37484, 24.99999999998784972 ) ;
#56361=CARTESIAN_POINT ( 'NONE',  ( 39.90000000000000568, 0.000000000000000000, 0.000000000000000000 ) ) ;
#56369=ADVANCED_FACE ( 'NONE', ( #50037 ), #940, .F. ) ;
#56379=DIRECTION ( 'NONE',  ( -1.000000000000000000, 0.000000000000000000, 0.000000000000000000 ) ) ;
#56380=LINE ( 'NONE', #34103, #6576 ) ;
#56392=CARTESIAN_POINT ( 'NONE',  ( 16.89999999999999858, 20.60000000000000142, -13.86939075806900057 ) ) ;
#56401=FACE_OUTER_BOUND ( 'NONE', #31824, .T. ) ;
#56402=ORIENTED_EDGE ( 'NONE', *, *, #49090, .F. ) ;
#56411=EDGE_CURVE ( 'NONE', #24688, #31770, #226, .T. ) ;
#56413=CARTESIAN_POINT ( 'NONE',  ( 41.09999999999999432, -21.00000000000000000, -13.86939075806900057 ) ) ;
#56414=ORIENTED_EDGE ( 'NONE', *, *, #59381, .F. ) ;
#56421=ORIENTED_EDGE ( 'NONE', *, *, #31102, .T. ) ;
#56432=ORIENTED_EDGE ( 'NONE', *, *, #22534, .T. ) ;
#56436=ORIENTED_EDGE ( 'NONE', *, *, #38511, .T. ) ;
#56454=DIRECTION ( 'NONE',  ( 0.000000000000000000, 0.000000000000000000, -1.000000000000000000 ) ) ;
#56458=AXIS2_PLACEMENT_3D ( 'NONE', #32840, #54421, #50821 ) ;
#56467=CYLINDRICAL_SURFACE ( 'NONE', #15711, 24.99999999998784972 ) ;
#56477=FACE_OUTER_BOUND ( 'NONE', #1240, .T. ) ;
#56478=DIRECTION ( 'NONE',  ( 0.000000000000000000, 0.000000000000000000, 1.000000000000000000 ) ) ;
#56491=CARTESIAN_POINT ( 'NONE',  ( 20.90000000000000213, -21.00000000000001421, -13.86939075806900945 ) ) ;
#56493=CYLINDRICAL_SURFACE ( 'NONE', #52605, 25.39999999999999858 ) ;
#56511=EDGE_LOOP ( 'NONE', ( #35919, #47835, #33207, #18977 ) ) ;
#56531=LINE ( 'NONE', #24709, #59468 ) ;
#56543=DIRECTION ( 'NONE',  ( -1.000000000000000000, 0.000000000000000000, 0.000000000000000000 ) ) ;
#56547=EDGE_CURVE ( 'NONE', #54114, #2916, #67698, .T. ) ;
#56555=ORIENTED_EDGE ( 'NONE', *, *, #5490, .T. ) ;
#56559=DIRECTION ( 'NONE',  ( -1.000000000000000000, 0.000000000000000000, 0.000000000000000000 ) ) ;
#56563=LINE ( 'NONE', #29681, #69349 ) ;
#56568=VECTOR ( 'NONE', #62062, 1000.000000000000000 ) ;
#56570=CARTESIAN_POINT ( 'NONE',  ( 47.00000000000000000, -0.7500000000000000000, 4.943429983321300014 ) ) ;
#56577=CIRCLE ( 'NONE', #4664, 24.99999999998784972 ) ;
#56579=CARTESIAN_POINT ( 'NONE',  ( 48.50000000000000000, -0.7500000000000000000, -3.418698582794335028 ) ) ;
#56580=DIRECTION ( 'NONE',  ( 1.000000000000000000, 0.000000000000000000, 0.000000000000000000 ) ) ;
#56581=EDGE_LOOP ( 'NONE', ( #55913, #58205 ) ) ;
#56585=ADVANCED_FACE ( 'NONE', ( #57443 ), #41172, .T. ) ;
#56586=DIRECTION ( 'NONE',  ( 0.000000000000000000, 1.000000000000000000, -0.000000000000000000 ) ) ;
#56600=ORIENTED_EDGE ( 'NONE', *, *, #2650, .T. ) ;
#56616=EDGE_CURVE ( 'NONE', #40050, #54625, #38758, .T. ) ;
#56617=CLOSED_SHELL ( 'NONE', ( #30438, #25744, #46431, #21346, #35935, #32, #63242, #61717, #47511, #56296, #18631, #27755 ) ) ;
#56629=CARTESIAN_POINT ( 'NONE',  ( 41.09999999999999432, 20.60000000000000142, -13.86939075806900057 ) ) ;
#56630=LINE ( 'NONE', #29401, #62824 ) ;
#56644=CIRCLE ( 'NONE', #32929, 2.458500000000000796 ) ;
#56653=DIRECTION ( 'NONE',  ( 0.000000000000000000, 0.000000000000000000, -1.000000000000000000 ) ) ;
#56654=VECTOR ( 'NONE', #66099, 1000.000000000000000 ) ;
#56666=CARTESIAN_POINT ( 'NONE',  ( 49.00000000000000000, 20.60000000000000142, -13.86939075806900057 ) ) ;
#56680=PRESENTATION_STYLE_ASSIGNMENT (( #51026 ) ) ;
#56687=ORIENTED_EDGE ( 'NONE', *, *, #16372, .F. ) ;
#56693=ORIENTED_EDGE ( 'NONE', *, *, #7316, .F. ) ;
#56698=ORIENTED_EDGE ( 'NONE', *, *, #10275, .T. ) ;
#56721=EDGE_CURVE ( 'NONE', #19077, #31121, #66964, .T. ) ;
#56728=AXIS2_PLACEMENT_3D ( 'NONE', #54408, #50474, #44457 ) ;
#56731=EDGE_LOOP ( 'NONE', ( #42346, #52809, #56432, #17061 ) ) ;
#56732=DIRECTION ( 'NONE',  ( -1.000000000000000000, 0.000000000000000000, 0.000000000000000000 ) ) ;
#56733=FACE_OUTER_BOUND ( 'NONE', #45017, .T. ) ;
#56734=CIRCLE ( 'NONE', #5974, 5.250000000000000000 ) ;
#56747=CARTESIAN_POINT ( 'NONE',  ( 49.00000000000000000, -0.7500000000000000000, 4.943429983321300014 ) ) ;
#56751=ORIENTED_EDGE ( 'NONE', *, *, #63498, .F. ) ;
#56761=CARTESIAN_POINT ( 'NONE',  ( 49.00000000000000000, 13.66939075806899950, 20.80000000000000426 ) ) ;
#56773=CARTESIAN_POINT ( 'NONE',  ( 46.39999999999999858, 21.00000000000000000, 2.750000000000000444 ) ) ;
#56784=DIRECTION ( 'NONE',  ( 1.000000000000000000, 0.000000000000000000, 0.000000000000000000 ) ) ;
#56790=VECTOR ( 'NONE', #15269, 1000.000000000000000 ) ;
#56798=DIRECTION ( 'NONE',  ( -1.000000000000000000, 0.000000000000000000, 0.000000000000000000 ) ) ;
#56799=CARTESIAN_POINT ( 'NONE',  ( 13.90000000000000036, -0.000000000000000000, -20.80000000000000426 ) ) ;
#56802=DIRECTION ( 'NONE',  ( 0.000000000000000000, 0.000000000000000000, -1.000000000000000000 ) ) ;
#56804=EDGE_CURVE ( 'NONE', #58634, #53797, #17299, .T. ) ;
#56805=CARTESIAN_POINT ( 'NONE',  ( 31.89999999999999858, 20.60000000000000142, -13.86939075806900057 ) ) ;
#56809=CARTESIAN_POINT ( 'NONE',  ( 55.00000000000000000, 16.96999999999999886, 21.00000000000000000 ) ) ;
#56820=VERTEX_POINT ( 'NONE', #1434 ) ;
#56846=ADVANCED_FACE ( 'NONE', ( #33619, #23002 ), #33278, .F. ) ;
#56853=CARTESIAN_POINT ( 'NONE',  ( 17.89999999999999858, -14.06939075806900874, 20.80000000000001137 ) ) ;
#56857=PRODUCT_CONTEXT ( 'NONE', #46719, 'mechanical' ) ;
#56891=CARTESIAN_POINT ( 'NONE',  ( 40.90000000000000568, -21.00000000000000000, 13.86939075806900057 ) ) ;
#56892=DIRECTION ( 'NONE',  ( 0.000000000000000000, 0.000000000000000000, 1.000000000000000000 ) ) ;
#56903=PLANE ( 'NONE',  #64019 ) ;
#56913=CARTESIAN_POINT ( 'NONE',  ( 28.90000000000000213, 20.60000000000000142, -13.86939075806900057 ) ) ;
#56917=AXIS2_PLACEMENT_3D ( 'NONE', #15291, #42849, #52064 ) ;
#56933=CARTESIAN_POINT ( 'NONE',  ( 8.900000000000002132, 0.000000000000000000, 0.000000000000000000 ) ) ;
#56935=CIRCLE ( 'NONE', #9510, 3.500000000000000000 ) ;
#56936=DIRECTION ( 'NONE',  ( 0.000000000000000000, 0.000000000000000000, 1.000000000000000000 ) ) ;
#56962=SURFACE_STYLE_USAGE ( .BOTH. , #63692 ) ;
#56965=CARTESIAN_POINT ( 'NONE',  ( 41.09999999999999432, -14.48845687959340012, -21.00000000000000000 ) ) ;
#56988=EDGE_CURVE ( 'NONE', #13299, #43994, #64713, .T. ) ;
#56991=CARTESIAN_POINT ( 'NONE',  ( 10.00000000000000000, -21.00000000000000000, -18.00000000000000355 ) ) ;
#57009=EDGE_CURVE ( 'NONE', #53333, #62865, #51260, .T. ) ;
#57010=CARTESIAN_POINT ( 'NONE',  ( 13.90000000000000213, -21.00000000000000000, 13.86939075806900057 ) ) ;
#57013=ORIENTED_EDGE ( 'NONE', *, *, #67945, .T. ) ;
#57028=ORIENTED_EDGE ( 'NONE', *, *, #2650, .F. ) ;
#57041=( GEOMETRIC_REPRESENTATION_CONTEXT ( 3 ) GLOBAL_UNCERTAINTY_ASSIGNED_CONTEXT ( ( #31681 ) ) GLOBAL_UNIT_ASSIGNED_CONTEXT ( ( #38648, #11757, #44281 ) ) REPRESENTATION_CONTEXT ( 'NONE', 'WORKASPACE' ) );
#57058=ORIENTED_EDGE ( 'NONE', *, *, #5996, .F. ) ;
#57062=CARTESIAN_POINT ( 'NONE',  ( 0.5000000000000000000, -21.00000000000000000, 18.00000000000000355 ) ) ;
#57077=VECTOR ( 'NONE', #9112, 1000.000000000000000 ) ;
#57100=FILL_AREA_STYLE ('',( #7612 ) ) ;
#57110=DIRECTION ( 'NONE',  ( -1.000000000000000000, 0.000000000000000000, 0.000000000000000000 ) ) ;
#57122=CIRCLE ( 'NONE', #4043, 24.99999999998789946 ) ;
#57130=CIRCLE ( 'NONE', #43557, 2.458500000000000796 ) ;
#57134=VERTEX_POINT ( 'NONE', #32510 ) ;
#57141=( GEOMETRIC_REPRESENTATION_CONTEXT ( 3 ) GLOBAL_UNCERTAINTY_ASSIGNED_CONTEXT ( ( #3396 ) ) GLOBAL_UNIT_ASSIGNED_CONTEXT ( ( #31112, #4243, #58336 ) ) REPRESENTATION_CONTEXT ( 'NONE', 'WORKASPACE' ) );
#57149=ADVANCED_FACE ( 'NONE', ( #63998 ), #4593, .T. ) ;
#57155=LINE ( 'NONE', #14014, #13256 ) ;
#57179=EDGE_LOOP ( 'NONE', ( #54882, #48909, #66779, #22464 ) ) ;
#57190=CARTESIAN_POINT ( 'NONE',  ( 31.89999999999999858, 0.000000000000000000, 2.458500000000000796 ) ) ;
#57191=VECTOR ( 'NONE', #34552, 1000.000000000000000 ) ;
#57193=CARTESIAN_POINT ( 'NONE',  ( 40.90000000000000568, -21.00000000000000000, -16.96999999999999886 ) ) ;
#57210=CARTESIAN_POINT ( 'NONE',  ( 9.900000000000000355, 14.08845687959340331, 21.00000000000000000 ) ) ;
#57213=FACE_OUTER_BOUND ( 'NONE', #66250, .T. ) ;
#57219=EDGE_CURVE ( 'NONE', #44331, #361, #61195, .T. ) ;
#57221=CARTESIAN_POINT ( 'NONE',  ( 39.00000000000000000, 16.96999999999999886, 21.00000000000000000 ) ) ;
#57242=FILL_AREA_STYLE ('',( #40624 ) ) ;
#57246=DIRECTION ( 'NONE',  ( 0.000000000000000000, 0.000000000000000000, 1.000000000000000000 ) ) ;
#57247=CARTESIAN_POINT ( 'NONE',  ( 41.09999999999999432, -21.00000000000000000, -13.86939075806900057 ) ) ;
#57257=EDGE_LOOP ( 'NONE', ( #53501, #6424, #56262, #48972 ) ) ;
#57261=VECTOR ( 'NONE', #40986, 1000.000000000000000 ) ;
#57287=VERTEX_POINT ( 'NONE', #66043 ) ;
#57292=DIRECTION ( 'NONE',  ( 0.000000000000000000, -1.000000000000000000, 0.000000000000000000 ) ) ;
#57294=CARTESIAN_POINT ( 'NONE',  ( 39.00000000000000000, 0.000000000000000000, 0.000000000000000000 ) ) ;
#57298=PLANE ( 'NONE',  #21975 ) ;
#57301=LINE ( 'NONE', #47048, #63541 ) ;
#57305=EDGE_CURVE ( 'NONE', #16845, #68516, #55790, .T. ) ;
#57306=LINE ( 'NONE', #20523, #24215 ) ;
#57313=FACE_OUTER_BOUND ( 'NONE', #63238, .T. ) ;
#57323=CIRCLE ( 'NONE', #52817, 5.250000000000000000 ) ;
#57344=EDGE_CURVE ( 'NONE', #40439, #12122, #60744, .T. ) ;
#57350=DIRECTION ( 'NONE',  ( 1.000000000000000000, -0.000000000000000000, 0.000000000000000000 ) ) ;
#57353=DIRECTION ( 'NONE',  ( 0.000000000000000000, 0.000000000000000000, -1.000000000000000000 ) ) ;
#57382=ORIENTED_EDGE ( 'NONE', *, *, #42837, .T. ) ;
#57389=EDGE_CURVE ( 'NONE', #361, #42085, #24310, .T. ) ;
#57401=DIRECTION ( 'NONE',  ( -1.000000000000000000, 0.000000000000000000, 0.000000000000000000 ) ) ;
#57421=VERTEX_POINT ( 'NONE', #57190 ) ;
#57435=EDGE_CURVE ( 'NONE', #53128, #64055, #3797, .T. ) ;
#57443=FACE_OUTER_BOUND ( 'NONE', #38765, .T. ) ;
#57469=CARTESIAN_POINT ( 'NONE',  ( 41.09999999999999432, -0.2000000000000000111, 0.000000000000000000 ) ) ;
#57472=EDGE_CURVE ( 'NONE', #16386, #17050, #46147, .T. ) ;
#57475=DIRECTION ( 'NONE',  ( -0.7071067811865472397, -0.5000000000000002220, -0.5000000000000002220 ) ) ;
#57500=VECTOR ( 'NONE', #41395, 1000.000000000000000 ) ;
#57504=DIRECTION ( 'NONE',  ( -1.000000000000000000, 0.000000000000000000, 0.000000000000000000 ) ) ;
#57508=DIRECTION ( 'NONE',  ( -1.000000000000000000, 0.000000000000000000, 0.000000000000000000 ) ) ;
#57514=SURFACE_SIDE_STYLE ('',( #62822 ) ) ;
#57515=AXIS2_PLACEMENT_3D ( 'NONE', #67479, #34919, #19368 ) ;
#57523=VERTEX_POINT ( 'NONE', #19986 ) ;
#57532=DIRECTION ( 'NONE',  ( 0.000000000000000000, 1.000000000000000000, 0.000000000000000000 ) ) ;
#57534=VECTOR ( 'NONE', #63804, 1000.000000000000000 ) ;
#57542=DIRECTION ( 'NONE',  ( 0.000000000000000000, -1.000000000000000000, 0.000000000000000000 ) ) ;
#57544=LINE ( 'NONE', #9825, #57077 ) ;
#57545=ORIENTED_EDGE ( 'NONE', *, *, #49121, .F. ) ;
#57546=VERTEX_POINT ( 'NONE', #62762 ) ;
#57549=EDGE_LOOP ( 'NONE', ( #20978, #54673, #40803, #37327 ) ) ;
#57550=EDGE_CURVE ( 'NONE', #45925, #42134, #9015, .T. ) ;
#57551=CARTESIAN_POINT ( 'NONE',  ( 9.900000000000000355, 0.000000000000000000, 2.154935995002245639E-16 ) ) ;
#57552=DIRECTION ( 'NONE',  ( 0.000000000000000000, 0.000000000000000000, 1.000000000000000000 ) ) ;
#57556=EDGE_CURVE ( 'NONE', #58634, #59658, #35901, .T. ) ;
#57557=DIRECTION ( 'NONE',  ( 1.000000000000000000, -0.000000000000000000, 0.000000000000000000 ) ) ;
#57564=EDGE_LOOP ( 'NONE', ( #3972, #39340, #27240, #59191, #57653, #34129, #25598, #49138 ) ) ;
#57568=EDGE_CURVE ( 'NONE', #42522, #36943, #34141, .T. ) ;
#57569=DIRECTION ( 'NONE',  ( 0.000000000000000000, 1.000000000000000000, 0.000000000000000000 ) ) ;
#57570=VECTOR ( 'NONE', #61261, 1000.000000000000000 ) ;
#57576=FACE_OUTER_BOUND ( 'NONE', #34905, .T. ) ;
#57578=EDGE_LOOP ( 'NONE', ( #20173, #39176, #56600, #69183, #38504, #39330, #10548, #6796 ) ) ;
#57583=PLANE ( 'NONE',  #29011 ) ;
#57592=FACE_OUTER_BOUND ( 'NONE', #30415, .T. ) ;
#57597=CARTESIAN_POINT ( 'NONE',  ( 8.900000000000002132, -21.00000000000000000, -18.00000000000000355 ) ) ;
#57599=DIRECTION ( 'NONE',  ( -1.000000000000000000, 0.000000000000000000, 0.000000000000000000 ) ) ;
#57602=CARTESIAN_POINT ( 'NONE',  ( 33.89999999999999858, -21.00000000000000000, 13.86939075806900057 ) ) ;
#57608=DIRECTION ( 'NONE',  ( 0.000000000000000000, 0.000000000000000000, -1.000000000000000000 ) ) ;
#57611=CYLINDRICAL_SURFACE ( 'NONE', #9296, 25.39999999999999858 ) ;
#57615=CARTESIAN_POINT ( 'NONE',  ( 47.00000000000000000, 0.7500000000000000000, 3.418698582794335028 ) ) ;
#57619=DIRECTION ( 'NONE',  ( 0.000000000000000000, -1.000000000000000000, 0.000000000000000000 ) ) ;
#57624=VECTOR ( 'NONE', #60994, 1000.000000000000000 ) ;
#57649=FACE_OUTER_BOUND ( 'NONE', #29680, .T. ) ;
#57653=ORIENTED_EDGE ( 'NONE', *, *, #15144, .T. ) ;
#57654=ORIENTED_EDGE ( 'NONE', *, *, #58593, .F. ) ;
#57664=DIRECTION ( 'NONE',  ( 1.000000000000000000, -0.000000000000000000, 0.000000000000000000 ) ) ;
#57668=VECTOR ( 'NONE', #54133, 1000.000000000000000 ) ;
#57671=ORIENTED_EDGE ( 'NONE', *, *, #17384, .T. ) ;
#57673=DIRECTION ( 'NONE',  ( -1.000000000000000000, 0.000000000000000000, 0.000000000000000000 ) ) ;
#57699=CARTESIAN_POINT ( 'NONE',  ( 29.89999999999999858, -0.2000000000089119934, 8.909539772616881237E-12 ) ) ;
#57726=CARTESIAN_POINT ( 'NONE',  ( 17.89999999999999858, -21.00000000000000000, 13.86939075806900057 ) ) ;
#57730=ORIENTED_EDGE ( 'NONE', *, *, #29573, .F. ) ;
#57733=VECTOR ( 'NONE', #39790, 1000.000000000000000 ) ;
#57739=DIRECTION ( 'NONE',  ( -1.000000000000000000, 0.000000000000000000, 0.000000000000000000 ) ) ;
#57755=EDGE_CURVE ( 'NONE', #62211, #54853, #55298, .T. ) ;
#57767=LINE ( 'NONE', #42202, #18181 ) ;
#57781=CLOSED_SHELL ( 'NONE', ( #68355, #58351, #47119, #6792, #4688, #55198, #1367, #34065, #50388, #41870 ) ) ;
#57793=EDGE_CURVE ( 'NONE', #31832, #13993, #44315, .T. ) ;
#57798=( LENGTH_UNIT ( ) NAMED_UNIT ( * ) SI_UNIT ( .MILLI., .METRE. ) );
#57808=VERTEX_POINT ( 'NONE', #54961 ) ;
#57810=CARTESIAN_POINT ( 'NONE',  ( 9.900000000000000355, 18.00000000000000355, 21.00000000000000000 ) ) ;
#57815=DIRECTION ( 'NONE',  ( -1.000000000000000000, 0.000000000000000000, 0.000000000000000000 ) ) ;
#57825=PLANE ( 'NONE',  #38425 ) ;
#57827=ORIENTED_EDGE ( 'NONE', *, *, #26258, .F. ) ;
#57832=UNCERTAINTY_MEASURE_WITH_UNIT (LENGTH_MEASURE( 1.000000000000000082E-05 ), #8524, 'distance_accuracy_value', 'NONE');
#57843=CIRCLE ( 'NONE', #40922, 24.99999999998784972 ) ;
#57847=EDGE_LOOP ( 'NONE', ( #37382, #23495, #59648, #49086 ) ) ;
#57848=( NAMED_UNIT ( * ) SI_UNIT ( $, .STERADIAN. ) SOLID_ANGLE_UNIT ( ) );
#57850=CARTESIAN_POINT ( 'NONE',  ( 15.89999999999999680, -0.2000000000089119934, 8.909539772616881237E-12 ) ) ;
#57858=CARTESIAN_POINT ( 'NONE',  ( 39.00000000000000000, -21.00000000000000000, 16.96999999999999886 ) ) ;
#57887=EDGE_CURVE ( 'NONE', #62304, #35449, #13890, .T. ) ;
#57888=VERTEX_POINT ( 'NONE', #3994 ) ;
#57889=CARTESIAN_POINT ( 'NONE',  ( 13.90000000000000213, 13.66939075806899240, -20.79999999999999361 ) ) ;
#57890=EDGE_CURVE ( 'NONE', #29633, #21334, #29801, .T. ) ;
#57900=LINE ( 'NONE', #41279, #36230 ) ;
#57901=VERTEX_POINT ( 'NONE', #25568 ) ;
#57917=DIRECTION ( 'NONE',  ( -1.000000000000000000, 0.000000000000000000, 0.000000000000000000 ) ) ;
#57921=ORIENTED_EDGE ( 'NONE', *, *, #35295, .F. ) ;
#57942=( GEOMETRIC_REPRESENTATION_CONTEXT ( 3 ) GLOBAL_UNCERTAINTY_ASSIGNED_CONTEXT ( ( #5504 ) ) GLOBAL_UNIT_ASSIGNED_CONTEXT ( ( #41262, #14756, #67086 ) ) REPRESENTATION_CONTEXT ( 'NONE', 'WORKASPACE' ) );
#57952=SURFACE_STYLE_FILL_AREA ( #63265 ) ;
#57954=LINE ( 'NONE', #42740, #19818 ) ;
#57967=DIRECTION ( 'NONE',  ( -1.000000000000000000, 0.000000000000000000, 0.000000000000000000 ) ) ;
#57976=ORIENTED_EDGE ( 'NONE', *, *, #36756, .T. ) ;
#57979=EDGE_LOOP ( 'NONE', ( #42509, #1228, #8610, #8912 ) ) ;
#57980=AXIS2_PLACEMENT_3D ( 'NONE', #62157, #25393, #9130 ) ;
#57985=ORIENTED_EDGE ( 'NONE', *, *, #40574, .F. ) ;
#57993=FACE_OUTER_BOUND ( 'NONE', #50692, .T. ) ;
#57999=COLOUR_RGB ( '', 0.31764706, 0.68627451, 0.89019608) ;
#58001=VERTEX_POINT ( 'NONE', #32949 ) ;
#58020=ORIENTED_EDGE ( 'NONE', *, *, #52563, .T. ) ;
#58021=CARTESIAN_POINT ( 'NONE',  ( 49.00000000000000000, -0.1999999999911430404, -8.864436962241481021E-12 ) ) ;
#58034=FACE_OUTER_BOUND ( 'NONE', #36687, .T. ) ;
#58060=EDGE_CURVE ( 'NONE', #8950, #30328, #25184, .T. ) ;
#58064=ORIENTED_EDGE ( 'NONE', *, *, #6841, .F. ) ;
#58066=CARTESIAN_POINT ( 'NONE',  ( 41.09999999999999432, 13.66939075806899950, -20.80000000000000426 ) ) ;
#58079=AXIS2_PLACEMENT_3D ( 'NONE', #152, #38327, #54592 ) ;
#58081=FACE_OUTER_BOUND ( 'NONE', #10573, .T. ) ;
#58092=AXIS2_PLACEMENT_3D ( 'NONE', #43222, #38618, #21666 ) ;
#58100=VERTEX_POINT ( 'NONE', #5035 ) ;
#58103=ORIENTED_EDGE ( 'NONE', *, *, #32950, .T. ) ;
#58114=DIRECTION ( 'NONE',  ( 0.000000000000000000, 0.000000000000000000, -1.000000000000000000 ) ) ;
#58121=DIRECTION ( 'NONE',  ( -1.000000000000000000, 0.000000000000000000, 0.000000000000000000 ) ) ;
#58122=FACE_OUTER_BOUND ( 'NONE', #69972, .T. ) ;
#58134=SURFACE_STYLE_USAGE ( .BOTH. , #47530 ) ;
#58136=DIRECTION ( 'NONE',  ( 0.000000000000000000, -1.000000000000000000, 0.000000000000000000 ) ) ;
#58147=CARTESIAN_POINT ( 'NONE',  ( 40.90000000000000568, -16.96999999999999886, -21.00000000000000000 ) ) ;
#58153=DIRECTION ( 'NONE',  ( 1.000000000000000000, -0.000000000000000000, 0.000000000000000000 ) ) ;
#58156=EDGE_CURVE ( 'NONE', #42522, #29082, #29360, .T. ) ;
#58159=CARTESIAN_POINT ( 'NONE',  ( 39.90000000000000568, 21.00000000000000000, -16.96999999999999886 ) ) ;
#58176=LINE ( 'NONE', #37320, #8824 ) ;
#58187=CIRCLE ( 'NONE', #49154, 24.99999999998784972 ) ;
#58191=PLANE ( 'NONE',  #32319 ) ;
#58205=ORIENTED_EDGE ( 'NONE', *, *, #33509, .T. ) ;
#58206=AXIS2_PLACEMENT_3D ( 'NONE', #5461, #58136, #42573 ) ;
#58213=CARTESIAN_POINT ( 'NONE',  ( 41.09999999999999432, 13.66939075806899950, 20.80000000000000426 ) ) ;
#58226=AXIS2_PLACEMENT_3D ( 'NONE', #50098, #38469, #54729 ) ;
#58227=DIRECTION ( 'NONE',  ( 0.000000000000000000, 0.000000000000000000, 1.000000000000000000 ) ) ;
#58232=DIRECTION ( 'NONE',  ( 0.000000000000000000, 1.000000000000000000, 0.000000000000000000 ) ) ;
#58237=AXIS2_PLACEMENT_3D ( 'NONE', #51093, #30580, #46834 ) ;
#58253=CARTESIAN_POINT ( 'NONE',  ( 41.09999999999999432, 21.00000000000000000, 13.98999642601811999 ) ) ;
#58260=ORIENTED_EDGE ( 'NONE', *, *, #12303, .T. ) ;
#58263=MECHANICAL_DESIGN_GEOMETRIC_PRESENTATION_REPRESENTATION('',(#10809),#57141);
#58267=CIRCLE ( 'NONE', #47964, 24.99999999998784972 ) ;
#58274=ADVANCED_FACE ( 'NONE', ( #30778 ), #41020, .F. ) ;
#58302=FILL_AREA_STYLE_COLOUR ( '', #18407 ) ;
#58304=FACE_OUTER_BOUND ( 'NONE', #42320, .T. ) ;
#58306=ADVANCED_FACE ( 'NONE', ( #30070 ), #18762, .T. ) ;
#58307=LINE ( 'NONE', #9511, #21623 ) ;
#58308=CIRCLE ( 'NONE', #66216, 24.99999999998789946 ) ;
#58315=EDGE_CURVE ( 'NONE', #59376, #23171, #52000, .T. ) ;
#58321=LINE ( 'NONE', #5274, #20335 ) ;
#58327=EDGE_CURVE ( 'NONE', #32793, #16596, #62453, .T. ) ;
#58336=( NAMED_UNIT ( * ) SI_UNIT ( $, .STERADIAN. ) SOLID_ANGLE_UNIT ( ) );
#58338=LINE ( 'NONE', #69281, #8342 ) ;
#58349=FACE_OUTER_BOUND ( 'NONE', #11630, .T. ) ;
#58351=ADVANCED_FACE ( 'NONE', ( #26430 ), #47997, .T. ) ;
#58354=CARTESIAN_POINT ( 'NONE',  ( 39.00000000000000000, 21.00000000000000000, -16.96999999999999886 ) ) ;
#58358=ORIENTED_EDGE ( 'NONE', *, *, #32749, .F. ) ;
#58378=VECTOR ( 'NONE', #35051, 1000.000000000000000 ) ;
#58389=LINE ( 'NONE', #729, #11332 ) ;
#58397=ORIENTED_EDGE ( 'NONE', *, *, #36727, .F. ) ;
#58405=VECTOR ( 'NONE', #32489, 1000.000000000000000 ) ;
#58411=VERTEX_POINT ( 'NONE', #59298 ) ;
#58421=EDGE_LOOP ( 'NONE', ( #12849, #56698, #63898, #66664 ) ) ;
#58425=FACE_OUTER_BOUND ( 'NONE', #18508, .T. ) ;
#58433=ORIENTED_EDGE ( 'NONE', *, *, #27442, .F. ) ;
#58435=LINE ( 'NONE', #58066, #38164 ) ;
#58442=DIRECTION ( 'NONE',  ( 1.000000000000000000, 0.000000000000000000, 0.000000000000000000 ) ) ;
#58445=CYLINDRICAL_SURFACE ( 'NONE', #8908, 24.99999999998789946 ) ;
#58470=AXIS2_PLACEMENT_3D ( 'NONE', #54929, #6483, #28043 ) ;
#58472=ORIENTED_EDGE ( 'NONE', *, *, #21580, .F. ) ;
#58476=ORIENTED_EDGE ( 'NONE', *, *, #11433, .T. ) ;
#58477=ORIENTED_EDGE ( 'NONE', *, *, #7984, .T. ) ;
#58479=ADVANCED_FACE ( 'NONE', ( #64608 ), #11201, .F. ) ;
#58495=DIRECTION ( 'NONE',  ( 0.000000000000000000, 0.000000000000000000, -1.000000000000000000 ) ) ;
#58509=EDGE_CURVE ( 'NONE', #9679, #22670, #55710, .T. ) ;
#58516=EDGE_CURVE ( 'NONE', #61299, #55382, #53467, .T. ) ;
#58522=PLANE ( 'NONE',  #21540 ) ;
#58523=CARTESIAN_POINT ( 'NONE',  ( 0.000000000000000000, 0.7500000000000000000, 0.000000000000000000 ) ) ;
#58531=DIRECTION ( 'NONE',  ( 0.000000000000000000, -1.000000000000000000, 0.000000000000000000 ) ) ;
#58534=ORIENTED_EDGE ( 'NONE', *, *, #61148, .F. ) ;
#58536=CARTESIAN_POINT ( 'NONE',  ( 40.90000000000000568, -0.2000000000000000111, 0.000000000000000000 ) ) ;
#58537=ORIENTED_EDGE ( 'NONE', *, *, #37142, .F. ) ;
#58546=ORIENTED_EDGE ( 'NONE', *, *, #69730, .T. ) ;
#58553=UNCERTAINTY_MEASURE_WITH_UNIT (LENGTH_MEASURE( 1.000000000000000082E-05 ), #39233, 'distance_accuracy_value', 'NONE');
#58559=DIRECTION ( 'NONE',  ( -1.000000000000000000, 0.000000000000000000, 0.000000000000000000 ) ) ;
#58570=CARTESIAN_POINT ( 'NONE',  ( 23.90000000000000213, -0.1999999999911795112, 8.826273045769999343E-12 ) ) ;
#58571=DIRECTION ( 'NONE',  ( 1.000000000000000000, -0.000000000000000000, 0.000000000000000000 ) ) ;
#58572=CARTESIAN_POINT ( 'NONE',  ( 49.00000000000000000, -0.1999999999911430404, -8.864436962241481021E-12 ) ) ;
#58593=EDGE_CURVE ( 'NONE', #57888, #68679, #23895, .T. ) ;
#58594=AXIS2_PLACEMENT_3D ( 'NONE', #43300, #64882, #21043 ) ;
#58596=DIRECTION ( 'NONE',  ( 1.000000000000000000, -0.000000000000000000, -0.000000000000000000 ) ) ;
#58598=ORIENTED_EDGE ( 'NONE', *, *, #8572, .T. ) ;
#58607=ORIENTED_EDGE ( 'NONE', *, *, #22420, .F. ) ;
#58609=EDGE_CURVE ( 'NONE', #13118, #22414, #64758, .T. ) ;
#58617=DIRECTION ( 'NONE',  ( 0.000000000000000000, 0.000000000000000000, 1.000000000000000000 ) ) ;
#58630=EDGE_CURVE ( 'NONE', #10620, #42134, #43303, .T. ) ;
#58632=CARTESIAN_POINT ( 'NONE',  ( 41.09999999999999432, 20.60000000000000142, 13.86939075806900057 ) ) ;
#58634=VERTEX_POINT ( 'NONE', #61359 ) ;
#58638=EDGE_CURVE ( 'NONE', #22897, #54988, #67392, .T. ) ;
#58676=DIRECTION ( 'NONE',  ( 0.000000000000000000, 1.000000000000000000, 0.000000000000000000 ) ) ;
#58684=ORIENTED_EDGE ( 'NONE', *, *, #47980, .T. ) ;
#58686=CIRCLE ( 'NONE', #13482, 2.458500000000000796 ) ;
#58698=ORIENTED_EDGE ( 'NONE', *, *, #47215, .F. ) ;
#58700=ORIENTED_EDGE ( 'NONE', *, *, #47372, .F. ) ;
#58710=ORIENTED_EDGE ( 'NONE', *, *, #12007, .T. ) ;
#58716=VECTOR ( 'NONE', #51970, 1000.000000000000000 ) ;
#58736=CYLINDRICAL_SURFACE ( 'NONE', #46461, 3.500000000000000000 ) ;
#58754=FACE_OUTER_BOUND ( 'NONE', #6559, .T. ) ;
#58757=DIRECTION ( 'NONE',  ( 0.000000000000000000, 0.000000000000000000, -1.000000000000000000 ) ) ;
#58758=DIRECTION ( 'NONE',  ( 0.000000000000000000, 0.000000000000000000, -1.000000000000000000 ) ) ;
#58760=CIRCLE ( 'NONE', #22613, 25.39999999999999858 ) ;
#58776=EDGE_CURVE ( 'NONE', #24121, #37027, #31328, .T. ) ;
#58781=ORIENTED_EDGE ( 'NONE', *, *, #29796, .F. ) ;
#58799=ADVANCED_FACE ( 'NONE', ( #43987 ), #38353, .T. ) ;
#58803=CARTESIAN_POINT ( 'NONE',  ( 41.09999999999999432, -21.00000000000000000, -13.86939075806900057 ) ) ;
#58806=ORIENTED_EDGE ( 'NONE', *, *, #56117, .F. ) ;
#58826=VERTEX_POINT ( 'NONE', #11463 ) ;
#58832=CARTESIAN_POINT ( 'NONE',  ( 15.89999999999999680, 20.60000000000000142, 13.86939075806899702 ) ) ;
#58837=( NAMED_UNIT ( * ) PLANE_ANGLE_UNIT ( ) SI_UNIT ( $, .RADIAN. ) );
#58838=VECTOR ( 'NONE', #5583, 1000.000000000000000 ) ;
#58843=CARTESIAN_POINT ( 'NONE',  ( -6.661338147750939243E-15, -17.79289321881346808, -20.50000000000000000 ) ) ;
#58845=FILL_AREA_STYLE_COLOUR ( '', #10760 ) ;
#58855=DIRECTION ( 'NONE',  ( -1.000000000000000000, 0.000000000000000000, 0.000000000000000000 ) ) ;
#58861=DIRECTION ( 'NONE',  ( 0.000000000000000000, -0.7071067811865474617, 0.7071067811865474617 ) ) ;
#58864=FILL_AREA_STYLE ('',( #15377 ) ) ;
#58869=LINE ( 'NONE', #31651, #21557 ) ;
#58873=DIRECTION ( 'NONE',  ( 0.000000000000000000, 0.000000000000000000, -1.000000000000000000 ) ) ;
#58885=CARTESIAN_POINT ( 'NONE',  ( 25.57999999999999829, 0.000000000000000000, 0.000000000000000000 ) ) ;
#58886=CIRCLE ( 'NONE', #45321, 24.99999999998784972 ) ;
#58895=CIRCLE ( 'NONE', #10338, 0.5000000000000000000 ) ;
#58898=CARTESIAN_POINT ( 'NONE',  ( 26.90000000000000213, -0.1999999999911795112, 8.826273045769999343E-12 ) ) ;
#58913=EDGE_LOOP ( 'NONE', ( #64254, #50902, #32622, #7824, #48385, #24052, #52828, #36612 ) ) ;
#58932=CARTESIAN_POINT ( 'NONE',  ( 46.39999999999999858, 21.00000000000000000, -2.250000000000000444 ) ) ;
#58934=FACE_OUTER_BOUND ( 'NONE', #63675, .T. ) ;
#58949=VECTOR ( 'NONE', #25735, 1000.000000000000000 ) ;
#58955=VERTEX_POINT ( 'NONE', #12496 ) ;
#58958=LINE ( 'NONE', #5226, #11282 ) ;
#58965=LINE ( 'NONE', #20088, #42397 ) ;
#58986=AXIS2_PLACEMENT_3D ( 'NONE', #60719, #17233, #45140 ) ;
#58988=DIRECTION ( 'NONE',  ( 0.000000000000000000, 0.7071067811865474617, -0.7071067811865474617 ) ) ;
#59006=FILL_AREA_STYLE_COLOUR ( '', #35807 ) ;
#59036=ADVANCED_FACE ( 'NONE', ( #1904 ), #51034, .F. ) ;
#59049=DIRECTION ( 'NONE',  ( 1.000000000000000000, -0.000000000000000000, 0.000000000000000000 ) ) ;
#59050=ORIENTED_EDGE ( 'NONE', *, *, #23572, .T. ) ;
#59058=VECTOR ( 'NONE', #4837, 1000.000000000000000 ) ;
#59071=DIRECTION ( 'NONE',  ( -1.000000000000000000, 0.000000000000000000, 0.000000000000000000 ) ) ;
#59094=AXIS2_PLACEMENT_3D ( 'NONE', #55820, #50517, #66767 ) ;
#59101=DIRECTION ( 'NONE',  ( 0.000000000000000000, -1.000000000000000000, 0.000000000000000000 ) ) ;
#59103=LINE ( 'NONE', #15974, #7673 ) ;
#59104=AXIS2_PLACEMENT_3D ( 'NONE', #15630, #69010, #58757 ) ;
#59111=AXIS2_PLACEMENT_3D ( 'NONE', #13436, #8468, #19094 ) ;
#59115=VECTOR ( 'NONE', #4009, 1000.000000000000000 ) ;
#59117=VECTOR ( 'NONE', #2018, 1000.000000000000000 ) ;
#59143=VERTEX_POINT ( 'NONE', #36165 ) ;
#59153=ORIENTED_EDGE ( 'NONE', *, *, #13703, .F. ) ;
#59163=CARTESIAN_POINT ( 'NONE',  ( 39.00000000000000000, 21.00000000000000000, 13.98999642601811999 ) ) ;
#59170=VECTOR ( 'NONE', #48035, 1000.000000000000000 ) ;
#59189=SURFACE_STYLE_FILL_AREA ( #4412 ) ;
#59191=ORIENTED_EDGE ( 'NONE', *, *, #46218, .F. ) ;
#59194=DIRECTION ( 'NONE',  ( -1.000000000000000000, 0.000000000000000000, 0.000000000000000000 ) ) ;
#59197=DIRECTION ( 'NONE',  ( 1.000000000000000000, 0.000000000000000000, 0.000000000000000000 ) ) ;
#59203=CARTESIAN_POINT ( 'NONE',  ( 39.00000000000000000, -16.96999999999999886, -21.00000000000000000 ) ) ;
#59209=EDGE_CURVE ( 'NONE', #4613, #69832, #27319, .T. ) ;
#59210=AXIS2_PLACEMENT_3D ( 'NONE', #55780, #60733, #50477 ) ;
#59229=DIRECTION ( 'NONE',  ( -1.000000000000000000, 0.000000000000000000, 0.000000000000000000 ) ) ;
#59232=ORIENTED_EDGE ( 'NONE', *, *, #35517, .T. ) ;
#59238=ADVANCED_FACE ( 'NONE', ( #48188 ), #69395, .F. ) ;
#59251=DIRECTION ( 'NONE',  ( 0.6785983445458472207, -0.6785983445458458885, -0.2810846377148227826 ) ) ;
#59271=STYLED_ITEM ( 'NONE', ( #69167 ), #43380 ) ;
#59281=ADVANCED_FACE ( 'NONE', ( #26616 ), #15664, .T. ) ;
#59282=ORIENTED_EDGE ( 'NONE', *, *, #40561, .F. ) ;
#59298=CARTESIAN_POINT ( 'NONE',  ( 31.89999999999999858, -21.00000000000001421, -13.86939075806900945 ) ) ;
#59304=ORIENTED_EDGE ( 'NONE', *, *, #42882, .T. ) ;
#59306=DIRECTION ( 'NONE',  ( 1.000000000000000000, -0.000000000000000000, 0.000000000000000000 ) ) ;
#59309=VECTOR ( 'NONE', #16529, 1000.000000000000000 ) ;
#59314=CARTESIAN_POINT ( 'NONE',  ( 24.90000000000000213, 13.66939075806899240, 20.79999999999999361 ) ) ;
#59315=CYLINDRICAL_SURFACE ( 'NONE', #23933, 2.458500000000000796 ) ;
#59321=ORIENTED_EDGE ( 'NONE', *, *, #15144, .F. ) ;
#59326=EDGE_CURVE ( 'NONE', #6900, #50683, #43568, .T. ) ;
#59328=ORIENTED_EDGE ( 'NONE', *, *, #14227, .F. ) ;
#59330=DIRECTION ( 'NONE',  ( 0.000000000000000000, 0.000000000000000000, -1.000000000000000000 ) ) ;
#59334=EDGE_CURVE ( 'NONE', #64531, #30734, #29035, .T. ) ;
#59335=SURFACE_STYLE_FILL_AREA ( #67943 ) ;
#59337=DIRECTION ( 'NONE',  ( 0.000000000000000000, 0.000000000000000000, -1.000000000000000000 ) ) ;
#59347=DIRECTION ( 'NONE',  ( -1.000000000000000000, 0.000000000000000000, 0.000000000000000000 ) ) ;
#59358=AXIS2_PLACEMENT_3D ( 'NONE', #6329, #49469, #6664 ) ;
#59359=CIRCLE ( 'NONE', #68397, 24.99999999998784972 ) ;
#59363=CARTESIAN_POINT ( 'NONE',  ( 41.09999999999999432, -21.00000000000000000, -14.57806571531351914 ) ) ;
#59364=ORIENTED_EDGE ( 'NONE', *, *, #5072, .T. ) ;
#59368=LINE ( 'NONE', #38162, #502 ) ;
#59369=LINE ( 'NONE', #10930, #38411 ) ;
#59376=VERTEX_POINT ( 'NONE', #23386 ) ;
#59381=EDGE_CURVE ( 'NONE', #7253, #49868, #55906, .T. ) ;
#59388=ORIENTED_EDGE ( 'NONE', *, *, #18664, .F. ) ;
#59389=LINE ( 'NONE', #10952, #38355 ) ;
#59391=PLANE ( 'NONE',  #522 ) ;
#59403=CIRCLE ( 'NONE', #4090, 24.99999999998784972 ) ;
#59413=AXIS2_PLACEMENT_3D ( 'NONE', #40240, #45897, #45538 ) ;
#59417=EDGE_LOOP ( 'NONE', ( #58103, #46119, #26342, #20495 ) ) ;
#59430=DIRECTION ( 'NONE',  ( -0.000000000000000000, -1.000000000000000000, 0.000000000000000000 ) ) ;
#59457=AXIS2_PLACEMENT_3D ( 'NONE', #42834, #65112, #31547 ) ;
#59461=ORIENTED_EDGE ( 'NONE', *, *, #58638, .T. ) ;
#59468=VECTOR ( 'NONE', #46269, 1000.000000000000000 ) ;
#59470=DIRECTION ( 'NONE',  ( -1.000000000000000000, 0.000000000000000000, 0.000000000000000000 ) ) ;
#59486=EDGE_LOOP ( 'NONE', ( #46660, #43751, #1747, #44499 ) ) ;
#59492=FACE_OUTER_BOUND ( 'NONE', #25688, .T. ) ;
#59502=ORIENTED_EDGE ( 'NONE', *, *, #14618, .F. ) ;
#59506=CARTESIAN_POINT ( 'NONE',  ( 26.90000000000000213, -14.06939075806902117, -20.80000000000000426 ) ) ;
#59512=LINE ( 'NONE', #11073, #68642 ) ;
#59514=DIRECTION ( 'NONE',  ( -1.000000000000000000, 0.000000000000000000, 0.000000000000000000 ) ) ;
#59524=EDGE_CURVE ( 'NONE', #38554, #34859, #57306, .T. ) ;
#59525=DIRECTION ( 'NONE',  ( 1.000000000000000000, -0.000000000000000000, -0.000000000000000000 ) ) ;
#59531=ORIENTED_EDGE ( 'NONE', *, *, #64048, .F. ) ;
#59534=CARTESIAN_POINT ( 'NONE',  ( 49.00000000000000000, -21.00000000000000000, 13.86939075806900057 ) ) ;
#59561=AXIS2_PLACEMENT_3D ( 'NONE', #19232, #13225, #34422 ) ;
#59577=ORIENTED_EDGE ( 'NONE', *, *, #62045, .F. ) ;
#59580=EDGE_CURVE ( 'NONE', #26524, #33050, #24786, .T. ) ;
#59604=EDGE_CURVE ( 'NONE', #67686, #25494, #32185, .T. ) ;
#59617=DIRECTION ( 'NONE',  ( 1.000000000000000000, -0.000000000000000000, 0.000000000000000000 ) ) ;
#59630=CARTESIAN_POINT ( 'NONE',  ( 26.90000000000000213, 20.60000000000000142, -13.86939075806900057 ) ) ;
#59640=CARTESIAN_POINT ( 'NONE',  ( 32.89999999999999858, 0.000000000000000000, 2.458500000000000796 ) ) ;
#59648=ORIENTED_EDGE ( 'NONE', *, *, #26527, .T. ) ;
#59658=VERTEX_POINT ( 'NONE', #31849 ) ;
#59659=CARTESIAN_POINT ( 'NONE',  ( 35.89999999999999858, 13.66939075806899240, 20.79999999999999361 ) ) ;
#59670=DIRECTION ( 'NONE',  ( 1.000000000000000000, -0.000000000000000000, 0.000000000000000000 ) ) ;
#59672=EDGE_CURVE ( 'NONE', #14096, #65971, #32547, .T. ) ;
#59675=ORIENTED_EDGE ( 'NONE', *, *, #49354, .F. ) ;
#59701=( NAMED_UNIT ( * ) PLANE_ANGLE_UNIT ( ) SI_UNIT ( $, .RADIAN. ) );
#59712=CARTESIAN_POINT ( 'NONE',  ( 46.39999999999999858, 33.00000000000000000, 2.250000000000000444 ) ) ;
#59713=FACE_OUTER_BOUND ( 'NONE', #31414, .T. ) ;
#59714=VECTOR ( 'NONE', #29421, 1000.000000000000000 ) ;
#59720=ORIENTED_EDGE ( 'NONE', *, *, #55745, .T. ) ;
#59724=CARTESIAN_POINT ( 'NONE',  ( 37.90000000000000568, -14.06939075806900874, 20.80000000000001137 ) ) ;
#59727=DIRECTION ( 'NONE',  ( -1.000000000000000000, 0.000000000000000000, 0.000000000000000000 ) ) ;
#59728=CARTESIAN_POINT ( 'NONE',  ( 48.50000000000000000, 0.000000000000000000, 0.000000000000000000 ) ) ;
#59740=ORIENTED_EDGE ( 'NONE', *, *, #55289, .T. ) ;
#59745=VERTEX_POINT ( 'NONE', #38534 ) ;
#59755=VECTOR ( 'NONE', #67605, 1000.000000000000000 ) ;
#59763=VERTEX_POINT ( 'NONE', #55143 ) ;
#59779=EDGE_CURVE ( 'NONE', #11292, #18694, #54794, .T. ) ;
#59788=ORIENTED_EDGE ( 'NONE', *, *, #64757, .T. ) ;
#59790=DIRECTION ( 'NONE',  ( 0.000000000000000000, 0.000000000000000000, -1.000000000000000000 ) ) ;
#59793=CARTESIAN_POINT ( 'NONE',  ( 34.89999999999999858, 0.000000000000000000, 0.000000000000000000 ) ) ;
#59795=PLANE ( 'NONE',  #714 ) ;
#59819=CIRCLE ( 'NONE', #63191, 24.99999999998784972 ) ;
#59824=PRESENTATION_STYLE_ASSIGNMENT (( #11712 ) ) ;
#59847=EDGE_LOOP ( 'NONE', ( #53978, #35990, #53468, #33292 ) ) ;
#59861=ADVANCED_FACE ( 'NONE', ( #40602 ), #3485, .F. ) ;
#59863=PLANE ( 'NONE',  #19182 ) ;
#59866=DIRECTION ( 'NONE',  ( 0.000000000000000000, 0.000000000000000000, 1.000000000000000000 ) ) ;
#59872=CIRCLE ( 'NONE', #40630, 24.99999999998784972 ) ;
#59875=ORIENTED_EDGE ( 'NONE', *, *, #34474, .T. ) ;
#59892=CARTESIAN_POINT ( 'NONE',  ( 7.900000000000000355, -14.48845687959340012, -21.00000000000000000 ) ) ;
#59911=ADVANCED_FACE ( 'NONE', ( #20095 ), #68541, .T. ) ;
#59917=ORIENTED_EDGE ( 'NONE', *, *, #46306, .T. ) ;
#59940=LINE ( 'NONE', #55343, #22142 ) ;
#59946=CARTESIAN_POINT ( 'NONE',  ( 55.00000000000000000, -21.00000000000000000, -16.96999999999999886 ) ) ;
#59949=ADVANCED_FACE ( 'NONE', ( #61831 ), #3140, .T. ) ;
#59951=CARTESIAN_POINT ( 'NONE',  ( 33.89999999999999858, -0.1999999999911430404, -8.864436962241481021E-12 ) ) ;
#59996=CIRCLE ( 'NONE', #16009, 24.99999999998789946 ) ;
#59999=ORIENTED_EDGE ( 'NONE', *, *, #20241, .F. ) ;
#60003=CARTESIAN_POINT ( 'NONE',  ( 17.89999999999999858, 20.60000000000000142, -13.86939075806900057 ) ) ;
#60005=ORIENTED_EDGE ( 'NONE', *, *, #40574, .T. ) ;
#60027=CYLINDRICAL_SURFACE ( 'NONE', #37583, 24.99999999998784972 ) ;
#60035=CIRCLE ( 'NONE', #19351, 2.458500000000000796 ) ;
#60041=CARTESIAN_POINT ( 'NONE',  ( 49.00000000000000000, -0.1999999999911430404, -8.864436962241481021E-12 ) ) ;
#60042=ORIENTED_EDGE ( 'NONE', *, *, #32438, .T. ) ;
#60045=EDGE_CURVE ( 'NONE', #30328, #44316, #5579, .T. ) ;
#60054=CARTESIAN_POINT ( 'NONE',  ( 10.00000000000000000, -18.00000000000000355, -21.00000000000000000 ) ) ;
#60068=DIRECTION ( 'NONE',  ( -1.000000000000000000, 0.000000000000000000, 0.000000000000000000 ) ) ;
#60075=FACE_OUTER_BOUND ( 'NONE', #61116, .T. ) ;
#60080=VERTEX_POINT ( 'NONE', #42704 ) ;
#60083=ORIENTED_EDGE ( 'NONE', *, *, #40615, .F. ) ;
#60085=VERTEX_POINT ( 'NONE', #59314 ) ;
#60096=ORIENTED_EDGE ( 'NONE', *, *, #53349, .T. ) ;
#60100=VERTEX_POINT ( 'NONE', #38117 ) ;
#60107=VERTEX_POINT ( 'NONE', #21831 ) ;
#60108=EDGE_CURVE ( 'NONE', #11005, #69324, #11217, .T. ) ;
#60130=ORIENTED_EDGE ( 'NONE', *, *, #26537, .F. ) ;
#60151=VERTEX_POINT ( 'NONE', #621 ) ;
#60152=EDGE_CURVE ( 'NONE', #27398, #10620, #49055, .T. ) ;
#60171=DIRECTION ( 'NONE',  ( 0.000000000000000000, -1.000000000000000000, 0.000000000000000000 ) ) ;
#60175=ORIENTED_EDGE ( 'NONE', *, *, #32950, .F. ) ;
#60191=DIRECTION ( 'NONE',  ( 0.000000000000000000, 0.000000000000000000, -1.000000000000000000 ) ) ;
#60197=DIRECTION ( 'NONE',  ( 0.000000000000000000, 0.000000000000000000, -1.000000000000000000 ) ) ;
#60198=EDGE_CURVE ( 'NONE', #13897, #57808, #62342, .T. ) ;
#60220=DIRECTION ( 'NONE',  ( 0.000000000000000000, 0.000000000000000000, -1.000000000000000000 ) ) ;
#60223=CARTESIAN_POINT ( 'NONE',  ( 39.90000000000000568, 16.96999999999999886, 21.00000000000000000 ) ) ;
#60241=LINE ( 'NONE', #33382, #23151 ) ;
#60257=MECHANICAL_DESIGN_GEOMETRIC_PRESENTATION_REPRESENTATION('',(#18450),#27510);
#60266=VERTEX_POINT ( 'NONE', #30183 ) ;
#60281=ADVANCED_FACE ( 'NONE', ( #52101 ), #35832, .F. ) ;
#60285=CARTESIAN_POINT ( 'NONE',  ( 49.00000000000000000, -0.1999999999911430404, -8.864436962241481021E-12 ) ) ;
#60286=PLANE ( 'NONE',  #16682 ) ;
#60295=ORIENTED_EDGE ( 'NONE', *, *, #33719, .F. ) ;
#60299=FACE_OUTER_BOUND ( 'NONE', #20533, .T. ) ;
#60304=DIRECTION ( 'NONE',  ( 0.000000000000000000, 0.000000000000000000, -1.000000000000000000 ) ) ;
#60312=ORIENTED_EDGE ( 'NONE', *, *, #56616, .T. ) ;
#60313=CARTESIAN_POINT ( 'NONE',  ( 47.00000000000000000, -0.7500000000000000000, -4.943429983321300014 ) ) ;
#60340=CARTESIAN_POINT ( 'NONE',  ( 49.00000000000000000, -0.1999999999911795112, 8.826273045769999343E-12 ) ) ;
#60348=DIRECTION ( 'NONE',  ( 1.000000000000000000, 0.000000000000000000, 0.000000000000000000 ) ) ;
#60356=LINE ( 'NONE', #27856, #59117 ) ;
#60375=CARTESIAN_POINT ( 'NONE',  ( 49.00000000000000000, -21.00000000000000000, 13.86939075806900057 ) ) ;
#60377=VERTEX_POINT ( 'NONE', #19918 ) ;
#60389=VECTOR ( 'NONE', #395, 1000.000000000000114 ) ;
#60403=VERTEX_POINT ( 'NONE', #38290 ) ;
#60414=MECHANICAL_DESIGN_GEOMETRIC_PRESENTATION_REPRESENTATION('',(#59271),#57041);
#60417=CARTESIAN_POINT ( 'NONE',  ( 25.90000000000000213, 0.000000000000000000, 0.000000000000000000 ) ) ;
#60442=EDGE_CURVE ( 'NONE', #8699, #18454, #68442, .T. ) ;
#60449=( NAMED_UNIT ( * ) PLANE_ANGLE_UNIT ( ) SI_UNIT ( $, .RADIAN. ) );
#60453=EDGE_CURVE ( 'NONE', #36902, #58100, #22373, .T. ) ;
#60455=STYLED_ITEM ( 'NONE', ( #56680 ), #67577 ) ;
#60459=CARTESIAN_POINT ( 'NONE',  ( 15.90000000000000036, 0.000000000000000000, 8.619743980008982554E-16 ) ) ;
#60475=CARTESIAN_POINT ( 'NONE',  ( 46.39999999999999858, 33.00000000000000000, 0.7500000000000000000 ) ) ;
#60486=VERTEX_POINT ( 'NONE', #37246 ) ;
#60488=DIRECTION ( 'NONE',  ( 0.000000000000000000, 0.000000000000000000, -1.000000000000000000 ) ) ;
#60495=DIRECTION ( 'NONE',  ( 0.000000000000000000, 0.000000000000000000, -1.000000000000000000 ) ) ;
#60499=AXIS2_PLACEMENT_3D ( 'NONE', #37946, #15683, #43237 ) ;
#60500=VECTOR ( 'NONE', #41785, 1000.000000000000000 ) ;
#60513=CARTESIAN_POINT ( 'NONE',  ( 27.00000000000000000, 0.000000000000000000, -2.458500000000000796 ) ) ;
#60519=CARTESIAN_POINT ( 'NONE',  ( 41.09999999999999432, 20.60000000000000142, -13.86939075806900057 ) ) ;
#60520=COLOUR_RGB ( '', 0.72549020, 0.75294118, 0.79215686) ;
#60521=DIRECTION ( 'NONE',  ( 1.000000000000000000, -0.000000000000000000, 0.000000000000000000 ) ) ;
#60526=CARTESIAN_POINT ( 'NONE',  ( 36.90000000000000568, 0.000000000000000000, 3.016910393003143647E-15 ) ) ;
#60531=CARTESIAN_POINT ( 'NONE',  ( 41.09999999999999432, -21.00000000000000000, 13.86939075806900057 ) ) ;
#60533=ORIENTED_EDGE ( 'NONE', *, *, #10802, .F. ) ;
#60544=DIRECTION ( 'NONE',  ( -1.000000000000000000, 0.000000000000000000, 0.000000000000000000 ) ) ;
#60545=FACE_OUTER_BOUND ( 'NONE', #24107, .T. ) ;
#60548=ORIENTED_EDGE ( 'NONE', *, *, #65195, .F. ) ;
#60550=EDGE_CURVE ( 'NONE', #17050, #1369, #24082, .T. ) ;
#60552=AXIS2_PLACEMENT_3D ( 'NONE', #52472, #25608, #47171 ) ;
#60560=AXIS2_PLACEMENT_3D ( 'NONE', #23539, #18577, #23191 ) ;
#60568=VECTOR ( 'NONE', #10033, 1000.000000000000000 ) ;
#60586=DIRECTION ( 'NONE',  ( 0.000000000000000000, 0.000000000000000000, -1.000000000000000000 ) ) ;
#60588=ORIENTED_EDGE ( 'NONE', *, *, #5698, .T. ) ;
#60595=VERTEX_POINT ( 'NONE', #50263 ) ;
#60607=AXIS2_PLACEMENT_3D ( 'NONE', #26461, #16544, #53686 ) ;
#60608=EDGE_CURVE ( 'NONE', #60107, #4446, #34327, .T. ) ;
#60615=ORIENTED_EDGE ( 'NONE', *, *, #37981, .T. ) ;
#60630=DIRECTION ( 'NONE',  ( 0.000000000000000000, 0.000000000000000000, -1.000000000000000000 ) ) ;
#60632=CARTESIAN_POINT ( 'NONE',  ( 40.90000000000000568, -16.96999999999999886, -21.00000000000000000 ) ) ;
#60638=ADVANCED_FACE ( 'NONE', ( #8165 ), #50615, .F. ) ;
#60642=LINE ( 'NONE', #50377, #47214 ) ;
#60648=FACE_OUTER_BOUND ( 'NONE', #54802, .T. ) ;
#60653=AXIS2_PLACEMENT_3D ( 'NONE', #4120, #69153, #20711 ) ;
#60688=ORIENTED_EDGE ( 'NONE', *, *, #55040, .T. ) ;
#60697=CARTESIAN_POINT ( 'NONE',  ( 49.00000000000000000, -21.00000000000000000, 13.86939075806900057 ) ) ;
#60700=ORIENTED_EDGE ( 'NONE', *, *, #66491, .F. ) ;
#60714=LINE ( 'NONE', #22550, #43315 ) ;
#60718=LINE ( 'NONE', #21853, #29446 ) ;
#60719=CARTESIAN_POINT ( 'NONE',  ( 49.00000000000000000, 0.000000000000000000, 0.000000000000000000 ) ) ;
#60721=PLANE ( 'NONE',  #41899 ) ;
#60733=DIRECTION ( 'NONE',  ( 0.000000000000000000, -0.7071067811865475727, 0.7071067811865475727 ) ) ;
#60744=LINE ( 'NONE', #1359, #11539 ) ;
#60750=CIRCLE ( 'NONE', #36914, 2.458500000000000796 ) ;
#60758=EDGE_CURVE ( 'NONE', #57901, #4860, #14222, .T. ) ;
#60772=ADVANCED_FACE ( 'NONE', ( #67582 ), #14888, .F. ) ;
#60776=ADVANCED_FACE ( 'NONE', ( #57313 ), #68274, .F. ) ;
#60787=DIRECTION ( 'NONE',  ( -1.000000000000000000, 0.000000000000000000, 0.000000000000000000 ) ) ;
#60788=CARTESIAN_POINT ( 'NONE',  ( 8.900000000000005684, 20.60000000000000142, 13.86939075806899702 ) ) ;
#60794=FILL_AREA_STYLE_COLOUR ( '', #41975 ) ;
#60807=SURFACE_STYLE_FILL_AREA ( #39247 ) ;
#60819=DIRECTION ( 'NONE',  ( 0.000000000000000000, -0.7071067811865474617, -0.7071067811865474617 ) ) ;
#60850=ORIENTED_EDGE ( 'NONE', *, *, #21381, .T. ) ;
#60854=EDGE_CURVE ( 'NONE', #18237, #46721, #15932, .T. ) ;
#60858=VECTOR ( 'NONE', #50446, 1000.000000000000000 ) ;
#60874=ORIENTED_EDGE ( 'NONE', *, *, #26377, .T. ) ;
#60890=CARTESIAN_POINT ( 'NONE',  ( 0.000000000000000000, 0.000000000000000000, 0.000000000000000000 ) ) ;
#60891=DIRECTION ( 'NONE',  ( 0.000000000000000000, -1.000000000000000000, 0.000000000000000000 ) ) ;
#60895=DIRECTION ( 'NONE',  ( -1.000000000000000000, 0.000000000000000000, 0.000000000000000000 ) ) ;
#60899=VECTOR ( 'NONE', #26380, 1000.000000000000000 ) ;
#60906=CARTESIAN_POINT ( 'NONE',  ( 39.00000000000000000, -14.48845687959340012, -21.00000000000000000 ) ) ;
#60934=LINE ( 'NONE', #27737, #51326 ) ;
#60935=EDGE_CURVE ( 'NONE', #6091, #36263, #10977, .T. ) ;
#60937=AXIS2_PLACEMENT_3D ( 'NONE', #26335, #58531, #58873 ) ;
#60940=EDGE_CURVE ( 'NONE', #9679, #57901, #27245, .T. ) ;
#60951=DIRECTION ( 'NONE',  ( 0.000000000000000000, 0.7071067811865474617, 0.7071067811865474617 ) ) ;
#60953=ORIENTED_EDGE ( 'NONE', *, *, #21582, .T. ) ;
#60958=ORIENTED_EDGE ( 'NONE', *, *, #38661, .F. ) ;
#60960=VECTOR ( 'NONE', #18954, 1000.000000000000000 ) ;
#60965=DIRECTION ( 'NONE',  ( 1.000000000000000000, -0.000000000000000000, 0.000000000000000000 ) ) ;
#60975=EDGE_CURVE ( 'NONE', #16609, #23148, #63955, .T. ) ;
#60981=CIRCLE ( 'NONE', #6827, 24.99999999998784972 ) ;
#60988=CARTESIAN_POINT ( 'NONE',  ( 39.00000000000000000, 0.000000000000000000, 0.000000000000000000 ) ) ;
#60992=EDGE_LOOP ( 'NONE', ( #60958, #67396 ) ) ;
#60994=DIRECTION ( 'NONE',  ( 0.000000000000000000, 0.000000000000000000, 1.000000000000000000 ) ) ;
#61003=DIRECTION ( 'NONE',  ( -1.000000000000000000, 0.000000000000000000, 0.000000000000000000 ) ) ;
#61017=VECTOR ( 'NONE', #23640, 1000.000000000000000 ) ;
#61018=EDGE_LOOP ( 'NONE', ( #48201, #67734, #58433, #69863, #27954, #36873, #15411, #36479 ) ) ;
#61020=EDGE_CURVE ( 'NONE', #40017, #31832, #40264, .T. ) ;
#61045=( NAMED_UNIT ( * ) PLANE_ANGLE_UNIT ( ) SI_UNIT ( $, .RADIAN. ) );
#61075=DIRECTION ( 'NONE',  ( 0.000000000000000000, 0.000000000000000000, 1.000000000000000000 ) ) ;
#61085=AXIS2_PLACEMENT_3D ( 'NONE', #56666, #19530, #52065 ) ;
#61092=ORIENTED_EDGE ( 'NONE', *, *, #68283, .F. ) ;
#61094=VERTEX_POINT ( 'NONE', #33573 ) ;
#61109=ORIENTED_EDGE ( 'NONE', *, *, #148, .T. ) ;
#61115=CARTESIAN_POINT ( 'NONE',  ( 10.00000000000000000, -18.00000000000000355, -21.00000000000000000 ) ) ;
#61116=EDGE_LOOP ( 'NONE', ( #30368, #43015, #9895, #37590, #19265, #10631, #33985, #27507 ) ) ;
#61117=ORIENTED_EDGE ( 'NONE', *, *, #35645, .T. ) ;
#61118=CARTESIAN_POINT ( 'NONE',  ( 35.89999999999999858, 13.66939075806899240, -20.79999999999999361 ) ) ;
#61136=CLOSED_SHELL ( 'NONE', ( #42737, #7370, #37949, #20634, #108, #44475, #277, #53759, #52643, #15279, #36466, #14830, #33381, #55789 ) ) ;
#61148=EDGE_CURVE ( 'NONE', #27390, #54230, #25775, .T. ) ;
#61154=CYLINDRICAL_SURFACE ( 'NONE', #44432, 24.99999999998789946 ) ;
#61159=FILL_AREA_STYLE ('',( #13434 ) ) ;
#61163=EDGE_CURVE ( 'NONE', #51833, #63119, #62174, .T. ) ;
#61190=CIRCLE ( 'NONE', #17147, 24.99999999998785327 ) ;
#61191=EDGE_CURVE ( 'NONE', #12812, #51717, #19049, .T. ) ;
#61195=CIRCLE ( 'NONE', #33011, 24.99999999998789946 ) ;
#61201=DIRECTION ( 'NONE',  ( 0.000000000000000000, 0.000000000000000000, -1.000000000000000000 ) ) ;
#61205=LINE ( 'NONE', #60531, #45201 ) ;
#61216=AXIS2_PLACEMENT_3D ( 'NONE', #24580, #40830, #28812 ) ;
#61221=CYLINDRICAL_SURFACE ( 'NONE', #8934, 24.99999999998794920 ) ;
#61223=ORIENTED_EDGE ( 'NONE', *, *, #51903, .T. ) ;
#61229=ADVANCED_FACE ( 'NONE', ( #14091 ), #35646, .T. ) ;
#61231=CARTESIAN_POINT ( 'NONE',  ( 49.00000000000000000, -0.2000000000089119934, 8.909539772616881237E-12 ) ) ;
#61236=ORIENTED_EDGE ( 'NONE', *, *, #63433, .T. ) ;
#61250=PLANE ( 'NONE',  #61535 ) ;
#61252=EDGE_CURVE ( 'NONE', #32206, #14663, #42366, .T. ) ;
#61254=VECTOR ( 'NONE', #20125, 1000.000000000000000 ) ;
#61259=ORIENTED_EDGE ( 'NONE', *, *, #29497, .T. ) ;
#61261=DIRECTION ( 'NONE',  ( 0.000000000000000000, 0.000000000000000000, 1.000000000000000000 ) ) ;
#61265=SURFACE_STYLE_FILL_AREA ( #19198 ) ;
#61269=EDGE_LOOP ( 'NONE', ( #32395, #54427 ) ) ;
#61287=ADVANCED_FACE ( 'NONE', ( #10537 ), #54039, .F. ) ;
#61298=AXIS2_PLACEMENT_3D ( 'NONE', #52141, #10065, #8996 ) ;
#61299=VERTEX_POINT ( 'NONE', #52995 ) ;
#61305=DIRECTION ( 'NONE',  ( -1.000000000000000000, 0.000000000000000000, 0.000000000000000000 ) ) ;
#61307=COLOUR_RGB ( '', 0.31764706, 0.68627451, 0.89019608) ;
#61329=EDGE_LOOP ( 'NONE', ( #43420, #6278, #66506, #44310 ) ) ;
#61333=FACE_OUTER_BOUND ( 'NONE', #62859, .T. ) ;
#61351=AXIS2_PLACEMENT_3D ( 'NONE', #22366, #60521, #11389 ) ;
#61353=DIRECTION ( 'NONE',  ( 0.000000000000000000, 0.000000000000000000, 1.000000000000000000 ) ) ;
#61356=CIRCLE ( 'NONE', #28612, 24.99999999998794920 ) ;
#61359=CARTESIAN_POINT ( 'NONE',  ( 41.09999999999999432, -14.48845687959340012, 21.00000000000000000 ) ) ;
#61363=ORIENTED_EDGE ( 'NONE', *, *, #5698, .F. ) ;
#61386=PLANE ( 'NONE',  #13023 ) ;
#61388=DIRECTION ( 'NONE',  ( 0.000000000000000000, -0.7071067811865474617, -0.7071067811865474617 ) ) ;
#61393=DIRECTION ( 'NONE',  ( 0.000000000000000000, 0.000000000000000000, -1.000000000000000000 ) ) ;
#61403=DIRECTION ( 'NONE',  ( 0.000000000000000000, 0.000000000000000000, -1.000000000000000000 ) ) ;
#61406=DIRECTION ( 'NONE',  ( 1.000000000000000000, -0.000000000000000000, 0.000000000000000000 ) ) ;
#61430=VERTEX_POINT ( 'NONE', #21927 ) ;
#61440=CARTESIAN_POINT ( 'NONE',  ( 38.90000000000000568, 13.66939075806899240, -20.79999999999999361 ) ) ;
#61447=( GEOMETRIC_REPRESENTATION_CONTEXT ( 3 ) GLOBAL_UNCERTAINTY_ASSIGNED_CONTEXT ( ( #52909 ) ) GLOBAL_UNIT_ASSIGNED_CONTEXT ( ( #33960, #62229, #12730 ) ) REPRESENTATION_CONTEXT ( 'NONE', 'WORKASPACE' ) );
#61450=CARTESIAN_POINT ( 'NONE',  ( 15.90000000000000036, -0.000000000000000000, -20.80000000000000426 ) ) ;
#61463=DIRECTION ( 'NONE',  ( 1.000000000000000000, 0.000000000000000000, 0.000000000000000000 ) ) ;
#61472=FACE_BOUND ( 'NONE', #24302, .T. ) ;
#61478=DIRECTION ( 'NONE',  ( -1.000000000000000000, 0.000000000000000000, 0.000000000000000000 ) ) ;
#61482=AXIS2_PLACEMENT_3D ( 'NONE', #10490, #54333, #47976 ) ;
#61499=VECTOR ( 'NONE', #64007, 1000.000000000000114 ) ;
#61504=VERTEX_POINT ( 'NONE', #61118 ) ;
#61506=CARTESIAN_POINT ( 'NONE',  ( 11.90000000000000036, 20.60000000000000142, -13.86939075806900057 ) ) ;
#61511=VECTOR ( 'NONE', #66305, 1000.000000000000000 ) ;
#61514=EDGE_LOOP ( 'NONE', ( #28852, #2629, #43745, #59531 ) ) ;
#61515=ORIENTED_EDGE ( 'NONE', *, *, #60758, .F. ) ;
#61516=VECTOR ( 'NONE', #8351, 1000.000000000000000 ) ;
#61522=EDGE_LOOP ( 'NONE', ( #36662, #47383, #35932, #28410, #57028 ) ) ;
#61529=DIRECTION ( 'NONE',  ( 0.000000000000000000, 0.000000000000000000, -1.000000000000000000 ) ) ;
#61531=CARTESIAN_POINT ( 'NONE',  ( 9.899999999999998579, -21.00000000000000000, 13.86939075806900057 ) ) ;
#61535=AXIS2_PLACEMENT_3D ( 'NONE', #24141, #34374, #45343 ) ;
#61541=VECTOR ( 'NONE', #16103, 1000.000000000000000 ) ;
#61543=VECTOR ( 'NONE', #11895, 1000.000000000000000 ) ;
#61554=ORIENTED_EDGE ( 'NONE', *, *, #31104, .T. ) ;
#61564=VECTOR ( 'NONE', #30116, 1000.000000000000000 ) ;
#61581=PLANE ( 'NONE',  #27281 ) ;
#61597=ORIENTED_EDGE ( 'NONE', *, *, #26010, .T. ) ;
#61606=AXIS2_PLACEMENT_3D ( 'NONE', #4541, #20445, #47664 ) ;
#61615=PRODUCT_DEFINITION_SHAPE ( 'NONE', 'NONE',  #18876 ) ;
#61618=CARTESIAN_POINT ( 'NONE',  ( 9.899999999999998579, 20.60000000000000142, 13.86939075806899702 ) ) ;
#61628=LINE ( 'NONE', #24162, #17507 ) ;
#61664=AXIS2_PLACEMENT_3D ( 'NONE', #50599, #12400, #65817 ) ;
#61667=CARTESIAN_POINT ( 'NONE',  ( 19.90000000000000213, -21.00000000000000000, 13.86939075806900057 ) ) ;
#61670=ORIENTED_EDGE ( 'NONE', *, *, #57219, .F. ) ;
#61676=DIRECTION ( 'NONE',  ( 0.000000000000000000, 0.000000000000000000, 1.000000000000000000 ) ) ;
#61683=LINE ( 'NONE', #41440, #60500 ) ;
#61693=CARTESIAN_POINT ( 'NONE',  ( 49.00000000000000000, -21.00000000000000000, 13.86939075806900057 ) ) ;
#61702=VERTEX_POINT ( 'NONE', #47245 ) ;
#61706=CARTESIAN_POINT ( 'NONE',  ( 49.00000000000000000, -21.00000000000000000, 13.86939075806900057 ) ) ;
#61717=ADVANCED_FACE ( 'NONE', ( #62172 ), #9408, .T. ) ;
#61720=VERTEX_POINT ( 'NONE', #40611 ) ;
#61721=FACE_OUTER_BOUND ( 'NONE', #29723, .T. ) ;
#61724=CARTESIAN_POINT ( 'NONE',  ( 36.90000000000000568, -21.00000000000001421, -13.86939075806900945 ) ) ;
#61735=ORIENTED_EDGE ( 'NONE', *, *, #11187, .T. ) ;
#61739=VERTEX_POINT ( 'NONE', #15763 ) ;
#61740=EDGE_CURVE ( 'NONE', #34997, #41893, #42626, .T. ) ;
#61757=CARTESIAN_POINT ( 'NONE',  ( 39.00000000000000000, 0.000000000000000000, 0.000000000000000000 ) ) ;
#61770=EDGE_LOOP ( 'NONE', ( #23500, #37310, #11440, #15691 ) ) ;
#61772=DIRECTION ( 'NONE',  ( 0.000000000000000000, -0.2142857142857142738, -0.9767710236555245951 ) ) ;
#61775=CARTESIAN_POINT ( 'NONE',  ( 32.89999999999999858, -21.00000000000000000, 13.86939075806900057 ) ) ;
#61792=VERTEX_POINT ( 'NONE', #33060 ) ;
#61798=ORIENTED_EDGE ( 'NONE', *, *, #28333, .T. ) ;
#61805=AXIS2_PLACEMENT_3D ( 'NONE', #10474, #32048, #53622 ) ;
#61809=ORIENTED_EDGE ( 'NONE', *, *, #27654, .F. ) ;
#61823=AXIS2_PLACEMENT_3D ( 'NONE', #62862, #14432, #57552 ) ;
#61831=FACE_OUTER_BOUND ( 'NONE', #65513, .T. ) ;
#61836=CARTESIAN_POINT ( 'NONE',  ( 41.09999999999999432, 13.66939075806899950, 20.80000000000000426 ) ) ;
#61858=ORIENTED_EDGE ( 'NONE', *, *, #58156, .T. ) ;
#61868=ADVANCED_FACE ( 'NONE', ( #28436 ), #27760, .T. ) ;
#61874=EDGE_CURVE ( 'NONE', #51947, #26978, #1567, .T. ) ;
#61875=FACE_OUTER_BOUND ( 'NONE', #48893, .T. ) ;
#61889=PLANE ( 'NONE',  #69385 ) ;
#61890=ORIENTED_EDGE ( 'NONE', *, *, #27784, .T. ) ;
#61905=ORIENTED_EDGE ( 'NONE', *, *, #20366, .F. ) ;
#61917=VERTEX_POINT ( 'NONE', #51765 ) ;
#61922=AXIS2_PLACEMENT_3D ( 'NONE', #67260, #60895, #13159 ) ;
#61925=FILL_AREA_STYLE ('',( #2524 ) ) ;
#61928=LINE ( 'NONE', #56629, #16994 ) ;
#61933=CARTESIAN_POINT ( 'NONE',  ( 24.90000000000000213, -0.1999999999911430404, -8.864436962241481021E-12 ) ) ;
#61936=DIRECTION ( 'NONE',  ( 0.000000000000000000, 0.000000000000000000, -1.000000000000000000 ) ) ;
#61940=CARTESIAN_POINT ( 'NONE',  ( 30.90000000000000213, -21.00000000000000000, 13.86939075806900057 ) ) ;
#61949=DIRECTION ( 'NONE',  ( 0.000000000000000000, 0.000000000000000000, 1.000000000000000000 ) ) ;
#61960=AXIS2_PLACEMENT_3D ( 'NONE', #13750, #19401, #50540 ) ;
#61967=PLANE ( 'NONE',  #61085 ) ;
#61968=EDGE_LOOP ( 'NONE', ( #66269, #31325, #21829, #63868 ) ) ;
#61971=ORIENTED_EDGE ( 'NONE', *, *, #45707, .T. ) ;
#61976=CARTESIAN_POINT ( 'NONE',  ( 49.00000000000000000, 13.66939075806899950, 20.80000000000000426 ) ) ;
#61990=ADVANCED_FACE ( 'NONE', ( #39735 ), #62356, .F. ) ;
#62008=CARTESIAN_POINT ( 'NONE',  ( 33.89999999999999858, 13.66939075806899240, -20.79999999999999361 ) ) ;
#62010=ORIENTED_EDGE ( 'NONE', *, *, #371, .T. ) ;
#62015=DIRECTION ( 'NONE',  ( 0.000000000000000000, 0.000000000000000000, -1.000000000000000000 ) ) ;
#62037=CARTESIAN_POINT ( 'NONE',  ( 41.09999999999999432, -21.00000000000000000, -13.86939075806900057 ) ) ;
#62038=ORIENTED_EDGE ( 'NONE', *, *, #60045, .T. ) ;
#62045=EDGE_CURVE ( 'NONE', #61430, #58411, #63776, .T. ) ;
#62046=CARTESIAN_POINT ( 'NONE',  ( 32.89999999999999858, -14.06939075806900163, -20.80000000000000426 ) ) ;
#62054=CARTESIAN_POINT ( 'NONE',  ( 46.39999999999999858, 33.00000000000000000, -2.250000000000000444 ) ) ;
#62062=DIRECTION ( 'NONE',  ( 0.000000000000000000, 0.000000000000000000, -1.000000000000000000 ) ) ;
#62071=LINE ( 'NONE', #40859, #60960 ) ;
#62085=FACE_OUTER_BOUND ( 'NONE', #7338, .T. ) ;
#62090=DIRECTION ( 'NONE',  ( 1.000000000000000000, 0.000000000000000000, 0.000000000000000000 ) ) ;
#62092=EDGE_CURVE ( 'NONE', #32705, #4531, #57323, .T. ) ;
#62104=ORIENTED_EDGE ( 'NONE', *, *, #58327, .F. ) ;
#62107=VECTOR ( 'NONE', #57401, 1000.000000000000000 ) ;
#62108=FILL_AREA_STYLE_COLOUR ( '', #42361 ) ;
#62112=DIRECTION ( 'NONE',  ( 0.000000000000000000, 0.000000000000000000, 1.000000000000000000 ) ) ;
#62122=CARTESIAN_POINT ( 'NONE',  ( 49.00000000000000000, -0.1999999999911795112, 8.826273045769999343E-12 ) ) ;
#62130=ORIENTED_EDGE ( 'NONE', *, *, #22821, .T. ) ;
#62142=LINE ( 'NONE', #3465, #41888 ) ;
#62143=CIRCLE ( 'NONE', #41823, 24.99999999998794920 ) ;
#62150=CARTESIAN_POINT ( 'NONE',  ( 36.90000000000000568, 20.60000000000000142, -13.86939075806900057 ) ) ;
#62157=CARTESIAN_POINT ( 'NONE',  ( 8.900000000000005684, -0.2000000000000000111, 0.000000000000000000 ) ) ;
#62158=ORIENTED_EDGE ( 'NONE', *, *, #18195, .T. ) ;
#62159=ORIENTED_EDGE ( 'NONE', *, *, #682, .T. ) ;
#62163=CARTESIAN_POINT ( 'NONE',  ( 25.57999999999999829, 0.000000000000000000, 0.000000000000000000 ) ) ;
#62167=DIRECTION ( 'NONE',  ( -1.000000000000000000, 0.000000000000000000, 0.000000000000000000 ) ) ;
#62171=VECTOR ( 'NONE', #69707, 1000.000000000000000 ) ;
#62172=FACE_OUTER_BOUND ( 'NONE', #33943, .T. ) ;
#62174=LINE ( 'NONE', #30715, #68490 ) ;
#62177=CARTESIAN_POINT ( 'NONE',  ( 39.90000000000000568, 0.000000000000000000, 3.447897592003593022E-15 ) ) ;
#62180=ORIENTED_EDGE ( 'NONE', *, *, #61163, .F. ) ;
#62183=CARTESIAN_POINT ( 'NONE',  ( 48.50000000000000000, -0.7500000000000000000, 3.418698582794335028 ) ) ;
#62184=ADVANCED_FACE ( 'NONE', ( #26287 ), #20974, .F. ) ;
#62185=( LENGTH_UNIT ( ) NAMED_UNIT ( * ) SI_UNIT ( .MILLI., .METRE. ) );
#62200=CARTESIAN_POINT ( 'NONE',  ( 11.90000000000000036, -0.000000000000000000, 20.80000000000000426 ) ) ;
#62205=ORIENTED_EDGE ( 'NONE', *, *, #55227, .T. ) ;
#62207=AXIS2_PLACEMENT_3D ( 'NONE', #49505, #1074, #44182 ) ;
#62211=VERTEX_POINT ( 'NONE', #26990 ) ;
#62229=( NAMED_UNIT ( * ) PLANE_ANGLE_UNIT ( ) SI_UNIT ( $, .RADIAN. ) );
#62236=CARTESIAN_POINT ( 'NONE',  ( 46.39999999999999858, 21.00000000000000000, -2.750000000000000444 ) ) ;
#62245=ORIENTED_EDGE ( 'NONE', *, *, #30348, .F. ) ;
#62259=EDGE_CURVE ( 'NONE', #41212, #55616, #33328, .T. ) ;
#62265=EDGE_CURVE ( 'NONE', #59745, #27714, #59512, .T. ) ;
#62266=DIRECTION ( 'NONE',  ( 1.000000000000000000, -0.000000000000000000, 0.000000000000000000 ) ) ;
#62277=DIRECTION ( 'NONE',  ( 0.000000000000000000, 0.000000000000000000, 1.000000000000000000 ) ) ;
#62278=LINE ( 'NONE', #67946, #58378 ) ;
#62284=CARTESIAN_POINT ( 'NONE',  ( 31.89999999999999858, -0.1999999999911795112, 8.826273045769999343E-12 ) ) ;
#62287=LINE ( 'NONE', #46725, #43442 ) ;
#62288=DIRECTION ( 'NONE',  ( -1.000000000000000000, 0.000000000000000000, 0.000000000000000000 ) ) ;
#62291=DIRECTION ( 'NONE',  ( -1.000000000000000000, 0.000000000000000000, 0.000000000000000000 ) ) ;
#62304=VERTEX_POINT ( 'NONE', #43587 ) ;
#62309=DIRECTION ( 'NONE',  ( -1.000000000000000000, 0.000000000000000000, 0.000000000000000000 ) ) ;
#62313=CARTESIAN_POINT ( 'NONE',  ( 8.900000000000005684, -21.00000000000000000, 13.86939075806900057 ) ) ;
#62315=ORIENTED_EDGE ( 'NONE', *, *, #69404, .F. ) ;
#62317=EDGE_LOOP ( 'NONE', ( #724, #28601, #53375, #31403 ) ) ;
#62319=EDGE_LOOP ( 'NONE', ( #40815, #49953, #7201, #52508 ) ) ;
#62328=ORIENTED_EDGE ( 'NONE', *, *, #9457, .T. ) ;
#62329=ORIENTED_EDGE ( 'NONE', *, *, #56411, .F. ) ;
#62330=ORIENTED_EDGE ( 'NONE', *, *, #10802, .T. ) ;
#62340=ORIENTED_EDGE ( 'NONE', *, *, #5996, .T. ) ;
#62342=LINE ( 'NONE', #22189, #10793 ) ;
#62347=CARTESIAN_POINT ( 'NONE',  ( 30.90000000000000213, 0.000000000000000000, 0.000000000000000000 ) ) ;
#62356=PLANE ( 'NONE',  #59561 ) ;
#62369=CARTESIAN_POINT ( 'NONE',  ( 46.39999999999999858, 21.00000000000000000, 1.750000000000000222 ) ) ;
#62375=VERTEX_POINT ( 'NONE', #66191 ) ;
#62379=PLANE ( 'NONE',  #7852 ) ;
#62384=DIRECTION ( 'NONE',  ( -1.000000000000000000, 0.000000000000000000, 0.000000000000000000 ) ) ;
#62389=VECTOR ( 'NONE', #18922, 1000.000000000000000 ) ;
#62393=DIRECTION ( 'NONE',  ( -0.000000000000000000, -1.000000000000000000, 0.000000000000000000 ) ) ;
#62410=VECTOR ( 'NONE', #8229, 1000.000000000000000 ) ;
#62414=AXIS2_PLACEMENT_3D ( 'NONE', #13606, #35158, #8288 ) ;
#62424=ORIENTED_EDGE ( 'NONE', *, *, #38205, .F. ) ;
#62433=DIRECTION ( 'NONE',  ( -1.000000000000000000, 0.000000000000000000, 0.000000000000000000 ) ) ;
#62434=DIRECTION ( 'NONE',  ( 0.000000000000000000, 0.000000000000000000, 1.000000000000000000 ) ) ;
#62436=DIRECTION ( 'NONE',  ( -0.7071067811865475727, -0.7071067811865475727, 0.000000000000000000 ) ) ;
#62440=( NAMED_UNIT ( * ) PLANE_ANGLE_UNIT ( ) SI_UNIT ( $, .RADIAN. ) );
#62444=DIRECTION ( 'NONE',  ( 0.000000000000000000, -1.000000000000000000, 0.000000000000000000 ) ) ;
#62453=CIRCLE ( 'NONE', #68129, 24.99999999998794920 ) ;
#62484=ORIENTED_EDGE ( 'NONE', *, *, #8156, .F. ) ;
#62485=VERTEX_POINT ( 'NONE', #56273 ) ;
#62486=CARTESIAN_POINT ( 'NONE',  ( 35.89999999999999858, 0.000000000000000000, 2.458500000000000796 ) ) ;
#62498=DIRECTION ( 'NONE',  ( 1.000000000000000000, -0.000000000000000000, 0.000000000000000000 ) ) ;
#62508=AXIS2_PLACEMENT_3D ( 'NONE', #67537, #14125, #28637 ) ;
#62518=EDGE_CURVE ( 'NONE', #15490, #13113, #30804, .T. ) ;
#62532=( NAMED_UNIT ( * ) PLANE_ANGLE_UNIT ( ) SI_UNIT ( $, .RADIAN. ) );
#62543=FACE_OUTER_BOUND ( 'NONE', #25223, .T. ) ;
#62544=LINE ( 'NONE', #30031, #48127 ) ;
#62547=LINE ( 'NONE', #31100, #47129 ) ;
#62558=CARTESIAN_POINT ( 'NONE',  ( 9.899999999999998579, -21.00000000000000355, -14.57806571531352269 ) ) ;
#62578=ORIENTED_EDGE ( 'NONE', *, *, #67848, .T. ) ;
#62583=CARTESIAN_POINT ( 'NONE',  ( 49.00000000000000000, -0.2000000000089119934, -8.913009219568841313E-12 ) ) ;
#62594=ADVANCED_FACE ( 'NONE', ( #36822 ), #62618, .T. ) ;
#62595=ORIENTED_EDGE ( 'NONE', *, *, #64381, .F. ) ;
#62610=ORIENTED_EDGE ( 'NONE', *, *, #37344, .T. ) ;
#62615=EDGE_CURVE ( 'NONE', #12122, #6097, #48122, .T. ) ;
#62618=CYLINDRICAL_SURFACE ( 'NONE', #31256, 24.99999999998789946 ) ;
#62630=FACE_OUTER_BOUND ( 'NONE', #64349, .T. ) ;
#62637=DIRECTION ( 'NONE',  ( 1.000000000000000000, -0.000000000000000000, 0.000000000000000000 ) ) ;
#62651=EDGE_LOOP ( 'NONE', ( #65872, #62010, #35151, #771 ) ) ;
#62656=CARTESIAN_POINT ( 'NONE',  ( 10.90000000000000036, -14.06939075806902117, -20.80000000000000426 ) ) ;
#62670=VECTOR ( 'NONE', #66076, 1000.000000000000000 ) ;
#62691=ORIENTED_EDGE ( 'NONE', *, *, #43450, .T. ) ;
#62706=EDGE_CURVE ( 'NONE', #11032, #19106, #64009, .T. ) ;
#62728=CIRCLE ( 'NONE', #27764, 24.99999999998784972 ) ;
#62739=CARTESIAN_POINT ( 'NONE',  ( 8.900000000000005684, -14.06939075806901940, -20.80000000000000426 ) ) ;
#62750=EDGE_CURVE ( 'NONE', #47619, #12122, #4137, .T. ) ;
#62756=VERTEX_POINT ( 'NONE', #34613 ) ;
#62762=CARTESIAN_POINT ( 'NONE',  ( 8.900000000000002132, 18.00000000000000355, -21.00000000000000000 ) ) ;
#62773=DIRECTION ( 'NONE',  ( 1.000000000000000000, -0.000000000000000000, 0.000000000000000000 ) ) ;
#62777=AXIS2_PLACEMENT_3D ( 'NONE', #68634, #41045, #46701 ) ;
#62778=ORIENTED_EDGE ( 'NONE', *, *, #60550, .F. ) ;
#62779=VERTEX_POINT ( 'NONE', #66451 ) ;
#62787=ORIENTED_EDGE ( 'NONE', *, *, #16000, .F. ) ;
#62790=UNCERTAINTY_MEASURE_WITH_UNIT (LENGTH_MEASURE( 1.000000000000000082E-05 ), #54529, 'distance_accuracy_value', 'NONE');
#62794=PRODUCT ( 'Stepper Motor', 'Stepper Motor', '', ( #56857 ) ) ;
#62804=LINE ( 'NONE', #35568, #12047 ) ;
#62807=FACE_OUTER_BOUND ( 'NONE', #22159, .T. ) ;
#62811=DIRECTION ( 'NONE',  ( 1.000000000000000000, 0.000000000000000000, 0.000000000000000000 ) ) ;
#62813=DIRECTION ( 'NONE',  ( 0.000000000000000000, -0.7071067811865474617, -0.7071067811865474617 ) ) ;
#62814=AXIS2_PLACEMENT_3D ( 'NONE', #2233, #40416, #51023 ) ;
#62822=SURFACE_STYLE_FILL_AREA ( #20390 ) ;
#62824=VECTOR ( 'NONE', #56280, 1000.000000000000000 ) ;
#62825=AXIS2_PLACEMENT_3D ( 'NONE', #38245, #43525, #27617 ) ;
#62836=VERTEX_POINT ( 'NONE', #40274 ) ;
#62838=PLANE ( 'NONE',  #52593 ) ;
#62848=EDGE_CURVE ( 'NONE', #4531, #60100, #28967, .T. ) ;
#62857=ORIENTED_EDGE ( 'NONE', *, *, #9457, .F. ) ;
#62859=EDGE_LOOP ( 'NONE', ( #62158, #6526, #47163, #39469 ) ) ;
#62862=CARTESIAN_POINT ( 'NONE',  ( 39.00000000000000000, 0.000000000000000000, 0.000000000000000000 ) ) ;
#62865=VERTEX_POINT ( 'NONE', #18341 ) ;
#62866=CARTESIAN_POINT ( 'NONE',  ( 18.89999999999999858, -0.2000000000089119934, -8.913009219568841313E-12 ) ) ;
#62868=PLANE ( 'NONE',  #3996 ) ;
#62872=CIRCLE ( 'NONE', #68536, 24.99999999998784972 ) ;
#62884=ORIENTED_EDGE ( 'NONE', *, *, #7886, .F. ) ;
#62901=DIRECTION ( 'NONE',  ( -1.000000000000000000, 0.000000000000000000, 0.000000000000000000 ) ) ;
#62914=DIRECTION ( 'NONE',  ( -1.000000000000000000, 0.000000000000000000, 0.000000000000000000 ) ) ;
#62940=VERTEX_POINT ( 'NONE', #67849 ) ;
#62941=PLANE ( 'NONE',  #31404 ) ;
#62947=DIRECTION ( 'NONE',  ( 0.000000000000000000, 0.000000000000000000, -1.000000000000000000 ) ) ;
#62948=VERTEX_POINT ( 'NONE', #25416 ) ;
#62955=VECTOR ( 'NONE', #42729, 1000.000000000000000 ) ;
#62957=DIRECTION ( 'NONE',  ( 0.000000000000000000, 0.000000000000000000, -1.000000000000000000 ) ) ;
#62973=DIRECTION ( 'NONE',  ( -1.000000000000000000, 0.000000000000000000, 0.000000000000000000 ) ) ;
#62993=CARTESIAN_POINT ( 'NONE',  ( 17.89999999999999858, -0.2000000000089119934, -8.913009219568841313E-12 ) ) ;
#63001=DIRECTION ( 'NONE',  ( 0.000000000000000000, 0.000000000000000000, 1.000000000000000000 ) ) ;
#63004=DIRECTION ( 'NONE',  ( 0.000000000000000000, 0.000000000000000000, -1.000000000000000000 ) ) ;
#63006=EDGE_CURVE ( 'NONE', #16172, #33489, #30013, .T. ) ;
#63011=EDGE_CURVE ( 'NONE', #58411, #16445, #15166, .T. ) ;
#63020=AXIS2_PLACEMENT_3D ( 'NONE', #43527, #16318, #27288 ) ;
#63023=DIRECTION ( 'NONE',  ( -1.000000000000000000, 0.000000000000000000, 0.000000000000000000 ) ) ;
#63025=CARTESIAN_POINT ( 'NONE',  ( 27.90000000000000213, -0.1999999999911795112, 8.826273045769999343E-12 ) ) ;
#63030=FACE_BOUND ( 'NONE', #16347, .T. ) ;
#63072=ORIENTED_EDGE ( 'NONE', *, *, #27017, .F. ) ;
#63076=DIRECTION ( 'NONE',  ( 0.000000000000000000, 1.000000000000000000, 0.000000000000000000 ) ) ;
#63083=( NAMED_UNIT ( * ) SI_UNIT ( $, .STERADIAN. ) SOLID_ANGLE_UNIT ( ) );
#63088=CARTESIAN_POINT ( 'NONE',  ( 39.00000000000000000, 0.000000000000000000, 5.250000000000000000 ) ) ;
#63100=CARTESIAN_POINT ( 'NONE',  ( 49.00000000000000000, -21.00000000000000000, 13.86939075806900057 ) ) ;
#63108=FACE_OUTER_BOUND ( 'NONE', #42920, .T. ) ;
#63109=SURFACE_SIDE_STYLE ('',( #42589 ) ) ;
#63119=VERTEX_POINT ( 'NONE', #48726 ) ;
#63120=SURFACE_STYLE_USAGE ( .BOTH. , #7697 ) ;
#63133=VECTOR ( 'NONE', #38983, 1000.000000000000000 ) ;
#63138=VECTOR ( 'NONE', #63519, 1000.000000000000000 ) ;
#63148=ORIENTED_EDGE ( 'NONE', *, *, #40615, .T. ) ;
#63156=DIRECTION ( 'NONE',  ( 1.000000000000000000, -0.000000000000000000, 0.000000000000000000 ) ) ;
#63158=( NAMED_UNIT ( * ) PLANE_ANGLE_UNIT ( ) SI_UNIT ( $, .RADIAN. ) );
#63159=LINE ( 'NONE', #30984, #29046 ) ;
#63163=FACE_OUTER_BOUND ( 'NONE', #45866, .T. ) ;
#63191=AXIS2_PLACEMENT_3D ( 'NONE', #48319, #44037, #43343 ) ;
#63195=CARTESIAN_POINT ( 'NONE',  ( 20.90000000000000213, -21.00000000000000000, 13.86939075806900057 ) ) ;
#63200=CARTESIAN_POINT ( 'NONE',  ( 41.09999999999999432, -14.48845687959340012, 21.00000000000000000 ) ) ;
#63204=ORIENTED_EDGE ( 'NONE', *, *, #7886, .T. ) ;
#63207=ORIENTED_EDGE ( 'NONE', *, *, #51634, .T. ) ;
#63211=VECTOR ( 'NONE', #64895, 1000.000000000000000 ) ;
#63215=CARTESIAN_POINT ( 'NONE',  ( 49.00000000000000000, -14.06939075806900163, -20.80000000000000426 ) ) ;
#63223=AXIS2_PLACEMENT_3D ( 'NONE', #67378, #67713, #51456 ) ;
#63225=LINE ( 'NONE', #42705, #40997 ) ;
#63230=CARTESIAN_POINT ( 'NONE',  ( 23.90000000000000213, -0.000000000000000000, -20.80000000000000426 ) ) ;
#63238=EDGE_LOOP ( 'NONE', ( #16686, #67062, #34064, #23553, #61515, #22248, #35343, #44708 ) ) ;
#63242=ADVANCED_FACE ( 'NONE', ( #6959 ), #17226, .T. ) ;
#63246=VERTEX_POINT ( 'NONE', #39825 ) ;
#63258=LINE ( 'NONE', #57597, #16088 ) ;
#63259=CARTESIAN_POINT ( 'NONE',  ( 46.39999999999999858, 33.00000000000000000, -2.250000000000000444 ) ) ;
#63260=DIRECTION ( 'NONE',  ( 1.000000000000000000, -0.000000000000000000, 0.000000000000000000 ) ) ;
#63265=FILL_AREA_STYLE ('',( #9521 ) ) ;
#63269=AXIS2_PLACEMENT_3D ( 'NONE', #19558, #15320, #4015 ) ;
#63273=CARTESIAN_POINT ( 'NONE',  ( 14.89999999999999680, 20.60000000000000142, 13.86939075806900057 ) ) ;
#63276=FILL_AREA_STYLE_COLOUR ( '', #60520 ) ;
#63292=EDGE_CURVE ( 'NONE', #3551, #10117, #55085, .T. ) ;
#63293=EDGE_CURVE ( 'NONE', #29691, #22003, #8760, .T. ) ;
#63298=EDGE_LOOP ( 'NONE', ( #35595, #36982, #38613, #49455, #34782, #40839, #47087, #54789 ) ) ;
#63302=VERTEX_POINT ( 'NONE', #28194 ) ;
#63304=DIRECTION ( 'NONE',  ( 0.000000000000000000, 0.7071067811865475727, 0.7071067811865475727 ) ) ;
#63305=DIRECTION ( 'NONE',  ( 0.000000000000000000, 0.000000000000000000, 1.000000000000000000 ) ) ;
#63309=VECTOR ( 'NONE', #59229, 1000.000000000000000 ) ;
#63318=CIRCLE ( 'NONE', #37380, 24.99999999998789946 ) ;
#63322=DIRECTION ( 'NONE',  ( 0.000000000000000000, 0.000000000000000000, -1.000000000000000000 ) ) ;
#63331=ADVANCED_FACE ( 'NONE', ( #62807 ), #14008, .T. ) ;
#63341=EDGE_CURVE ( 'NONE', #30940, #47029, #27949, .T. ) ;
#63360=DIRECTION ( 'NONE',  ( 1.000000000000000000, -0.000000000000000000, 0.000000000000000000 ) ) ;
#63363=DIRECTION ( 'NONE',  ( 0.000000000000000000, 0.000000000000000000, -1.000000000000000000 ) ) ;
#63374=FACE_OUTER_BOUND ( 'NONE', #67122, .T. ) ;
#63383=CARTESIAN_POINT ( 'NONE',  ( 27.90000000000000213, 0.000000000000000000, 2.154935995002245293E-15 ) ) ;
#63396=ORIENTED_EDGE ( 'NONE', *, *, #8257, .F. ) ;
#63400=ORIENTED_EDGE ( 'NONE', *, *, #11148, .F. ) ;
#63402=DIRECTION ( 'NONE',  ( 0.000000000000000000, 0.000000000000000000, 1.000000000000000000 ) ) ;
#63406=ORIENTED_EDGE ( 'NONE', *, *, #66956, .T. ) ;
#63420=ORIENTED_EDGE ( 'NONE', *, *, #21613, .T. ) ;
#63433=EDGE_CURVE ( 'NONE', #16007, #40969, #46534, .T. ) ;
#63437=EDGE_CURVE ( 'NONE', #53130, #32607, #63159, .T. ) ;
#63439=CIRCLE ( 'NONE', #50998, 5.000000000000000000 ) ;
#63447=PRESENTATION_STYLE_ASSIGNMENT (( #58134 ) ) ;
#63470=VECTOR ( 'NONE', #8964, 1000.000000000000000 ) ;
#63488=ADVANCED_FACE ( 'NONE', ( #21420 ), #32041, .T. ) ;
#63490=VECTOR ( 'NONE', #37926, 1000.000000000000114 ) ;
#63493=CARTESIAN_POINT ( 'NONE',  ( 32.89999999999999858, -14.06939075806902117, -20.80000000000000426 ) ) ;
#63494=ORIENTED_EDGE ( 'NONE', *, *, #61740, .T. ) ;
#63497=VECTOR ( 'NONE', #47902, 1000.000000000000000 ) ;
#63498=EDGE_CURVE ( 'NONE', #12180, #7082, #16821, .T. ) ;
#63499=EDGE_CURVE ( 'NONE', #37491, #59376, #43748, .T. ) ;
#63500=ORIENTED_EDGE ( 'NONE', *, *, #5781, .F. ) ;
#63507=EDGE_CURVE ( 'NONE', #44316, #46512, #31699, .T. ) ;
#63519=DIRECTION ( 'NONE',  ( 0.000000000000000000, 0.000000000000000000, 1.000000000000000000 ) ) ;
#63520=VERTEX_POINT ( 'NONE', #47947 ) ;
#63533=ORIENTED_EDGE ( 'NONE', *, *, #37344, .F. ) ;
#63538=ORIENTED_EDGE ( 'NONE', *, *, #10214, .T. ) ;
#63541=VECTOR ( 'NONE', #35363, 1000.000000000000000 ) ;
#63548=CARTESIAN_POINT ( 'NONE',  ( 8.900000000000002132, 21.00000000000000000, 18.00000000000000355 ) ) ;
#63550=CARTESIAN_POINT ( 'NONE',  ( 47.00000000000000000, 0.000000000000000000, 0.000000000000000000 ) ) ;
#63556=DIRECTION ( 'NONE',  ( 0.000000000000000000, 0.000000000000000000, 1.000000000000000000 ) ) ;
#63569=ORIENTED_EDGE ( 'NONE', *, *, #22526, .F. ) ;
#63586=ORIENTED_EDGE ( 'NONE', *, *, #6335, .F. ) ;
#63592=PLANE ( 'NONE',  #40744 ) ;
#63595=CIRCLE ( 'NONE', #29696, 2.458500000000000796 ) ;
#63603=ADVANCED_FACE ( 'NONE', ( #7491 ), #61221, .T. ) ;
#63605=( NAMED_UNIT ( * ) SI_UNIT ( $, .STERADIAN. ) SOLID_ANGLE_UNIT ( ) );
#63607=DIRECTION ( 'NONE',  ( 0.000000000000000000, -1.000000000000000000, 0.000000000000000000 ) ) ;
#63617=CARTESIAN_POINT ( 'NONE',  ( 11.90000000000000036, -0.2000000000089119934, -8.913009219568841313E-12 ) ) ;
#63624=( LENGTH_UNIT ( ) NAMED_UNIT ( * ) SI_UNIT ( .MILLI., .METRE. ) );
#63628=DIRECTION ( 'NONE',  ( -1.000000000000000000, 0.000000000000000000, 0.000000000000000000 ) ) ;
#63643=DIRECTION ( 'NONE',  ( 0.000000000000000000, 0.000000000000000000, 1.000000000000000000 ) ) ;
#63659=EDGE_LOOP ( 'NONE', ( #5842, #27958, #8053, #9045 ) ) ;
#63660=DIRECTION ( 'NONE',  ( 0.000000000000000000, 0.000000000000000000, 1.000000000000000000 ) ) ;
#63666=EDGE_LOOP ( 'NONE', ( #17888, #39712, #68182, #10379 ) ) ;
#63675=EDGE_LOOP ( 'NONE', ( #51070, #6941, #58477, #47807 ) ) ;
#63686=DIRECTION ( 'NONE',  ( 0.000000000000000000, 0.000000000000000000, -1.000000000000000000 ) ) ;
#63688=ORIENTED_EDGE ( 'NONE', *, *, #26377, .F. ) ;
#63689=EDGE_CURVE ( 'NONE', #14272, #6091, #43965, .T. ) ;
#63691=CARTESIAN_POINT ( 'NONE',  ( 39.00000000000000000, -21.00000000000000000, -16.96999999999999886 ) ) ;
#63692=SURFACE_SIDE_STYLE ('',( #35392 ) ) ;
#63694=EDGE_LOOP ( 'NONE', ( #72, #13461, #42930, #7523, #30803, #27257, #6700, #66666 ) ) ;
#63703=DIRECTION ( 'NONE',  ( 0.000000000000000000, 0.000000000000000000, 1.000000000000000000 ) ) ;
#63718=CARTESIAN_POINT ( 'NONE',  ( 41.09999999999999432, -14.06939075806900163, 20.80000000000000426 ) ) ;
#63722=DIRECTION ( 'NONE',  ( 1.000000000000000000, -0.000000000000000000, 0.000000000000000000 ) ) ;
#63723=VECTOR ( 'NONE', #56798, 1000.000000000000000 ) ;
#63730=DIRECTION ( 'NONE',  ( 1.000000000000000000, -0.000000000000000000, 0.000000000000000000 ) ) ;
#63758=VECTOR ( 'NONE', #31927, 1000.000000000000000 ) ;
#63776=LINE ( 'NONE', #52111, #4250 ) ;
#63779=VERTEX_POINT ( 'NONE', #9608 ) ;
#63797=EDGE_LOOP ( 'NONE', ( #59788, #47959, #60175, #17078 ) ) ;
#63804=DIRECTION ( 'NONE',  ( -1.000000000000000000, 0.000000000000000000, 0.000000000000000000 ) ) ;
#63809=MECHANICAL_DESIGN_GEOMETRIC_PRESENTATION_REPRESENTATION('',(#64915),#34391);
#63810=ORIENTED_EDGE ( 'NONE', *, *, #60758, .T. ) ;
#63811=CARTESIAN_POINT ( 'NONE',  ( 10.90000000000000036, -14.06939075806900874, 20.80000000000001137 ) ) ;
#63825=ORIENTED_EDGE ( 'NONE', *, *, #36521, .F. ) ;
#63846=CIRCLE ( 'NONE', #13151, 24.99999999998789946 ) ;
#63851=AXIS2_PLACEMENT_3D ( 'NONE', #33054, #54640, #6188 ) ;
#63855=EDGE_CURVE ( 'NONE', #8645, #13751, #20906, .T. ) ;
#63866=DIRECTION ( 'NONE',  ( -1.000000000000000000, 0.000000000000000000, 0.000000000000000000 ) ) ;
#63867=FILL_AREA_STYLE_COLOUR ( '', #36719 ) ;
#63868=ORIENTED_EDGE ( 'NONE', *, *, #54162, .F. ) ;
#63872=DIRECTION ( 'NONE',  ( 0.000000000000000000, 0.000000000000000000, 1.000000000000000000 ) ) ;
#63875=DIRECTION ( 'NONE',  ( -1.000000000000000000, 0.000000000000000000, 0.000000000000000000 ) ) ;
#63878=DIRECTION ( 'NONE',  ( 0.000000000000000000, 0.000000000000000000, -1.000000000000000000 ) ) ;
#63890=ADVANCED_FACE ( 'NONE', ( #58034 ), #31184, .F. ) ;
#63893=DIRECTION ( 'NONE',  ( 0.000000000000000000, 0.000000000000000000, 1.000000000000000000 ) ) ;
#63895=CIRCLE ( 'NONE', #25486, 24.99999999998789946 ) ;
#63898=ORIENTED_EDGE ( 'NONE', *, *, #14790, .T. ) ;
#63903=DIRECTION ( 'NONE',  ( -1.000000000000000000, 0.000000000000000000, 0.000000000000000000 ) ) ;
#63910=CARTESIAN_POINT ( 'NONE',  ( 14.89999999999999680, -0.1999999999911430404, -8.864436962241481021E-12 ) ) ;
#63920=PLANE ( 'NONE',  #5652 ) ;
#63921=CARTESIAN_POINT ( 'NONE',  ( 41.09999999999999432, -21.00000000000000000, -13.86939075806900057 ) ) ;
#63926=( GEOMETRIC_REPRESENTATION_CONTEXT ( 3 ) GLOBAL_UNCERTAINTY_ASSIGNED_CONTEXT ( ( #20357 ) ) GLOBAL_UNIT_ASSIGNED_CONTEXT ( ( #63624, #37444, #16215 ) ) REPRESENTATION_CONTEXT ( 'NONE', 'WORKASPACE' ) );
#63936=CARTESIAN_POINT ( 'NONE',  ( 46.39999999999999858, 33.00000000000000000, -1.750000000000000222 ) ) ;
#63955=CIRCLE ( 'NONE', #39103, 0.5000000000000000000 ) ;
#63960=CARTESIAN_POINT ( 'NONE',  ( 7.900000000000000355, -21.00000000000000000, 18.00000000000000355 ) ) ;
#63976=LINE ( 'NONE', #37788, #55315 ) ;
#63987=ORIENTED_EDGE ( 'NONE', *, *, #62706, .T. ) ;
#63996=DIRECTION ( 'NONE',  ( 0.000000000000000000, 0.000000000000000000, -1.000000000000000000 ) ) ;
#63998=FACE_OUTER_BOUND ( 'NONE', #18164, .T. ) ;
#64007=DIRECTION ( 'NONE',  ( 0.000000000000000000, 0.7071067811865474617, 0.7071067811865474617 ) ) ;
#64008=AXIS2_PLACEMENT_3D ( 'NONE', #6378, #27940, #17316 ) ;
#64009=CIRCLE ( 'NONE', #33494, 24.99999999998784972 ) ;
#64010=DIRECTION ( 'NONE',  ( 1.000000000000000000, -0.000000000000000000, 0.000000000000000000 ) ) ;
#64019=AXIS2_PLACEMENT_3D ( 'NONE', #19089, #57619, #36046 ) ;
#64031=CARTESIAN_POINT ( 'NONE',  ( 15.89999999999999680, -21.00000000000000000, 13.86939075806900057 ) ) ;
#64038=ORIENTED_EDGE ( 'NONE', *, *, #39085, .T. ) ;
#64048=EDGE_CURVE ( 'NONE', #20196, #41718, #12349, .T. ) ;
#64052=( NAMED_UNIT ( * ) SI_UNIT ( $, .STERADIAN. ) SOLID_ANGLE_UNIT ( ) );
#64055=VERTEX_POINT ( 'NONE', #24018 ) ;
#64087=VECTOR ( 'NONE', #47690, 1000.000000000000000 ) ;
#64097=ORIENTED_EDGE ( 'NONE', *, *, #29933, .F. ) ;
#64106=STYLED_ITEM ( 'NONE', ( #48051 ), #20709 ) ;
#64111=ORIENTED_EDGE ( 'NONE', *, *, #49440, .T. ) ;
#64114=ORIENTED_EDGE ( 'NONE', *, *, #36284, .T. ) ;
#64131=DIRECTION ( 'NONE',  ( -1.000000000000000000, 0.000000000000000000, 0.000000000000000000 ) ) ;
#64132=ORIENTED_EDGE ( 'NONE', *, *, #48235, .T. ) ;
#64157=PRESENTATION_STYLE_ASSIGNMENT (( #31622 ) ) ;
#64159=( GEOMETRIC_REPRESENTATION_CONTEXT ( 3 ) GLOBAL_UNCERTAINTY_ASSIGNED_CONTEXT ( ( #53593 ) ) GLOBAL_UNIT_ASSIGNED_CONTEXT ( ( #26311, #19953, #42217 ) ) REPRESENTATION_CONTEXT ( 'NONE', 'WORKASPACE' ) );
#64177=CARTESIAN_POINT ( 'NONE',  ( 41.09999999999999432, -14.48845687959340012, 21.00000000000000000 ) ) ;
#64178=SURFACE_STYLE_USAGE ( .BOTH. , #63109 ) ;
#64202=ORIENTED_EDGE ( 'NONE', *, *, #43753, .T. ) ;
#64213=CARTESIAN_POINT ( 'NONE',  ( 39.00000000000000000, 16.96999999999999886, -21.00000000000000000 ) ) ;
#64220=AXIS2_PLACEMENT_3D ( 'NONE', #46041, #48052, #69632 ) ;
#64226=VERTEX_POINT ( 'NONE', #14474 ) ;
#64230=EDGE_CURVE ( 'NONE', #7472, #51947, #67862, .T. ) ;
#64233=EDGE_CURVE ( 'NONE', #56183, #66802, #52668, .T. ) ;
#64249=FACE_OUTER_BOUND ( 'NONE', #47747, .T. ) ;
#64254=ORIENTED_EDGE ( 'NONE', *, *, #14790, .F. ) ;
#64257=EDGE_LOOP ( 'NONE', ( #30408, #18312, #38539, #37199 ) ) ;
#64260=DIRECTION ( 'NONE',  ( 0.000000000000000000, -0.5547756303226734076, 0.8320000000000482565 ) ) ;
#64266=CARTESIAN_POINT ( 'NONE',  ( 25.57999999999999829, 0.000000000000000000, 0.000000000000000000 ) ) ;
#64267=ORIENTED_EDGE ( 'NONE', *, *, #7555, .F. ) ;
#64269=AXIS2_PLACEMENT_3D ( 'NONE', #40200, #46203, #30307 ) ;
#64276=AXIS2_PLACEMENT_3D ( 'NONE', #53102, #4655, #26215 ) ;
#64286=ORIENTED_EDGE ( 'NONE', *, *, #32903, .F. ) ;
#64288=DIRECTION ( 'NONE',  ( 0.000000000000000000, 0.000000000000000000, -1.000000000000000000 ) ) ;
#64303=( NAMED_UNIT ( * ) SI_UNIT ( $, .STERADIAN. ) SOLID_ANGLE_UNIT ( ) );
#64304=ORIENTED_EDGE ( 'NONE', *, *, #69137, .F. ) ;
#64310=DIRECTION ( 'NONE',  ( 0.000000000000000000, 0.000000000000000000, -1.000000000000000000 ) ) ;
#64311=AXIS2_PLACEMENT_3D ( 'NONE', #36630, #62436, #46883 ) ;
#64322=DIRECTION ( 'NONE',  ( 0.000000000000000000, 0.7071067811865474617, 0.7071067811865474617 ) ) ;
#64324=DIRECTION ( 'NONE',  ( 1.000000000000000000, -0.000000000000000000, 0.000000000000000000 ) ) ;
#64327=LINE ( 'NONE', #57615, #49011 ) ;
#64342=ADVANCED_FACE ( 'NONE', ( #11923 ), #60027, .T. ) ;
#64345=ORIENTED_EDGE ( 'NONE', *, *, #22526, .T. ) ;
#64349=EDGE_LOOP ( 'NONE', ( #35316, #28149, #49037, #18967 ) ) ;
#64364=ORIENTED_EDGE ( 'NONE', *, *, #65053, .T. ) ;
#64381=EDGE_CURVE ( 'NONE', #7253, #50419, #22559, .T. ) ;
#64400=LINE ( 'NONE', #16294, #14745 ) ;
#64413=CARTESIAN_POINT ( 'NONE',  ( 49.00000000000000000, 20.60000000000000142, -13.86939075806900057 ) ) ;
#64414=AXIS2_PLACEMENT_3D ( 'NONE', #42652, #3771, #46899 ) ;
#64422=VERTEX_POINT ( 'NONE', #5271 ) ;
#64426=DIRECTION ( 'NONE',  ( -1.000000000000000000, 0.000000000000000000, 0.000000000000000000 ) ) ;
#64437=CARTESIAN_POINT ( 'NONE',  ( 49.00000000000000000, -0.1999999999911430404, -8.864436962241481021E-12 ) ) ;
#64441=EDGE_CURVE ( 'NONE', #55425, #64531, #27177, .T. ) ;
#64442=LINE ( 'NONE', #16001, #15355 ) ;
#64446=ADVANCED_FACE ( 'NONE', ( #6293, #27866 ), #49439, .T. ) ;
#64459=EDGE_LOOP ( 'NONE', ( #42926, #48368, #62691, #62180 ) ) ;
#64462=AXIS2_PLACEMENT_3D ( 'NONE', #59793, #15631, #58758 ) ;
#64470=ORIENTED_EDGE ( 'NONE', *, *, #54711, .F. ) ;
#64474=AXIS2_PLACEMENT_3D ( 'NONE', #41892, #47553, #46840 ) ;
#64483=FACE_OUTER_BOUND ( 'NONE', #61514, .T. ) ;
#64495=DIRECTION ( 'NONE',  ( 0.5001543609659999667, 1.060466075314215496E-16, 0.8659362650950080953 ) ) ;
#64503=ORIENTED_EDGE ( 'NONE', *, *, #9036, .T. ) ;
#64513=AXIS2_PLACEMENT_3D ( 'NONE', #21018, #49628, #55288 ) ;
#64529=DIRECTION ( 'NONE',  ( 1.000000000000000000, -0.000000000000000000, 0.000000000000000000 ) ) ;
#64531=VERTEX_POINT ( 'NONE', #17585 ) ;
#64553=FACE_OUTER_BOUND ( 'NONE', #25404, .T. ) ;
#64554=AXIS2_PLACEMENT_3D ( 'NONE', #37516, #21256, #734 ) ;
#64559=CLOSED_SHELL ( 'NONE', ( #849, #1036, #64446, #27249, #5443, #18962, #55418, #62594, #44550, #48120, #69823, #67729 ) ) ;
#64579=FACE_OUTER_BOUND ( 'NONE', #45467, .T. ) ;
#64581=DIRECTION ( 'NONE',  ( 1.000000000000000000, 0.000000000000000000, 0.000000000000000000 ) ) ;
#64584=DIRECTION ( 'NONE',  ( 0.000000000000000000, 0.000000000000000000, -1.000000000000000000 ) ) ;
#64593=FACE_OUTER_BOUND ( 'NONE', #54156, .T. ) ;
#64608=FACE_OUTER_BOUND ( 'NONE', #38693, .T. ) ;
#64614=FACE_OUTER_BOUND ( 'NONE', #3919, .T. ) ;
#64619=VERTEX_POINT ( 'NONE', #34878 ) ;
#64628=ORIENTED_EDGE ( 'NONE', *, *, #11103, .F. ) ;
#64648=ORIENTED_EDGE ( 'NONE', *, *, #14884, .T. ) ;
#64660=AXIS2_PLACEMENT_3D ( 'NONE', #60054, #34556, #27884 ) ;
#64667=FACE_OUTER_BOUND ( 'NONE', #10030, .T. ) ;
#64669=AXIS2_PLACEMENT_3D ( 'NONE', #43419, #11240, #65687 ) ;
#64671=CARTESIAN_POINT ( 'NONE',  ( 39.00000000000000000, 0.000000000000000000, 0.000000000000000000 ) ) ;
#64675=DIRECTION ( 'NONE',  ( 0.000000000000000000, 0.7071067811865474617, -0.7071067811865474617 ) ) ;
#64686=ORIENTED_EDGE ( 'NONE', *, *, #68656, .T. ) ;
#64690=DIRECTION ( 'NONE',  ( 0.000000000000000000, -1.000000000000000000, 0.000000000000000000 ) ) ;
#64694=VERTEX_POINT ( 'NONE', #56805 ) ;
#64704=VERTEX_POINT ( 'NONE', #14734 ) ;
#64713=CIRCLE ( 'NONE', #59111, 24.99999999998784972 ) ;
#64731=ORIENTED_EDGE ( 'NONE', *, *, #44270, .T. ) ;
#64757=EDGE_CURVE ( 'NONE', #12819, #53577, #35949, .T. ) ;
#64758=CIRCLE ( 'NONE', #4956, 25.39999999999999858 ) ;
#64762=EDGE_CURVE ( 'NONE', #48516, #18370, #9077, .T. ) ;
#64766=DIRECTION ( 'NONE',  ( 1.000000000000000000, -0.000000000000000000, 0.000000000000000000 ) ) ;
#64768=STYLED_ITEM ( 'NONE', ( #26680 ), #66294 ) ;
#64770=EDGE_CURVE ( 'NONE', #69700, #64422, #26052, .T. ) ;
#64779=CARTESIAN_POINT ( 'NONE',  ( 41.09999999999999432, 14.08845687959340331, 21.00000000000000000 ) ) ;
#64791=ORIENTED_EDGE ( 'NONE', *, *, #16709, .T. ) ;
#64794=ORIENTED_EDGE ( 'NONE', *, *, #39303, .T. ) ;
#64795=ORIENTED_EDGE ( 'NONE', *, *, #47321, .F. ) ;
#64799=DIRECTION ( 'NONE',  ( 1.000000000000000000, -0.000000000000000000, 0.000000000000000000 ) ) ;
#64809=DIRECTION ( 'NONE',  ( 1.000000000000000000, -0.000000000000000000, 0.000000000000000000 ) ) ;
#64847=EDGE_CURVE ( 'NONE', #66802, #13113, #38766, .T. ) ;
#64849=ORIENTED_EDGE ( 'NONE', *, *, #2200, .T. ) ;
#64856=EDGE_LOOP ( 'NONE', ( #53293, #44883, #26272, #62328 ) ) ;
#64861=LINE ( 'NONE', #12135, #18505 ) ;
#64872=CARTESIAN_POINT ( 'NONE',  ( 41.09999999999999432, 20.60000000000000142, -13.86939075806900057 ) ) ;
#64878=CIRCLE ( 'NONE', #47906, 2.458500000000000796 ) ;
#64882=DIRECTION ( 'NONE',  ( 1.000000000000000000, -0.000000000000000000, -0.000000000000000000 ) ) ;
#64885=VECTOR ( 'NONE', #60191, 1000.000000000000000 ) ;
#64895=DIRECTION ( 'NONE',  ( 0.000000000000000000, 0.000000000000000000, 1.000000000000000000 ) ) ;
#64904=CARTESIAN_POINT ( 'NONE',  ( 22.90000000000000213, -21.00000000000000000, 13.86939075806900057 ) ) ;
#64908=ADVANCED_FACE ( 'NONE', ( #60648 ), #17162, .T. ) ;
#64915=STYLED_ITEM ( 'NONE', ( #66412 ), #67216 ) ;
#64918=EDGE_CURVE ( 'NONE', #20883, #60595, #33161, .T. ) ;
#64950=AXIS2_PLACEMENT_3D ( 'NONE', #29786, #62309, #18834 ) ;
#64960=EDGE_CURVE ( 'NONE', #34559, #67161, #44714, .T. ) ;
#64969=CARTESIAN_POINT ( 'NONE',  ( 38.90000000000000568, 13.66939075806899950, 20.80000000000000426 ) ) ;
#64972=ORIENTED_EDGE ( 'NONE', *, *, #37162, .T. ) ;
#64978=CARTESIAN_POINT ( 'NONE',  ( 50.00000000000000711, 0.7500000000000000000, 4.943429983321300902 ) ) ;
#64981=MECHANICAL_DESIGN_GEOMETRIC_PRESENTATION_REPRESENTATION('',(#67230),#18667);
#64984=ORIENTED_EDGE ( 'NONE', *, *, #19261, .T. ) ;
#64985=MECHANICAL_DESIGN_GEOMETRIC_PRESENTATION_REPRESENTATION('',(#46891),#6326);
#64986=DIRECTION ( 'NONE',  ( 0.000000000000000000, 0.000000000000000000, 1.000000000000000000 ) ) ;
#64987=ORIENTED_EDGE ( 'NONE', *, *, #3301, .T. ) ;
#64991=EDGE_CURVE ( 'NONE', #60595, #38472, #49687, .T. ) ;
#64998=CARTESIAN_POINT ( 'NONE',  ( 49.00000000000000000, -0.7500000000000000000, -3.929058411375430104 ) ) ;
#65007=CARTESIAN_POINT ( 'NONE',  ( 41.09999999999999432, -21.00000000000000000, 14.57806571531351914 ) ) ;
#65017=FACE_OUTER_BOUND ( 'NONE', #3005, .T. ) ;
#65034=LINE ( 'NONE', #42763, #40863 ) ;
#65046=VERTEX_POINT ( 'NONE', #49244 ) ;
#65048=FACE_OUTER_BOUND ( 'NONE', #30071, .T. ) ;
#65051=EDGE_LOOP ( 'NONE', ( #28924, #19893, #9821, #45895 ) ) ;
#65053=EDGE_CURVE ( 'NONE', #1557, #50270, #61356, .T. ) ;
#65063=VERTEX_POINT ( 'NONE', #110 ) ;
#65070=ORIENTED_EDGE ( 'NONE', *, *, #58776, .T. ) ;
#65071=ORIENTED_EDGE ( 'NONE', *, *, #51678, .F. ) ;
#65079=LINE ( 'NONE', #48116, #18822 ) ;
#65080=CARTESIAN_POINT ( 'NONE',  ( 17.89999999999999858, -0.000000000000000000, -20.80000000000000426 ) ) ;
#65110=CARTESIAN_POINT ( 'NONE',  ( 28.90000000000000213, -14.06939075806900163, -20.80000000000000426 ) ) ;
#65111=ORIENTED_EDGE ( 'NONE', *, *, #15636, .F. ) ;
#65112=DIRECTION ( 'NONE',  ( 1.000000000000000000, -0.000000000000000000, 0.000000000000000000 ) ) ;
#65119=DIRECTION ( 'NONE',  ( 0.000000000000000000, 0.000000000000000000, -1.000000000000000000 ) ) ;
#65120=EDGE_CURVE ( 'NONE', #58826, #29208, #42879, .T. ) ;
#65121=VECTOR ( 'NONE', #49928, 1000.000000000000000 ) ;
#65130=VECTOR ( 'NONE', #52622, 1000.000000000000000 ) ;
#65131=VECTOR ( 'NONE', #2966, 1000.000000000000000 ) ;
#65153=CARTESIAN_POINT ( 'NONE',  ( 41.09999999999999432, -14.06939075806901940, -20.80000000000000426 ) ) ;
#65162=( GEOMETRIC_REPRESENTATION_CONTEXT ( 3 ) GLOBAL_UNCERTAINTY_ASSIGNED_CONTEXT ( ( #19644 ) ) GLOBAL_UNIT_ASSIGNED_CONTEXT ( ( #53350, #69248, #63605 ) ) REPRESENTATION_CONTEXT ( 'NONE', 'WORKASPACE' ) );
#65169=ADVANCED_FACE ( 'NONE', ( #49576, #55573 ), #23039, .F. ) ;
#65171=ORIENTED_EDGE ( 'NONE', *, *, #47464, .F. ) ;
#65195=EDGE_CURVE ( 'NONE', #1574, #38911, #24128, .T. ) ;
#65227=ORIENTED_EDGE ( 'NONE', *, *, #63341, .F. ) ;
#65237=CARTESIAN_POINT ( 'NONE',  ( 49.00000000000000000, -0.1999999999911430404, -8.864436962241481021E-12 ) ) ;
#65242=ORIENTED_EDGE ( 'NONE', *, *, #14618, .T. ) ;
#65247=ORIENTED_EDGE ( 'NONE', *, *, #8533, .F. ) ;
#65275=DIRECTION ( 'NONE',  ( 0.000000000000000000, 0.000000000000000000, 1.000000000000000000 ) ) ;
#65291=CARTESIAN_POINT ( 'NONE',  ( 49.00000000000000000, 13.66939075806899950, 20.80000000000000426 ) ) ;
#65308=FACE_OUTER_BOUND ( 'NONE', #40743, .T. ) ;
#65309=ORIENTED_EDGE ( 'NONE', *, *, #2366, .F. ) ;
#65321=CARTESIAN_POINT ( 'NONE',  ( 8.900000000000002132, 0.000000000000000000, 0.000000000000000000 ) ) ;
#65346=ORIENTED_EDGE ( 'NONE', *, *, #65120, .T. ) ;
#65351=AXIS2_PLACEMENT_3D ( 'NONE', #12919, #46159, #50426 ) ;
#65359=DIRECTION ( 'NONE',  ( -1.000000000000000000, 0.000000000000000000, 0.000000000000000000 ) ) ;
#65363=ADVANCED_FACE ( 'NONE', ( #26194 ), #25852, .F. ) ;
#65374=CARTESIAN_POINT ( 'NONE',  ( 40.90000000000000568, 21.00000000000000000, -16.96999999999999886 ) ) ;
#65381=DIRECTION ( 'NONE',  ( -1.000000000000000000, 0.000000000000000000, 0.000000000000000000 ) ) ;
#65444=EDGE_CURVE ( 'NONE', #11546, #54114, #67619, .T. ) ;
#65448=LINE ( 'NONE', #17693, #12790 ) ;
#65458=DIRECTION ( 'NONE',  ( 0.000000000000000000, 0.000000000000000000, -1.000000000000000000 ) ) ;
#65459=ORIENTED_EDGE ( 'NONE', *, *, #39862, .T. ) ;
#65463=VECTOR ( 'NONE', #13764, 1000.000000000000000 ) ;
#65476=LINE ( 'NONE', #16698, #25299 ) ;
#65479=AXIS2_PLACEMENT_3D ( 'NONE', #37748, #69583, #20777 ) ;
#65482=ORIENTED_EDGE ( 'NONE', *, *, #40272, .T. ) ;
#65498=CARTESIAN_POINT ( 'NONE',  ( 9.900000000000000355, -0.000000000000000000, -20.80000000000000426 ) ) ;
#65499=DIRECTION ( 'NONE',  ( 0.000000000000000000, 0.000000000000000000, -1.000000000000000000 ) ) ;
#65504=CARTESIAN_POINT ( 'NONE',  ( 22.90000000000000213, -14.06939075806900163, -20.80000000000000426 ) ) ;
#65508=AXIS2_PLACEMENT_3D ( 'NONE', #18583, #40144, #55388 ) ;
#65513=EDGE_LOOP ( 'NONE', ( #49296, #1485, #67847, #42785 ) ) ;
#65519=CARTESIAN_POINT ( 'NONE',  ( 21.90000000000000213, -0.000000000000000000, 20.80000000000000426 ) ) ;
#65520=ORIENTED_EDGE ( 'NONE', *, *, #39704, .F. ) ;
#65535=ORIENTED_EDGE ( 'NONE', *, *, #44132, .T. ) ;
#65547=EDGE_CURVE ( 'NONE', #34324, #30734, #21921, .T. ) ;
#65549=ORIENTED_EDGE ( 'NONE', *, *, #59524, .F. ) ;
#65551=DIRECTION ( 'NONE',  ( 0.000000000000000000, 0.000000000000000000, -1.000000000000000000 ) ) ;
#65580=ORIENTED_EDGE ( 'NONE', *, *, #3614, .T. ) ;
#65589=CARTESIAN_POINT ( 'NONE',  ( 41.09999999999999432, -14.06939075806901940, -20.80000000000000426 ) ) ;
#65593=PLANE ( 'NONE',  #22528 ) ;
#65598=CIRCLE ( 'NONE', #62207, 24.99999999998784972 ) ;
#65607=DIRECTION ( 'NONE',  ( -1.000000000000000000, 0.000000000000000000, 0.000000000000000000 ) ) ;
#65608=CARTESIAN_POINT ( 'NONE',  ( 9.900000000000000355, 21.00000000000000000, 18.00000000000000355 ) ) ;
#65613=ORIENTED_EDGE ( 'NONE', *, *, #16243, .T. ) ;
#65649=CARTESIAN_POINT ( 'NONE',  ( 8.900000000000002132, 21.00000000000000000, 18.00000000000000355 ) ) ;
#65660=CLOSED_SHELL ( 'NONE', ( #69810, #69069, #23729, #6505, #47164, #59281 ) ) ;
#65664=LINE ( 'NONE', #622, #28578 ) ;
#65670=ORIENTED_EDGE ( 'NONE', *, *, #54144, .T. ) ;
#65673=ADVANCED_FACE ( 'NONE', ( #28222 ), #39180, .F. ) ;
#65677=CARTESIAN_POINT ( 'NONE',  ( 16.89999999999999858, -14.06939075806900874, 20.80000000000001137 ) ) ;
#65687=DIRECTION ( 'NONE',  ( 0.000000000000000000, 0.000000000000000000, -1.000000000000000000 ) ) ;
#65701=EDGE_LOOP ( 'NONE', ( #61670, #34033, #38443, #36706 ) ) ;
#65717=CARTESIAN_POINT ( 'NONE',  ( 25.57999999999999829, 0.000000000000000000, 0.000000000000000000 ) ) ;
#65758=VECTOR ( 'NONE', #20145, 1000.000000000000000 ) ;
#65771=ORIENTED_EDGE ( 'NONE', *, *, #2768, .T. ) ;
#65792=EDGE_CURVE ( 'NONE', #53157, #66031, #7684, .T. ) ;
#65805=ORIENTED_EDGE ( 'NONE', *, *, #9969, .F. ) ;
#65807=DIRECTION ( 'NONE',  ( 1.000000000000000000, 0.000000000000000000, 0.000000000000000000 ) ) ;
#65813=CARTESIAN_POINT ( 'NONE',  ( 46.39999999999999858, 21.00000000000000000, 1.250000000000000000 ) ) ;
#65815=DIRECTION ( 'NONE',  ( -1.000000000000000000, 0.000000000000000000, 0.000000000000000000 ) ) ;
#65817=DIRECTION ( 'NONE',  ( 0.000000000000000000, 0.000000000000000000, -1.000000000000000000 ) ) ;
#65828=MANIFOLD_SOLID_BREP ( 'LPattern1[6]', #10356 ) ;
#65829=LINE ( 'NONE', #44590, #53444 ) ;
#65834=CARTESIAN_POINT ( 'NONE',  ( 30.90000000000000213, -0.1999999999911795112, 8.826273045769999343E-12 ) ) ;
#65852=PLANE ( 'NONE',  #36138 ) ;
#65853=ORIENTED_EDGE ( 'NONE', *, *, #12175, .F. ) ;
#65862=CARTESIAN_POINT ( 'NONE',  ( 40.90000000000000568, -21.00000000000001421, -13.86939075806900945 ) ) ;
#65872=ORIENTED_EDGE ( 'NONE', *, *, #57550, .T. ) ;
#65873=CARTESIAN_POINT ( 'NONE',  ( 27.90000000000000213, -0.000000000000000000, -20.80000000000000071 ) ) ;
#65877=CARTESIAN_POINT ( 'NONE',  ( 41.09999999999999432, -14.06939075806900163, 20.80000000000000426 ) ) ;
#65890=ORIENTED_EDGE ( 'NONE', *, *, #68349, .T. ) ;
#65895=ORIENTED_EDGE ( 'NONE', *, *, #46515, .T. ) ;
#65899=CIRCLE ( 'NONE', #28598, 24.99999999998789946 ) ;
#65908=AXIS2_PLACEMENT_3D ( 'NONE', #22808, #45404, #33757 ) ;
#65910=EDGE_CURVE ( 'NONE', #14663, #29539, #66966, .T. ) ;
#65935=AXIS2_PLACEMENT_3D ( 'NONE', #59712, #54419, #27533 ) ;
#65936=CARTESIAN_POINT ( 'NONE',  ( 39.00000000000000000, -21.00000000000000000, -16.96999999999999886 ) ) ;
#65938=DIRECTION ( 'NONE',  ( 0.000000000000000000, 0.000000000000000000, -1.000000000000000000 ) ) ;
#65958=EDGE_CURVE ( 'NONE', #45256, #54885, #68851, .T. ) ;
#65960=LINE ( 'NONE', #11179, #20694 ) ;
#65971=VERTEX_POINT ( 'NONE', #39435 ) ;
#65972=CARTESIAN_POINT ( 'NONE',  ( 39.00000000000000000, -5.250000000000000000, 0.000000000000000000 ) ) ;
#65991=CARTESIAN_POINT ( 'NONE',  ( 28.90000000000000213, 0.000000000000000000, 0.000000000000000000 ) ) ;
#65999=VECTOR ( 'NONE', #52335, 1000.000000000000114 ) ;
#66002=FACE_OUTER_BOUND ( 'NONE', #18677, .T. ) ;
#66004=EDGE_CURVE ( 'NONE', #44820, #46180, #65960, .T. ) ;
#66006=( GEOMETRIC_REPRESENTATION_CONTEXT ( 3 ) GLOBAL_UNCERTAINTY_ASSIGNED_CONTEXT ( ( #38032 ) ) GLOBAL_UNIT_ASSIGNED_CONTEXT ( ( #51157, #68835, #2718 ) ) REPRESENTATION_CONTEXT ( 'NONE', 'WORKASPACE' ) );
#66011=DIRECTION ( 'NONE',  ( -1.000000000000000000, 0.000000000000000000, 0.000000000000000000 ) ) ;
#66027=LINE ( 'NONE', #12272, #29161 ) ;
#66029=CARTESIAN_POINT ( 'NONE',  ( 33.89999999999999858, -0.2000000000089119934, 8.909539772616881237E-12 ) ) ;
#66031=VERTEX_POINT ( 'NONE', #54680 ) ;
#66043=CARTESIAN_POINT ( 'NONE',  ( 29.89999999999999858, -14.06939075806902117, -20.80000000000000426 ) ) ;
#66047=DIRECTION ( 'NONE',  ( -1.000000000000000000, 0.000000000000000000, 0.000000000000000000 ) ) ;
#66052=( LENGTH_UNIT ( ) NAMED_UNIT ( * ) SI_UNIT ( .MILLI., .METRE. ) );
#66055=ORIENTED_EDGE ( 'NONE', *, *, #33769, .T. ) ;
#66076=DIRECTION ( 'NONE',  ( 0.000000000000000000, 0.000000000000000000, 1.000000000000000000 ) ) ;
#66079=VERTEX_POINT ( 'NONE', #39097 ) ;
#66084=DIRECTION ( 'NONE',  ( -1.000000000000000000, 0.000000000000000000, 0.000000000000000000 ) ) ;
#66087=LINE ( 'NONE', #17662, #43266 ) ;
#66090=EDGE_CURVE ( 'NONE', #47619, #59376, #27453, .T. ) ;
#66099=DIRECTION ( 'NONE',  ( -1.000000000000000000, 0.000000000000000000, 0.000000000000000000 ) ) ;
#66101=CARTESIAN_POINT ( 'NONE',  ( 49.00000000000000000, -0.7500000000000000000, 3.929058411375430104 ) ) ;
#66138=ORIENTED_EDGE ( 'NONE', *, *, #53762, .T. ) ;
#66166=PLANE ( 'NONE',  #33002 ) ;
#66174=MANIFOLD_SOLID_BREP ( 'Cut-Extrude1[5]', #40820 ) ;
#66191=CARTESIAN_POINT ( 'NONE',  ( 12.90000000000000213, 13.66939075806899240, -20.79999999999999361 ) ) ;
#66200=PLANE ( 'NONE',  #37212 ) ;
#66201=CARTESIAN_POINT ( 'NONE',  ( 41.09999999999999432, 13.66939075806899950, 20.80000000000000426 ) ) ;
#66210=AXIS2_PLACEMENT_3D ( 'NONE', #55184, #22663, #44210 ) ;
#66216=AXIS2_PLACEMENT_3D ( 'NONE', #47856, #26648, #52843 ) ;
#66217=CIRCLE ( 'NONE', #609, 24.99999999998794920 ) ;
#66218=AXIS2_PLACEMENT_3D ( 'NONE', #34582, #56171, #51200 ) ;
#66219=DIRECTION ( 'NONE',  ( 1.000000000000000000, -0.000000000000000000, 0.000000000000000000 ) ) ;
#66228=LINE ( 'NONE', #65873, #11301 ) ;
#66240=ORIENTED_EDGE ( 'NONE', *, *, #42387, .T. ) ;
#66243=FACE_OUTER_BOUND ( 'NONE', #57179, .T. ) ;
#66250=EDGE_LOOP ( 'NONE', ( #8030, #37218, #24398, #43156 ) ) ;
#66264=EDGE_LOOP ( 'NONE', ( #44871, #31552, #51060, #49421 ) ) ;
#66266=AXIS2_PLACEMENT_3D ( 'NONE', #26918, #48479, #41237 ) ;
#66269=ORIENTED_EDGE ( 'NONE', *, *, #49359, .F. ) ;
#66294=MANIFOLD_SOLID_BREP ( 'LPattern1[25]', #26156 ) ;
#66305=DIRECTION ( 'NONE',  ( 0.000000000000000000, -1.000000000000000000, 0.000000000000000000 ) ) ;
#66320=ORIENTED_EDGE ( 'NONE', *, *, #68542, .T. ) ;
#66327=ORIENTED_EDGE ( 'NONE', *, *, #54330, .T. ) ;
#66343=ORIENTED_EDGE ( 'NONE', *, *, #16798, .T. ) ;
#66344=PLANE ( 'NONE',  #52718 ) ;
#66355=EDGE_CURVE ( 'NONE', #33050, #48502, #37643, .T. ) ;
#66371=EDGE_CURVE ( 'NONE', #32538, #2059, #64861, .T. ) ;
#66377=ORIENTED_EDGE ( 'NONE', *, *, #22130, .T. ) ;
#66380=CARTESIAN_POINT ( 'NONE',  ( 41.09999999999999432, -0.2000000000000000111, 0.000000000000000000 ) ) ;
#66392=EDGE_LOOP ( 'NONE', ( #65070, #64849, #20687, #69359 ) ) ;
#66401=ORIENTED_EDGE ( 'NONE', *, *, #3614, .F. ) ;
#66412=PRESENTATION_STYLE_ASSIGNMENT (( #63120 ) ) ;
#66415=ORIENTED_EDGE ( 'NONE', *, *, #53349, .F. ) ;
#66430=ORIENTED_EDGE ( 'NONE', *, *, #18936, .F. ) ;
#66451=CARTESIAN_POINT ( 'NONE',  ( 17.89999999999999858, -14.06939075806902117, -20.80000000000000426 ) ) ;
#66457=DIRECTION ( 'NONE',  ( 0.000000000000000000, -0.7071067811865474617, 0.7071067811865474617 ) ) ;
#66459=FACE_BOUND ( 'NONE', #52600, .T. ) ;
#66490=DIRECTION ( 'NONE',  ( -1.000000000000000000, 0.000000000000000000, 0.000000000000000000 ) ) ;
#66491=EDGE_CURVE ( 'NONE', #31468, #30799, #2925, .T. ) ;
#66492=DIRECTION ( 'NONE',  ( 1.000000000000000000, -0.000000000000000000, 0.000000000000000000 ) ) ;
#66503=CARTESIAN_POINT ( 'NONE',  ( 15.89999999999999680, -0.2000000000089119934, -8.913009219568841313E-12 ) ) ;
#66506=ORIENTED_EDGE ( 'NONE', *, *, #19605, .T. ) ;
#66511=ORIENTED_EDGE ( 'NONE', *, *, #19327, .F. ) ;
#66515=CARTESIAN_POINT ( 'NONE',  ( 27.90000000000000213, -0.000000000000000000, 20.80000000000000426 ) ) ;
#66531=EDGE_CURVE ( 'NONE', #63520, #17564, #13176, .T. ) ;
#66553=CARTESIAN_POINT ( 'NONE',  ( 9.900000000000000355, -21.00000000000000000, 18.00000000000000355 ) ) ;
#66559=ORIENTED_EDGE ( 'NONE', *, *, #69404, .T. ) ;
#66576=PLANE ( 'NONE',  #2850 ) ;
#66580=LINE ( 'NONE', #62313, #26105 ) ;
#66593=ADVANCED_FACE ( 'NONE', ( #9635 ), #21292, .T. ) ;
#66601=VECTOR ( 'NONE', #41255, 1000.000000000000000 ) ;
#66603=ORIENTED_EDGE ( 'NONE', *, *, #43207, .F. ) ;
#66611=ORIENTED_EDGE ( 'NONE', *, *, #50701, .F. ) ;
#66626=CARTESIAN_POINT ( 'NONE',  ( 10.00000000000000000, 14.08845687959340331, 21.00000000000000000 ) ) ;
#66635=CYLINDRICAL_SURFACE ( 'NONE', #3079, 5.250000000000000000 ) ;
#66637=CARTESIAN_POINT ( 'NONE',  ( 49.00000000000000000, -0.7500000000000000000, 4.943429983321300014 ) ) ;
#66638=ORIENTED_EDGE ( 'NONE', *, *, #14781, .F. ) ;
#66643=ADVANCED_FACE ( 'NONE', ( #26591 ), #46750, .T. ) ;
#66646=DIRECTION ( 'NONE',  ( 1.000000000000000000, -0.000000000000000000, 0.000000000000000000 ) ) ;
#66651=DIRECTION ( 'NONE',  ( 0.000000000000000000, -0.7071067811865474617, 0.7071067811865474617 ) ) ;
#66652=CARTESIAN_POINT ( 'NONE',  ( 37.90000000000000568, 0.000000000000000000, 2.458500000000000796 ) ) ;
#66660=EDGE_CURVE ( 'NONE', #23509, #49868, #35465, .T. ) ;
#66664=ORIENTED_EDGE ( 'NONE', *, *, #7903, .F. ) ;
#66666=ORIENTED_EDGE ( 'NONE', *, *, #21024, .F. ) ;
#66676=ORIENTED_EDGE ( 'NONE', *, *, #46240, .T. ) ;
#66679=DIRECTION ( 'NONE',  ( 0.000000000000000000, 0.000000000000000000, -1.000000000000000000 ) ) ;
#66684=ORIENTED_EDGE ( 'NONE', *, *, #41424, .F. ) ;
#66685=CARTESIAN_POINT ( 'NONE',  ( 49.00000000000000000, -21.00000000000000000, 13.86939075806900057 ) ) ;
#66699=ORIENTED_EDGE ( 'NONE', *, *, #2768, .F. ) ;
#66718=ORIENTED_EDGE ( 'NONE', *, *, #5303, .F. ) ;
#66725=DIRECTION ( 'NONE',  ( 0.000000000000000000, 0.000000000000000000, -1.000000000000000000 ) ) ;
#66742=ADVANCED_FACE ( 'NONE', ( #48861 ), #421, .F. ) ;
#66748=CIRCLE ( 'NONE', #50960, 24.99999999998794920 ) ;
#66750=DIRECTION ( 'NONE',  ( 1.000000000000000000, 0.000000000000000000, 0.000000000000000000 ) ) ;
#66761=CARTESIAN_POINT ( 'NONE',  ( 25.57999999999999829, 0.000000000000000000, 0.000000000000000000 ) ) ;
#66764=DIRECTION ( 'NONE',  ( 0.000000000000000000, 0.000000000000000000, 1.000000000000000000 ) ) ;
#66766=ORIENTED_EDGE ( 'NONE', *, *, #18664, .T. ) ;
#66767=DIRECTION ( 'NONE',  ( 0.000000000000000000, 0.000000000000000000, -1.000000000000000000 ) ) ;
#66769=ORIENTED_EDGE ( 'NONE', *, *, #56117, .T. ) ;
#66771=ORIENTED_EDGE ( 'NONE', *, *, #30666, .F. ) ;
#66779=ORIENTED_EDGE ( 'NONE', *, *, #4347, .T. ) ;
#66802=VERTEX_POINT ( 'NONE', #37558 ) ;
#66804=DIRECTION ( 'NONE',  ( 1.000000000000000000, -0.000000000000000000, 0.000000000000000000 ) ) ;
#66814=VERTEX_POINT ( 'NONE', #54517 ) ;
#66819=EDGE_CURVE ( 'NONE', #31121, #2764, #37905, .T. ) ;
#66823=EDGE_CURVE ( 'NONE', #57134, #18694, #27983, .T. ) ;
#66832=DIRECTION ( 'NONE',  ( 1.000000000000000000, -0.000000000000000000, 0.000000000000000000 ) ) ;
#66833=CARTESIAN_POINT ( 'NONE',  ( 49.00000000000000000, -0.7500000000000000000, 3.929058411375430104 ) ) ;
#66848=DIRECTION ( 'NONE',  ( 0.000000000000000000, 0.7071067811865474617, 0.7071067811865474617 ) ) ;
#66854=AXIS2_PLACEMENT_3D ( 'NONE', #31025, #53649, #53308 ) ;
#66857=MANIFOLD_SOLID_BREP ( 'LPattern1[3]', #6939 ) ;
#66865=ADVANCED_FACE ( 'NONE', ( #13791 ), #50586, .F. ) ;
#66867=FACE_BOUND ( 'NONE', #33932, .T. ) ;
#66868=CARTESIAN_POINT ( 'NONE',  ( 39.90000000000000568, 16.96999999999999886, -21.00000000000000000 ) ) ;
#66872=ORIENTED_EDGE ( 'NONE', *, *, #28672, .T. ) ;
#66898=EDGE_CURVE ( 'NONE', #46985, #14663, #35002, .T. ) ;
#66902=EDGE_CURVE ( 'NONE', #50419, #28489, #14017, .T. ) ;
#66904=VECTOR ( 'NONE', #2235, 1000.000000000000000 ) ;
#66905=EDGE_LOOP ( 'NONE', ( #28768, #68083, #9642, #39687 ) ) ;
#66926=LINE ( 'NONE', #3639, #13398 ) ;
#66933=ORIENTED_EDGE ( 'NONE', *, *, #33987, .F. ) ;
#66952=ORIENTED_EDGE ( 'NONE', *, *, #21777, .T. ) ;
#66953=DIRECTION ( 'NONE',  ( -1.000000000000000000, 0.000000000000000000, 0.000000000000000000 ) ) ;
#66956=EDGE_CURVE ( 'NONE', #69324, #23983, #4261, .T. ) ;
#66964=CIRCLE ( 'NONE', #15049, 2.458500000000000796 ) ;
#66965=VERTEX_POINT ( 'NONE', #53047 ) ;
#66966=CIRCLE ( 'NONE', #16159, 3.500000000000000444 ) ;
#66967=EDGE_CURVE ( 'NONE', #54114, #42963, #26169, .T. ) ;
#66971=( GEOMETRIC_REPRESENTATION_CONTEXT ( 3 ) GLOBAL_UNCERTAINTY_ASSIGNED_CONTEXT ( ( #68457 ) ) GLOBAL_UNIT_ASSIGNED_CONTEXT ( ( #62185, #62532, #29657 ) ) REPRESENTATION_CONTEXT ( 'NONE', 'WORKASPACE' ) );
#66978=VERTEX_POINT ( 'NONE', #36061 ) ;
#66989=DIRECTION ( 'NONE',  ( 0.000000000000000000, 0.7071067811865474617, -0.7071067811865474617 ) ) ;
#67002=PLANE ( 'NONE',  #38458 ) ;
#67005=DIRECTION ( 'NONE',  ( 0.000000000000000000, 0.7071067811865474617, 0.7071067811865474617 ) ) ;
#67008=CARTESIAN_POINT ( 'NONE',  ( 0.000000000000000000, -0.7500000000000000000, 0.000000000000000000 ) ) ;
#67009=ORIENTED_EDGE ( 'NONE', *, *, #37981, .F. ) ;
#67010=EDGE_CURVE ( 'NONE', #41893, #68810, #46667, .T. ) ;
#67015=VERTEX_POINT ( 'NONE', #15573 ) ;
#67016=VECTOR ( 'NONE', #23267, 1000.000000000000000 ) ;
#67017=VECTOR ( 'NONE', #44732, 1000.000000000000000 ) ;
#67018=DIRECTION ( 'NONE',  ( 0.000000000000000000, 0.000000000000000000, -1.000000000000000000 ) ) ;
#67024=AXIS2_PLACEMENT_3D ( 'NONE', #23858, #39076, #55687 ) ;
#67062=ORIENTED_EDGE ( 'NONE', *, *, #56206, .F. ) ;
#67073=CARTESIAN_POINT ( 'NONE',  ( 13.90000000000000213, -0.2000000000089119934, -8.913009219568841313E-12 ) ) ;
#67082=ORIENTED_EDGE ( 'NONE', *, *, #28472, .F. ) ;
#67086=( NAMED_UNIT ( * ) SI_UNIT ( $, .STERADIAN. ) SOLID_ANGLE_UNIT ( ) );
#67104=ORIENTED_EDGE ( 'NONE', *, *, #19261, .F. ) ;
#67107=ORIENTED_EDGE ( 'NONE', *, *, #58609, .F. ) ;
#67119=VECTOR ( 'NONE', #69796, 1000.000000000000000 ) ;
#67122=EDGE_LOOP ( 'NONE', ( #57654, #19843, #46687, #46277, #43999, #9323, #45096, #47060 ) ) ;
#67148=DIRECTION ( 'NONE',  ( -1.000000000000000000, 0.000000000000000000, 0.000000000000000000 ) ) ;
#67149=EDGE_LOOP ( 'NONE', ( #55615, #36347, #60953, #13896 ) ) ;
#67152=CIRCLE ( 'NONE', #6195, 24.99999999998784972 ) ;
#67157=CARTESIAN_POINT ( 'NONE',  ( 27.90000000000000213, -14.06939075806902117, -20.80000000000000426 ) ) ;
#67161=VERTEX_POINT ( 'NONE', #6328 ) ;
#67163=VECTOR ( 'NONE', #37153, 1000.000000000000000 ) ;
#67169=CARTESIAN_POINT ( 'NONE',  ( 46.39999999999999858, 21.00000000000000000, -2.750000000000000444 ) ) ;
#67173=( LENGTH_UNIT ( ) NAMED_UNIT ( * ) SI_UNIT ( .MILLI., .METRE. ) );
#67183=AXIS2_PLACEMENT_3D ( 'NONE', #58572, #47599, #59866 ) ;
#67186=ADVANCED_FACE ( 'NONE', ( #38177 ), #54769, .T. ) ;
#67193=FACE_OUTER_BOUND ( 'NONE', #56074, .T. ) ;
#67207=ORIENTED_EDGE ( 'NONE', *, *, #43600, .F. ) ;
#67215=B_SPLINE_CURVE_WITH_KNOTS ( 'NONE', 3,
 ( #6705, #2104, #1077, #66101 ),
 .UNSPECIFIED., .F., .F.,
 ( 4, 4 ),
 ( 9.477163989440372305, 10.17593572399551860 ),
 .UNSPECIFIED. ) ;
#67216=MANIFOLD_SOLID_BREP ( 'LPattern1[19]', #37460 ) ;
#67230=STYLED_ITEM ( 'NONE', ( #31629 ), #44638 ) ;
#67236=VERTEX_POINT ( 'NONE', #56491 ) ;
#67260=CARTESIAN_POINT ( 'NONE',  ( 49.00000000000000000, -0.1999999999911795112, 8.826273045769999343E-12 ) ) ;
#67264=ORIENTED_EDGE ( 'NONE', *, *, #16767, .F. ) ;
#67266=DIRECTION ( 'NONE',  ( -1.000000000000000000, 0.000000000000000000, 0.000000000000000000 ) ) ;
#67302=ADVANCED_FACE ( 'NONE', ( #28921 ), #50495, .T. ) ;
#67319=AXIS2_PLACEMENT_3D ( 'NONE', #5691, #47414, #15612 ) ;
#67340=EDGE_CURVE ( 'NONE', #40849, #49649, #31660, .T. ) ;
#67354=CARTESIAN_POINT ( 'NONE',  ( 49.00000000000000000, 0.000000000000000000, 0.000000000000000000 ) ) ;
#67356=DIRECTION ( 'NONE',  ( 0.000000000000000000, 0.000000000000000000, -1.000000000000000000 ) ) ;
#67360=LINE ( 'NONE', #56392, #62389 ) ;
#67375=VECTOR ( 'NONE', #23169, 1000.000000000000000 ) ;
#67378=CARTESIAN_POINT ( 'NONE',  ( 49.00000000000000000, -0.2000000000089119934, 8.909539772616881237E-12 ) ) ;
#67392=LINE ( 'NONE', #7628, #15092 ) ;
#67396=ORIENTED_EDGE ( 'NONE', *, *, #56721, .F. ) ;
#67413=DIRECTION ( 'NONE',  ( 0.000000000000000000, -1.000000000000000000, 0.000000000000000000 ) ) ;
#67428=PRESENTATION_STYLE_ASSIGNMENT (( #41592 ) ) ;
#67449=CARTESIAN_POINT ( 'NONE',  ( 39.00000000000000000, -21.00000000000000000, -14.57806571531351914 ) ) ;
#67450=ORIENTED_EDGE ( 'NONE', *, *, #32686, .T. ) ;
#67479=CARTESIAN_POINT ( 'NONE',  ( 49.00000000000000000, 13.66939075806899950, 20.80000000000000426 ) ) ;
#67480=CARTESIAN_POINT ( 'NONE',  ( 41.09999999999999432, -14.06939075806901940, -20.80000000000000426 ) ) ;
#67493=EDGE_CURVE ( 'NONE', #61430, #12238, #60241, .T. ) ;
#67500=ORIENTED_EDGE ( 'NONE', *, *, #23563, .F. ) ;
#67513=AXIS2_PLACEMENT_3D ( 'NONE', #54239, #49611, #11429 ) ;
#67524=ORIENTED_EDGE ( 'NONE', *, *, #25253, .T. ) ;
#67532=DIRECTION ( 'NONE',  ( 0.000000000000000000, 0.7071067811865474617, 0.7071067811865474617 ) ) ;
#67537=CARTESIAN_POINT ( 'NONE',  ( 8.900000000000005684, -0.2000000000000000111, 0.000000000000000000 ) ) ;
#67541=CARTESIAN_POINT ( 'NONE',  ( 27.90000000000000213, 13.66939075806899240, 20.79999999999999361 ) ) ;
#67551=FILL_AREA_STYLE ('',( #28660 ) ) ;
#67559=ORIENTED_EDGE ( 'NONE', *, *, #67858, .F. ) ;
#67560=DIRECTION ( 'NONE',  ( 0.000000000000000000, 0.000000000000000000, 1.000000000000000000 ) ) ;
#67566=CARTESIAN_POINT ( 'NONE',  ( 39.00000000000000000, 0.000000000000000000, 0.000000000000000000 ) ) ;
#67577=MANIFOLD_SOLID_BREP ( 'LPattern1[23]', #16012 ) ;
#67580=VECTOR ( 'NONE', #17152, 1000.000000000000000 ) ;
#67582=FACE_OUTER_BOUND ( 'NONE', #55216, .T. ) ;
#67590=DIRECTION ( 'NONE',  ( 1.000000000000000000, -0.000000000000000000, 0.000000000000000000 ) ) ;
#67600=DIRECTION ( 'NONE',  ( -1.000000000000000000, 0.000000000000000000, 0.000000000000000000 ) ) ;
#67602=DIRECTION ( 'NONE',  ( 0.000000000000000000, 0.000000000000000000, -1.000000000000000000 ) ) ;
#67603=CARTESIAN_POINT ( 'NONE',  ( 23.90000000000000213, -0.2000000000089119934, 8.909539772616881237E-12 ) ) ;
#67605=DIRECTION ( 'NONE',  ( 1.000000000000000000, 0.000000000000000000, 0.000000000000000000 ) ) ;
#67608=DIRECTION ( 'NONE',  ( 0.000000000000000000, 0.000000000000000000, -1.000000000000000000 ) ) ;
#67615=CARTESIAN_POINT ( 'NONE',  ( 47.00000000000000000, 0.000000000000000000, 0.000000000000000000 ) ) ;
#67619=LINE ( 'NONE', #24131, #55768 ) ;
#67648=ORIENTED_EDGE ( 'NONE', *, *, #15597, .T. ) ;
#67668=AXIS2_PLACEMENT_3D ( 'NONE', #31488, #9562, #63660 ) ;
#67675=AXIS2_PLACEMENT_3D ( 'NONE', #62284, #46722, #13852 ) ;
#67679=AXIS2_PLACEMENT_3D ( 'NONE', #41586, #63156, #36285 ) ;
#67686=VERTEX_POINT ( 'NONE', #57726 ) ;
#67693=DIRECTION ( 'NONE',  ( 0.000000000000000000, 0.000000000000000000, -1.000000000000000000 ) ) ;
#67696=FACE_BOUND ( 'NONE', #13427, .T. ) ;
#67698=LINE ( 'NONE', #24918, #29661 ) ;
#67700=DIRECTION ( 'NONE',  ( 0.000000000000000000, 0.000000000000000000, -1.000000000000000000 ) ) ;
#67703=DIRECTION ( 'NONE',  ( 0.000000000000000000, 1.000000000000000000, 0.000000000000000000 ) ) ;
#67708=AXIS2_PLACEMENT_3D ( 'NONE', #41626, #20756, #69894 ) ;
#67709=DIRECTION ( 'NONE',  ( -1.000000000000000000, 0.000000000000000000, 0.000000000000000000 ) ) ;
#67710=VERTEX_POINT ( 'NONE', #31919 ) ;
#67713=DIRECTION ( 'NONE',  ( -1.000000000000000000, 0.000000000000000000, 0.000000000000000000 ) ) ;
#67716=CARTESIAN_POINT ( 'NONE',  ( 0.000000000000000000, -17.79289321881347163, 20.50000000000002487 ) ) ;
#67722=ORIENTED_EDGE ( 'NONE', *, *, #5221, .F. ) ;
#67729=ADVANCED_FACE ( 'NONE', ( #48180 ), #15302, .F. ) ;
#67732=DIRECTION ( 'NONE',  ( 0.000000000000000000, 0.000000000000000000, 1.000000000000000000 ) ) ;
#67734=ORIENTED_EDGE ( 'NONE', *, *, #49956, .T. ) ;
#67736=AXIS2_PLACEMENT_3D ( 'NONE', #40457, #41510, #62015 ) ;
#67737=FACE_OUTER_BOUND ( 'NONE', #17720, .T. ) ;
#67747=EDGE_CURVE ( 'NONE', #9246, #56820, #64442, .T. ) ;
#67754=CARTESIAN_POINT ( 'NONE',  ( 39.00000000000000000, 0.000000000000000000, 0.000000000000000000 ) ) ;
#67755=AXIS2_PLACEMENT_3D ( 'NONE', #46067, #34047, #23458 ) ;
#67756=EDGE_CURVE ( 'NONE', #53390, #51374, #5744, .T. ) ;
#67758=FACE_OUTER_BOUND ( 'NONE', #63797, .T. ) ;
#67760=ORIENTED_EDGE ( 'NONE', *, *, #27585, .F. ) ;
#67779=CARTESIAN_POINT ( 'NONE',  ( 33.89999999999999858, -14.06939075806900874, 20.80000000000001137 ) ) ;
#67788=CARTESIAN_POINT ( 'NONE',  ( 13.90000000000000213, 20.60000000000000142, -13.86939075806900057 ) ) ;
#67800=MANIFOLD_SOLID_BREP ( 'LPattern1[21]', #14891 ) ;
#67804=ORIENTED_EDGE ( 'NONE', *, *, #58509, .F. ) ;
#67810=ORIENTED_EDGE ( 'NONE', *, *, #7984, .F. ) ;
#67823=CIRCLE ( 'NONE', #64462, 2.458500000000000796 ) ;
#67828=CARTESIAN_POINT ( 'NONE',  ( 33.89999999999999858, 0.000000000000000000, 0.000000000000000000 ) ) ;
#67833=CARTESIAN_POINT ( 'NONE',  ( 0.000000000000000000, 20.50000000000000000, -17.79289321881345032 ) ) ;
#67842=EDGE_LOOP ( 'NONE', ( #22443, #22244, #62330, #42764 ) ) ;
#67847=ORIENTED_EDGE ( 'NONE', *, *, #18195, .F. ) ;
#67848=EDGE_CURVE ( 'NONE', #36598, #44196, #1752, .T. ) ;
#67849=CARTESIAN_POINT ( 'NONE',  ( 0.000000000000000000, 20.50000000000000000, -17.79289321881345032 ) ) ;
#67851=LINE ( 'NONE', #19403, #68143 ) ;
#67858=EDGE_CURVE ( 'NONE', #49899, #66965, #44695, .T. ) ;
#67859=FACE_OUTER_BOUND ( 'NONE', #21507, .T. ) ;
#67862=LINE ( 'NONE', #36030, #321 ) ;
#67876=EDGE_LOOP ( 'NONE', ( #7282, #60615, #248, #789 ) ) ;
#67877=DIRECTION ( 'NONE',  ( 1.000000000000000000, -0.000000000000000000, 0.000000000000000000 ) ) ;
#67886=CONICAL_SURFACE ( 'NONE', #3539, 2.458500000000000796, 1.047019301333029784 ) ;
#67909=ORIENTED_EDGE ( 'NONE', *, *, #43239, .F. ) ;
#67912=DIRECTION ( 'NONE',  ( -1.000000000000000000, 0.000000000000000000, 0.000000000000000000 ) ) ;
#67919=VECTOR ( 'NONE', #20286, 1000.000000000000000 ) ;
#67922=EDGE_LOOP ( 'NONE', ( #51282, #9860, #31234, #7551 ) ) ;
#67924=CARTESIAN_POINT ( 'NONE',  ( 25.57999999999999829, 0.000000000000000000, 0.000000000000000000 ) ) ;
#67926=ORIENTED_EDGE ( 'NONE', *, *, #34412, .F. ) ;
#67929=EDGE_LOOP ( 'NONE', ( #53723, #3481, #12055, #3707 ) ) ;
#67937=( NAMED_UNIT ( * ) PLANE_ANGLE_UNIT ( ) SI_UNIT ( $, .RADIAN. ) );
#67943=FILL_AREA_STYLE ('',( #10202 ) ) ;
#67945=EDGE_CURVE ( 'NONE', #39379, #35639, #57130, .T. ) ;
#67946=CARTESIAN_POINT ( 'NONE',  ( 41.09999999999999432, 13.66939075806899950, -20.80000000000000426 ) ) ;
#67973=ORIENTED_EDGE ( 'NONE', *, *, #49660, .T. ) ;
#67976=DIRECTION ( 'NONE',  ( 0.000000000000000000, 0.000000000000000000, -1.000000000000000000 ) ) ;
#67988=CYLINDRICAL_SURFACE ( 'NONE', #10093, 0.5000000000000000000 ) ;
#67989=CARTESIAN_POINT ( 'NONE',  ( 41.09999999999999432, -21.00000000000000000, -13.86939075806900057 ) ) ;
#67994=VECTOR ( 'NONE', #56559, 1000.000000000000000 ) ;
#68001=VERTEX_POINT ( 'NONE', #9217 ) ;
#68005=ORIENTED_EDGE ( 'NONE', *, *, #63689, .T. ) ;
#68012=AXIS2_PLACEMENT_3D ( 'NONE', #12622, #56132, #7676 ) ;
#68015=CARTESIAN_POINT ( 'NONE',  ( 41.09999999999999432, -14.06939075806900163, 20.80000000000000426 ) ) ;
#68021=EDGE_CURVE ( 'NONE', #2849, #67686, #59359, .T. ) ;
#68041=AXIS2_PLACEMENT_3D ( 'NONE', #66029, #17597, #2036 ) ;
#68042=DIRECTION ( 'NONE',  ( 0.000000000000000000, 0.000000000000000000, -1.000000000000000000 ) ) ;
#68051=ORIENTED_EDGE ( 'NONE', *, *, #39684, .F. ) ;
#68064=VECTOR ( 'NONE', #41240, 1000.000000000000000 ) ;
#68083=ORIENTED_EDGE ( 'NONE', *, *, #62615, .T. ) ;
#68095=VECTOR ( 'NONE', #57508, 1000.000000000000000 ) ;
#68109=CARTESIAN_POINT ( 'NONE',  ( 39.00000000000000000, -21.00000000000000000, -14.57806571531351914 ) ) ;
#68129=AXIS2_PLACEMENT_3D ( 'NONE', #46330, #10510, #13455 ) ;
#68143=VECTOR ( 'NONE', #62901, 1000.000000000000000 ) ;
#68168=DIRECTION ( 'NONE',  ( 0.000000000000000000, 0.000000000000000000, 1.000000000000000000 ) ) ;
#68182=ORIENTED_EDGE ( 'NONE', *, *, #7316, .T. ) ;
#68186=VECTOR ( 'NONE', #67148, 1000.000000000000000 ) ;
#68192=AXIS2_PLACEMENT_3D ( 'NONE', #53355, #296, #49764 ) ;
#68197=DIRECTION ( 'NONE',  ( -1.000000000000000000, 0.000000000000000000, 0.000000000000000000 ) ) ;
#68215=EDGE_CURVE ( 'NONE', #30328, #43890, #22941, .T. ) ;
#68218=CARTESIAN_POINT ( 'NONE',  ( 40.90000000000000568, 0.000000000000000000, 0.000000000000000000 ) ) ;
#68226=DIRECTION ( 'NONE',  ( 0.000000000000000000, 0.000000000000000000, 1.000000000000000000 ) ) ;
#68232=ORIENTED_EDGE ( 'NONE', *, *, #10773, .F. ) ;
#68238=AXIS2_PLACEMENT_3D ( 'NONE', #38595, #53829, #21982 ) ;
#68247=VERTEX_POINT ( 'NONE', #10956 ) ;
#68261=EDGE_CURVE ( 'NONE', #53834, #68001, #51527, .T. ) ;
#68274=PLANE ( 'NONE',  #20993 ) ;
#68279=ORIENTED_EDGE ( 'NONE', *, *, #25082, .F. ) ;
#68283=EDGE_CURVE ( 'NONE', #21280, #14789, #7361, .T. ) ;
#68284=AXIS2_PLACEMENT_3D ( 'NONE', #22829, #40118, #34118 ) ;
#68287=CARTESIAN_POINT ( 'NONE',  ( 39.90000000000000568, -0.2000000000000000111, 0.000000000000000000 ) ) ;
#68288=CARTESIAN_POINT ( 'NONE',  ( 18.89999999999999858, -0.1999999999911795112, 8.826273045769999343E-12 ) ) ;
#68306=COLOUR_RGB ( '', 0.66274510, 0.83137255, 0.94901961) ;
#68308=AXIS2_PLACEMENT_3D ( 'NONE', #42287, #6799, #36636 ) ;
#68334=AXIS2_PLACEMENT_3D ( 'NONE', #20209, #41773, #14915 ) ;
#68341=EDGE_CURVE ( 'NONE', #41718, #19639, #50363, .T. ) ;
#68349=EDGE_CURVE ( 'NONE', #47484, #31270, #35268, .T. ) ;
#68355=ADVANCED_FACE ( 'NONE', ( #17973 ), #13010, .F. ) ;
#68358=FACE_OUTER_BOUND ( 'NONE', #9222, .T. ) ;
#68359=ORIENTED_EDGE ( 'NONE', *, *, #7113, .T. ) ;
#68382=LINE ( 'NONE', #47174, #22623 ) ;
#68397=AXIS2_PLACEMENT_3D ( 'NONE', #42082, #52352, #68960 ) ;
#68414=DIRECTION ( 'NONE',  ( -1.000000000000000000, 0.000000000000000000, 0.000000000000000000 ) ) ;
#68432=AXIS2_PLACEMENT_3D ( 'NONE', #18926, #13959, #35518 ) ;
#68438=DIRECTION ( 'NONE',  ( -1.000000000000000000, 0.000000000000000000, 0.000000000000000000 ) ) ;
#68439=LINE ( 'NONE', #9389, #21263 ) ;
#68441=AXIS2_PLACEMENT_3D ( 'NONE', #26059, #68837, #20391 ) ;
#68442=CIRCLE ( 'NONE', #4045, 2.458500000000000796 ) ;
#68444=ORIENTED_EDGE ( 'NONE', *, *, #66660, .T. ) ;
#68454=VERTEX_POINT ( 'NONE', #57210 ) ;
#68457=UNCERTAINTY_MEASURE_WITH_UNIT (LENGTH_MEASURE( 1.000000000000000082E-05 ), #62185, 'distance_accuracy_value', 'NONE');
#68460=DIRECTION ( 'NONE',  ( 1.000000000000000000, -0.000000000000000000, 0.000000000000000000 ) ) ;
#68468=SURFACE_STYLE_FILL_AREA ( #10462 ) ;
#68471=ORIENTED_EDGE ( 'NONE', *, *, #62518, .T. ) ;
#68474=DIRECTION ( 'NONE',  ( 0.000000000000000000, 0.000000000000000000, -1.000000000000000000 ) ) ;
#68475=EDGE_CURVE ( 'NONE', #20196, #40849, #25753, .T. ) ;
#68481=CONICAL_SURFACE ( 'NONE', #40250, 4.000000000000000000, 0.7853981633974476129 ) ;
#68490=VECTOR ( 'NONE', #51220, 1000.000000000000000 ) ;
#68492=CARTESIAN_POINT ( 'NONE',  ( 39.90000000000000568, -0.000000000000000000, -20.80000000000000071 ) ) ;
#68493=AXIS2_PLACEMENT_3D ( 'NONE', #25249, #8973, #42559 ) ;
#68495=AXIS2_PLACEMENT_3D ( 'NONE', #62866, #57557, #26796 ) ;
#68509=LINE ( 'NONE', #20063, #6734 ) ;
#68513=DIRECTION ( 'NONE',  ( 0.000000000000000000, 1.000000000000000000, 0.000000000000000000 ) ) ;
#68514=VERTEX_POINT ( 'NONE', #19713 ) ;
#68516=VERTEX_POINT ( 'NONE', #41646 ) ;
#68522=CARTESIAN_POINT ( 'NONE',  ( 49.00000000000000000, -0.2000000000089119934, 8.909539772616881237E-12 ) ) ;
#68524=CARTESIAN_POINT ( 'NONE',  ( 46.39999999999999858, 21.00000000000000000, -1.250000000000000000 ) ) ;
#68530=PLANE ( 'NONE',  #24791 ) ;
#68534=EDGE_CURVE ( 'NONE', #4520, #22003, #4873, .T. ) ;
#68536=AXIS2_PLACEMENT_3D ( 'NONE', #16897, #290, #27504 ) ;
#68541=PLANE ( 'NONE',  #32252 ) ;
#68542=EDGE_CURVE ( 'NONE', #31770, #36169, #27861, .T. ) ;
#68544=EDGE_LOOP ( 'NONE', ( #53938, #55201, #5899, #50690 ) ) ;
#68551=AXIS2_PLACEMENT_3D ( 'NONE', #20512, #64690, #37826 ) ;
#68556=CARTESIAN_POINT ( 'NONE',  ( 26.90000000000000213, -21.00000000000000000, 13.86939075806900057 ) ) ;
#68563=DIRECTION ( 'NONE',  ( 0.000000000000000000, -0.7071067811865475727, -0.7071067811865475727 ) ) ;
#68566=DIRECTION ( 'NONE',  ( 0.000000000000000000, 0.7071067811865474617, -0.7071067811865474617 ) ) ;
#68580=ADVANCED_FACE ( 'NONE', ( #33122 ), #43742, .F. ) ;
#68587=CYLINDRICAL_SURFACE ( 'NONE', #45858, 25.39999999999999858 ) ;
#68594=CARTESIAN_POINT ( 'NONE',  ( 41.09999999999999432, -14.06939075806901940, -20.80000000000000426 ) ) ;
#68596=DIRECTION ( 'NONE',  ( -0.000000000000000000, -0.7071067811865474617, 0.7071067811865474617 ) ) ;
#68598=FACE_OUTER_BOUND ( 'NONE', #27344, .T. ) ;
#68603=VECTOR ( 'NONE', #38772, 1000.000000000000000 ) ;
#68606=CARTESIAN_POINT ( 'NONE',  ( 29.89999999999999858, 0.000000000000000000, 0.000000000000000000 ) ) ;
#68626=ADVANCED_FACE ( 'NONE', ( #64614 ), #27476, .F. ) ;
#68628=ADVANCED_FACE ( 'NONE', ( #37746 ), #33477, .T. ) ;
#68634=CARTESIAN_POINT ( 'NONE',  ( 49.00000000000000000, 20.60000000000000142, -13.86939075806900057 ) ) ;
#68639=PLANE ( 'NONE',  #15890 ) ;
#68642=VECTOR ( 'NONE', #21332, 1000.000000000000000 ) ;
#68653=CARTESIAN_POINT ( 'NONE',  ( 25.57999999999999829, 0.000000000000000000, 0.000000000000000000 ) ) ;
#68656=EDGE_CURVE ( 'NONE', #43571, #27271, #6417, .T. ) ;
#68660=CARTESIAN_POINT ( 'NONE',  ( 12.90000000000000213, -14.06939075806900163, -20.80000000000000426 ) ) ;
#68665=PLANE ( 'NONE',  #68334 ) ;
#68666=DIRECTION ( 'NONE',  ( 1.000000000000000000, -0.000000000000000000, 0.000000000000000000 ) ) ;
#68678=DIRECTION ( 'NONE',  ( 1.000000000000000000, -0.000000000000000000, 0.000000000000000000 ) ) ;
#68679=VERTEX_POINT ( 'NONE', #59659 ) ;
#68694=VERTEX_POINT ( 'NONE', #55393 ) ;
#68702=ADVANCED_FACE ( 'NONE', ( #50076 ), #66344, .F. ) ;
#68729=LINE ( 'NONE', #30888, #17593 ) ;
#68730=ORIENTED_EDGE ( 'NONE', *, *, #42717, .T. ) ;
#68738=LINE ( 'NONE', #4733, #67919 ) ;
#68748=ADVANCED_FACE ( 'NONE', ( #6933 ), #7634, .T. ) ;
#68767=DIRECTION ( 'NONE',  ( 0.000000000000000000, 0.000000000000000000, -1.000000000000000000 ) ) ;
#68772=ORIENTED_EDGE ( 'NONE', *, *, #51588, .F. ) ;
#68784=EDGE_LOOP ( 'NONE', ( #46440, #35768 ) ) ;
#68795=CIRCLE ( 'NONE', #1061, 24.99999999998784972 ) ;
#68807=DIRECTION ( 'NONE',  ( 0.000000000000000000, -0.7071067811865475727, 0.7071067811865475727 ) ) ;
#68808=FACE_OUTER_BOUND ( 'NONE', #15335, .T. ) ;
#68810=VERTEX_POINT ( 'NONE', #40858 ) ;
#68820=ORIENTED_EDGE ( 'NONE', *, *, #19159, .F. ) ;
#68835=( NAMED_UNIT ( * ) PLANE_ANGLE_UNIT ( ) SI_UNIT ( $, .RADIAN. ) );
#68837=DIRECTION ( 'NONE',  ( 0.000000000000000000, -1.000000000000000000, 0.000000000000000000 ) ) ;
#68850=CARTESIAN_POINT ( 'NONE',  ( 39.00000000000000000, 0.000000000000000000, 5.000000000000000000 ) ) ;
#68851=LINE ( 'NONE', #43012, #33107 ) ;
#68866=DIRECTION ( 'NONE',  ( 0.000000000000000000, -0.7071067811865474617, -0.7071067811865474617 ) ) ;
#68871=LINE ( 'NONE', #62150, #14078 ) ;
#68884=ORIENTED_EDGE ( 'NONE', *, *, #5151, .T. ) ;
#68898=VECTOR ( 'NONE', #29246, 1000.000000000000000 ) ;
#68905=DIRECTION ( 'NONE',  ( -1.000000000000000000, 0.000000000000000000, -0.000000000000000000 ) ) ;
#68922=FACE_OUTER_BOUND ( 'NONE', #46001, .T. ) ;
#68924=AXIS2_PLACEMENT_3D ( 'NONE', #8789, #40607, #62167 ) ;
#68932=DIRECTION ( 'NONE',  ( 0.000000000000000000, 0.000000000000000000, -1.000000000000000000 ) ) ;
#68945=AXIS2_PLACEMENT_3D ( 'NONE', #56991, #12542, #8549 ) ;
#68959=EDGE_CURVE ( 'NONE', #59745, #54092, #69720, .T. ) ;
#68960=DIRECTION ( 'NONE',  ( 0.000000000000000000, 0.000000000000000000, -1.000000000000000000 ) ) ;
#68979=CARTESIAN_POINT ( 'NONE',  ( 16.89999999999999858, -0.1999999999911430404, -8.864436962241481021E-12 ) ) ;
#68980=VECTOR ( 'NONE', #48027, 1000.000000000000000 ) ;
#68986=ORIENTED_EDGE ( 'NONE', *, *, #15122, .F. ) ;
#69001=ORIENTED_EDGE ( 'NONE', *, *, #15266, .F. ) ;
#69004=ADVANCED_FACE ( 'NONE', ( #50929 ), #14867, .T. ) ;
#69005=CARTESIAN_POINT ( 'NONE',  ( 21.90000000000000213, 13.66939075806899240, 20.79999999999999361 ) ) ;
#69010=DIRECTION ( 'NONE',  ( 1.000000000000000000, -0.000000000000000000, 0.000000000000000000 ) ) ;
#69031=VERTEX_POINT ( 'NONE', #42776 ) ;
#69033=VECTOR ( 'NONE', #59514, 1000.000000000000000 ) ;
#69052=ORIENTED_EDGE ( 'NONE', *, *, #65547, .T. ) ;
#69060=ORIENTED_EDGE ( 'NONE', *, *, #52163, .T. ) ;
#69069=ADVANCED_FACE ( 'NONE', ( #65048 ), #54095, .F. ) ;
#69091=CARTESIAN_POINT ( 'NONE',  ( 39.90000000000000568, 13.66939075806899240, 20.79999999999999361 ) ) ;
#69095=ORIENTED_EDGE ( 'NONE', *, *, #32749, .T. ) ;
#69107=LINE ( 'NONE', #58147, #42595 ) ;
#69115=DIRECTION ( 'NONE',  ( -1.000000000000000000, 0.000000000000000000, 0.000000000000000000 ) ) ;
#69137=EDGE_CURVE ( 'NONE', #5466, #13881, #29010, .T. ) ;
#69153=DIRECTION ( 'NONE',  ( -1.000000000000000000, 0.000000000000000000, 0.000000000000000000 ) ) ;
#69158=AXIS2_PLACEMENT_3D ( 'NONE', #34887, #34541, #35956 ) ;
#69163=ORIENTED_EDGE ( 'NONE', *, *, #54319, .F. ) ;
#69167=PRESENTATION_STYLE_ASSIGNMENT (( #41945 ) ) ;
#69170=LINE ( 'NONE', #37692, #35828 ) ;
#69173=AXIS2_PLACEMENT_3D ( 'NONE', #22827, #6225, #11171 ) ;
#69183=ORIENTED_EDGE ( 'NONE', *, *, #29444, .T. ) ;
#69186=VECTOR ( 'NONE', #30784, 1000.000000000000000 ) ;
#69191=DIRECTION ( 'NONE',  ( 0.000000000000000000, 0.000000000000000000, -1.000000000000000000 ) ) ;
#69200=CARTESIAN_POINT ( 'NONE',  ( 39.00000000000000000, -21.00000000000000000, 14.57806571531351914 ) ) ;
#69208=ORIENTED_EDGE ( 'NONE', *, *, #69547, .T. ) ;
#69222=CARTESIAN_POINT ( 'NONE',  ( 0.5000000000000000000, -18.00000000000000355, -21.00000000000000000 ) ) ;
#69248=( NAMED_UNIT ( * ) PLANE_ANGLE_UNIT ( ) SI_UNIT ( $, .RADIAN. ) );
#69250=CARTESIAN_POINT ( 'NONE',  ( 46.39999999999999858, 33.00000000000000000, -0.7500000000000000000 ) ) ;
#69251=ORIENTED_EDGE ( 'NONE', *, *, #46307, .F. ) ;
#69252=CARTESIAN_POINT ( 'NONE',  ( 49.00000000000000000, -0.1999999999911795112, 8.826273045769999343E-12 ) ) ;
#69255=PLANE ( 'NONE',  #47858 ) ;
#69259=CARTESIAN_POINT ( 'NONE',  ( 28.90000000000000213, -0.2000000000089119934, -8.913009219568841313E-12 ) ) ;
#69271=DIRECTION ( 'NONE',  ( 0.6785983445458472207, 0.6785983445458458885, 0.2810846377148227826 ) ) ;
#69281=CARTESIAN_POINT ( 'NONE',  ( 41.09999999999999432, 13.66939075806899950, -20.80000000000000426 ) ) ;
#69282=FACE_OUTER_BOUND ( 'NONE', #13368, .T. ) ;
#69286=DIRECTION ( 'NONE',  ( 0.000000000000000000, 0.000000000000000000, -1.000000000000000000 ) ) ;
#69301=VECTOR ( 'NONE', #29423, 1000.000000000000114 ) ;
#69311=DIRECTION ( 'NONE',  ( 1.000000000000000000, -0.000000000000000000, -0.000000000000000000 ) ) ;
#69321=ORIENTED_EDGE ( 'NONE', *, *, #30201, .T. ) ;
#69324=VERTEX_POINT ( 'NONE', #30338 ) ;
#69345=CARTESIAN_POINT ( 'NONE',  ( 39.00000000000000000, 0.000000000000000000, 2.458500000000000796 ) ) ;
#69349=VECTOR ( 'NONE', #51252, 1000.000000000000000 ) ;
#69353=CARTESIAN_POINT ( 'NONE',  ( 34.89999999999999858, 3.010794155703768650E-16, -2.458500000000000796 ) ) ;
#69359=ORIENTED_EDGE ( 'NONE', *, *, #31436, .F. ) ;
#69365=VECTOR ( 'NONE', #25831, 1000.000000000000000 ) ;
#69366=DIRECTION ( 'NONE',  ( -1.000000000000000000, 0.000000000000000000, 0.000000000000000000 ) ) ;
#69373=CARTESIAN_POINT ( 'NONE',  ( 29.89999999999999858, -0.2000000000089119934, -8.913009219568841313E-12 ) ) ;
#69384=DIRECTION ( 'NONE',  ( 0.000000000000000000, 0.000000000000000000, -1.000000000000000000 ) ) ;
#69385=AXIS2_PLACEMENT_3D ( 'NONE', #51987, #62947, #2485 ) ;
#69390=ORIENTED_EDGE ( 'NONE', *, *, #33995, .T. ) ;
#69395=PLANE ( 'NONE',  #58092 ) ;
#69402=VERTEX_POINT ( 'NONE', #2411 ) ;
#69404=EDGE_CURVE ( 'NONE', #21068, #28, #50840, .T. ) ;
#69409=AXIS2_PLACEMENT_3D ( 'NONE', #8480, #7781, #18385 ) ;
#69419=ORIENTED_EDGE ( 'NONE', *, *, #32159, .T. ) ;
#69438=CIRCLE ( 'NONE', #20878, 3.500000000000000000 ) ;
#69441=DIRECTION ( 'NONE',  ( 0.000000000000000000, 0.000000000000000000, -1.000000000000000000 ) ) ;
#69464=PLANE ( 'NONE',  #64513 ) ;
#69466=CARTESIAN_POINT ( 'NONE',  ( 15.89999999999999680, 20.60000000000000142, -13.86939075806900057 ) ) ;
#69470=DIRECTION ( 'NONE',  ( -1.000000000000000000, 0.000000000000000000, 0.000000000000000000 ) ) ;
#69472=EDGE_CURVE ( 'NONE', #35639, #39379, #31367, .T. ) ;
#69507=COLOUR_RGB ( '', 0.66274510, 0.83137255, 0.94901961) ;
#69510=CIRCLE ( 'NONE', #61606, 24.99999999998789946 ) ;
#69512=ORIENTED_EDGE ( 'NONE', *, *, #40723, .T. ) ;
#69514=SURFACE_STYLE_USAGE ( .BOTH. , #4126 ) ;
#69532=DIRECTION ( 'NONE',  ( 0.000000000000000000, 0.000000000000000000, 1.000000000000000000 ) ) ;
#69547=EDGE_CURVE ( 'NONE', #2059, #25912, #15131, .T. ) ;
#69558=CARTESIAN_POINT ( 'NONE',  ( 29.89999999999999858, 3.010794155703768650E-16, -2.458500000000000796 ) ) ;
#69562=STYLED_ITEM ( 'NONE', ( #59824 ), #67800 ) ;
#69574=DIRECTION ( 'NONE',  ( -1.000000000000000000, 0.000000000000000000, 0.000000000000000000 ) ) ;
#69579=VERTEX_POINT ( 'NONE', #47647 ) ;
#69581=MECHANICAL_DESIGN_GEOMETRIC_PRESENTATION_REPRESENTATION('',(#29882),#63926);
#69582=DIRECTION ( 'NONE',  ( 0.000000000000000000, 0.000000000000000000, -1.000000000000000000 ) ) ;
#69583=DIRECTION ( 'NONE',  ( -1.000000000000000000, 0.000000000000000000, 0.000000000000000000 ) ) ;
#69587=ORIENTED_EDGE ( 'NONE', *, *, #56988, .T. ) ;
#69598=CARTESIAN_POINT ( 'NONE',  ( 47.00000000000000000, -0.7500000000000000000, -4.943429983321300014 ) ) ;
#69599=CIRCLE ( 'NONE', #35647, 24.99999999998789946 ) ;
#69611=ORIENTED_EDGE ( 'NONE', *, *, #46240, .F. ) ;
#69616=VECTOR ( 'NONE', #32869, 1000.000000000000000 ) ;
#69618=CARTESIAN_POINT ( 'NONE',  ( 39.00000000000000000, 0.000000000000000000, 5.000000000000000000 ) ) ;
#69620=AXIS2_PLACEMENT_3D ( 'NONE', #2783, #51587, #51224 ) ;
#69632=DIRECTION ( 'NONE',  ( 0.000000000000000000, 0.000000000000000000, 1.000000000000000000 ) ) ;
#69634=EDGE_CURVE ( 'NONE', #51627, #19691, #11538, .T. ) ;
#69648=EDGE_LOOP ( 'NONE', ( #46128, #33196, #15422, #56421, #53877 ) ) ;
#69649=FACE_OUTER_BOUND ( 'NONE', #61522, .T. ) ;
#69671=ORIENTED_EDGE ( 'NONE', *, *, #41435, .T. ) ;
#69691=ORIENTED_EDGE ( 'NONE', *, *, #21859, .F. ) ;
#69700=VERTEX_POINT ( 'NONE', #7273 ) ;
#69707=DIRECTION ( 'NONE',  ( -0.000000000000000000, -1.000000000000000000, 0.000000000000000000 ) ) ;
#69709=CIRCLE ( 'NONE', #43698, 25.39999999999999858 ) ;
#69711=ORIENTED_EDGE ( 'NONE', *, *, #541, .T. ) ;
#69720=CIRCLE ( 'NONE', #20034, 24.99999999998784972 ) ;
#69722=DIRECTION ( 'NONE',  ( 1.000000000000000000, -0.000000000000000000, -0.000000000000000000 ) ) ;
#69723=EDGE_CURVE ( 'NONE', #14509, #12, #16867, .T. ) ;
#69730=EDGE_CURVE ( 'NONE', #33533, #49649, #37015, .T. ) ;
#69740=CARTESIAN_POINT ( 'NONE',  ( 41.09999999999999432, -21.00000000000000000, 13.86939075806900057 ) ) ;
#69752=DIRECTION ( 'NONE',  ( 0.000000000000000000, -1.000000000000000000, 0.000000000000000000 ) ) ;
#69760=DIRECTION ( 'NONE',  ( -1.000000000000000000, 0.000000000000000000, 0.000000000000000000 ) ) ;
#69768=EDGE_CURVE ( 'NONE', #30390, #55486, #22176, .T. ) ;
#69796=DIRECTION ( 'NONE',  ( 0.000000000000000000, -1.000000000000000000, 0.000000000000000000 ) ) ;
#69797=DIRECTION ( 'NONE',  ( 0.000000000000000000, 0.000000000000000000, 1.000000000000000000 ) ) ;
#69800=DIRECTION ( 'NONE',  ( 1.000000000000000000, -0.000000000000000000, 0.000000000000000000 ) ) ;
#69801=ORIENTED_EDGE ( 'NONE', *, *, #25759, .T. ) ;
#69802=LINE ( 'NONE', #25626, #52851 ) ;
#69804=SURFACE_STYLE_USAGE ( .BOTH. , #16400 ) ;
#69805=VECTOR ( 'NONE', #21891, 1000.000000000000000 ) ;
#69810=ADVANCED_FACE ( 'NONE', ( #51823 ), #35187, .F. ) ;
#69813=DIRECTION ( 'NONE',  ( 0.000000000000000000, -1.000000000000000000, 0.000000000000000000 ) ) ;
#69818=CARTESIAN_POINT ( 'NONE',  ( 19.90000000000000213, 20.60000000000000142, 13.86939075806899702 ) ) ;
#69823=ADVANCED_FACE ( 'NONE', ( #14351 ), #2332, .T. ) ;
#69831=ORIENTED_EDGE ( 'NONE', *, *, #26676, .T. ) ;
#69832=VERTEX_POINT ( 'NONE', #51115 ) ;
#69838=CARTESIAN_POINT ( 'NONE',  ( 19.90000000000000213, -0.2000000000089119934, 8.909539772616881237E-12 ) ) ;
#69845=UNCERTAINTY_MEASURE_WITH_UNIT (LENGTH_MEASURE( 1.000000000000000082E-05 ), #9067, 'distance_accuracy_value', 'NONE');
#69846=FACE_OUTER_BOUND ( 'NONE', #8547, .T. ) ;
#69852=ORIENTED_EDGE ( 'NONE', *, *, #23611, .T. ) ;
#69856=EDGE_CURVE ( 'NONE', #54625, #40050, #60750, .T. ) ;
#69863=ORIENTED_EDGE ( 'NONE', *, *, #45997, .F. ) ;
#69870=CARTESIAN_POINT ( 'NONE',  ( 15.89999999999999680, 13.66939075806899240, -20.79999999999999361 ) ) ;
#69881=LINE ( 'NONE', #21446, #46771 ) ;
#69894=DIRECTION ( 'NONE',  ( 0.000000000000000000, 0.000000000000000000, 1.000000000000000000 ) ) ;
#69902=DIRECTION ( 'NONE',  ( 0.000000000000000000, 0.000000000000000000, -1.000000000000000000 ) ) ;
#69926=ADVANCED_FACE ( 'NONE', ( #31330 ), #9031, .F. ) ;
#69937=ORIENTED_EDGE ( 'NONE', *, *, #65444, .T. ) ;
#69946=ADVANCED_FACE ( 'NONE', ( #15043 ), #21395, .F. ) ;
#69952=EDGE_CURVE ( 'NONE', #4860, #66079, #68439, .T. ) ;
#69955=CIRCLE ( 'NONE', #49610, 3.500000000000000000 ) ;
#69964=ORIENTED_EDGE ( 'NONE', *, *, #22420, .T. ) ;
#69972=EDGE_LOOP ( 'NONE', ( #66699, #15520 ) ) ;
#69975=ORIENTED_EDGE ( 'NONE', *, *, #12286, .F. ) ;
ENDSEC;
END-ISO-10303-21;
